ISO-10303-21;
HEADER;
FILE_DESCRIPTION (('STEP AP214'),
    '1' );
FILE_NAME ('Inlet Housing.step',
    '2026-10-23T18:01:19',
    ( '' ),
    ( '' ),
    'SwSTEP 2.0',
    'SolidWorks 2025',
    '' );
FILE_SCHEMA (( 'AUTOMOTIVE_DESIGN' ));
ENDSEC;

DATA;
#1=ORIENTED_EDGE ( 'NONE', *, *, #12221, .T. ) ;
#9=DIRECTION ( 'NONE',  ( 0.000000000000000000, 1.000000000000000000, 0.000000000000000000 ) ) ;
#10=DIRECTION ( 'NONE',  ( 0.000000000000000000, 0.000000000000000000, 1.000000000000000000 ) ) ;
#11=ORIENTED_EDGE ( 'NONE', *, *, #1358, .T. ) ;
#18=CARTESIAN_POINT ( 'NONE',  ( 3.512958614626789711, 1.913572711384756708, -0.7285857137282393259 ) ) ;
#19=ORIENTED_EDGE ( 'NONE', *, *, #5081, .F. ) ;
#29=CARTESIAN_POINT ( 'NONE',  ( 3.875000000000000000, 1.885381157978844868, -0.5000000000000002220 ) ) ;
#33=CARTESIAN_POINT ( 'NONE',  ( 4.627329080935005834, 1.724141250851881191, -0.2956774535502572077 ) ) ;
#42=EDGE_CURVE ( 'NONE', #4100, #13687, #5470, .T. ) ;
#45=ORIENTED_EDGE ( 'NONE', *, *, #8856, .F. ) ;
#47=DIRECTION ( 'NONE',  ( -1.000000000000000000, -0.000000000000000000, -0.000000000000000000 ) ) ;
#52=EDGE_CURVE ( 'NONE', #3395, #10754, #14120, .T. ) ;
#58=ORIENTED_EDGE ( 'NONE', *, *, #5402, .F. ) ;
#60=CARTESIAN_POINT ( 'NONE',  ( 3.426491571325181340, -1.679378605318059048, -1.679378605318041950 ) ) ;
#63=ORIENTED_EDGE ( 'NONE', *, *, #4346, .F. ) ;
#65=DIRECTION ( 'NONE',  ( 0.000000000000000000, 0.000000000000000000, 1.000000000000000000 ) ) ;
#66=ORIENTED_EDGE ( 'NONE', *, *, #9058, .F. ) ;
#69=AXIS2_PLACEMENT_3D ( 'NONE', #6911, #5755, #13762 ) ;
#76=DIRECTION ( 'NONE',  ( 0.3420201433256623846, 0.000000000000000000, 0.9396926207859106484 ) ) ;
#78=EDGE_CURVE ( 'NONE', #7551, #8303, #4616, .T. ) ;
#83=AXIS2_PLACEMENT_3D ( 'NONE', #10254, #9341, #11313 ) ;
#89=EDGE_LOOP ( 'NONE', ( #7077, #10683, #6520, #11153 ) ) ;
#90=ORIENTED_EDGE ( 'NONE', *, *, #12016, .T. ) ;
#101=AXIS2_PLACEMENT_3D ( 'NONE', #4920, #3459, #11799 ) ;
#104=FACE_OUTER_BOUND ( 'NONE', #11519, .T. ) ;
#106=CARTESIAN_POINT ( 'NONE',  ( 4.657203315104130326, 1.728603760376735909, 0.2078873897356731115 ) ) ;
#107=ORIENTED_EDGE ( 'NONE', *, *, #12678, .F. ) ;
#110=ORIENTED_EDGE ( 'NONE', *, *, #10895, .T. ) ;
#111=CIRCLE ( 'NONE', #4039, 0.3750000000000004996 ) ;
#114=VERTEX_POINT ( 'NONE', #12839 ) ;
#115=CARTESIAN_POINT ( 'NONE',  ( 6.826491571325181695, 0.000000000000000000, 0.000000000000000000 ) ) ;
#117=CARTESIAN_POINT ( 'NONE',  ( 2.774999999999999911, 3.360000000000016751, 0.9799999999999461364 ) ) ;
#122=CARTESIAN_POINT ( 'NONE',  ( 3.874999999999999556, 2.750000000000000000, -1.320000000000000062 ) ) ;
#123=CIRCLE ( 'NONE', #13312, 0.2944999999999987073 ) ;
#124=CIRCLE ( 'NONE', #8691, 0.9999999999999996669 ) ;
#129=AXIS2_PLACEMENT_3D ( 'NONE', #12929, #1218, #11933 ) ;
#147=EDGE_CURVE ( 'NONE', #7267, #14527, #433, .T. ) ;
#149=CONICAL_SURFACE ( 'NONE', #9948, 0.2944999999999987073, 0.7853981633974366217 ) ;
#150=CARTESIAN_POINT ( 'NONE',  ( 3.875000000000000000, 3.137999999999999901, 0.5000000000000002220 ) ) ;
#156=EDGE_CURVE ( 'NONE', #504, #12467, #11937, .T. ) ;
#159=VERTEX_POINT ( 'NONE', #11630 ) ;
#161=CARTESIAN_POINT ( 'NONE',  ( 3.426491571325181340, -1.679378605318041950, 1.384878605318060174 ) ) ;
#166=ORIENTED_EDGE ( 'NONE', *, *, #13997, .F. ) ;
#168=DIRECTION ( 'NONE',  ( 1.000000000000000000, 0.000000000000000000, 0.000000000000000000 ) ) ;
#170=EDGE_LOOP ( 'NONE', ( #1546, #1638, #4736, #4813 ) ) ;
#172=DIRECTION ( 'NONE',  ( 1.000000000000000000, 0.000000000000000000, 0.000000000000000000 ) ) ;
#178=CARTESIAN_POINT ( 'NONE',  ( 3.652559170054249904, 1.936257245559476869, -0.4479448007622380823 ) ) ;
#182=DIRECTION ( 'NONE',  ( 0.000000000000000000, 0.000000000000000000, -1.000000000000000000 ) ) ;
#187=ORIENTED_EDGE ( 'NONE', *, *, #8888, .T. ) ;
#190=CARTESIAN_POINT ( 'NONE',  ( 3.426491571325181340, 0.000000000000000000, 0.000000000000000000 ) ) ;
#192=FACE_BOUND ( 'NONE', #6135, .T. ) ;
#201=AXIS2_PLACEMENT_3D ( 'NONE', #268, #9637, #13052 ) ;
#203=PLANE ( 'NONE',  #5048 ) ;
#205=LINE ( 'NONE', #13137, #4871 ) ;
#206=CARTESIAN_POINT ( 'NONE',  ( 4.545987629778766248, 1.714706108888804481, 0.4425078797212881887 ) ) ;
#207=ORIENTED_EDGE ( 'NONE', *, *, #6693, .F. ) ;
#210=DIRECTION ( 'NONE',  ( -1.000000000000000000, -0.000000000000000000, -0.000000000000000000 ) ) ;
#215=LENGTH_MEASURE_WITH_UNIT ( LENGTH_MEASURE( 0.02539999999999999897 ), #6283 );
#218=CARTESIAN_POINT ( 'NONE',  ( 6.787121492585022509, 0.000000000000000000, 0.000000000000000000 ) ) ;
#226=PLANE ( 'NONE',  #3739 ) ;
#228=ORIENTED_EDGE ( 'NONE', *, *, #3551, .T. ) ;
#230=ORIENTED_EDGE ( 'NONE', *, *, #13541, .F. ) ;
#235=EDGE_CURVE ( 'NONE', #5730, #4833, #8634, .T. ) ;
#239=FACE_OUTER_BOUND ( 'NONE', #14821, .T. ) ;
#240=DIRECTION ( 'NONE',  ( -0.000000000000000000, 1.000000000000000000, -0.000000000000000000 ) ) ;
#252=DIRECTION ( 'NONE',  ( -1.150251786806006500E-15, 0.000000000000000000, 1.000000000000000000 ) ) ;
#254=CYLINDRICAL_SURFACE ( 'NONE', #1961, 2.500000000000000444 ) ;
#255=EDGE_CURVE ( 'NONE', #14724, #7714, #12509, .T. ) ;
#258=DIRECTION ( 'NONE',  ( -1.000000000000000000, -0.000000000000000000, -0.000000000000000000 ) ) ;
#263=ORIENTED_EDGE ( 'NONE', *, *, #11976, .T. ) ;
#268=CARTESIAN_POINT ( 'NONE',  ( 6.826491571325181695, 1.679378605318059492, 1.679378605318041506 ) ) ;
#269=CARTESIAN_POINT ( 'NONE',  ( 2.807000000000000828, 1.679378605318042395, -1.679378605318058604 ) ) ;
#270=TOROIDAL_SURFACE ( 'NONE', #12014, 0.5849999999999996314, 0.1000000000000000056 ) ;
#274=DIRECTION ( 'NONE',  ( -1.000000000000000000, -0.000000000000000000, -0.000000000000000000 ) ) ;
#275=CARTESIAN_POINT ( 'NONE',  ( 3.598246013678398914, 1.876591252814830524, 0.7602127166807192138 ) ) ;
#279=ORIENTED_EDGE ( 'NONE', *, *, #7763, .F. ) ;
#293=CARTESIAN_POINT ( 'NONE',  ( 6.826491571325181695, 1.679378605318059492, 1.272378605318041478 ) ) ;
#295=CARTESIAN_POINT ( 'NONE',  ( 6.208491571325183145, -1.679378605318047946, -1.679378605318053497 ) ) ;
#296=ORIENTED_EDGE ( 'NONE', *, *, #3192, .T. ) ;
#300=ORIENTED_EDGE ( 'NONE', *, *, #13461, .F. ) ;
#301=FACE_OUTER_BOUND ( 'NONE', #6779, .T. ) ;
#302=AXIS2_PLACEMENT_3D ( 'NONE', #1388, #8381, #4776 ) ;
#303=CARTESIAN_POINT ( 'NONE',  ( 6.176491571325181340, 1.679378605318035733, -1.272378605318063016 ) ) ;
#306=CARTESIAN_POINT ( 'NONE',  ( 6.826491571325181695, -1.679378605318048390, 1.272378605318051914 ) ) ;
#307=EDGE_CURVE ( 'NONE', #9198, #11593, #9851, .T. ) ;
#314=DIRECTION ( 'NONE',  ( 0.000000000000000000, 0.000000000000000000, -1.000000000000000000 ) ) ;
#316=ADVANCED_FACE ( 'NONE', ( #874 ), #6177, .F. ) ;
#317=DIRECTION ( 'NONE',  ( 0.000000000000000000, 1.000000000000000000, 0.000000000000000000 ) ) ;
#320=AXIS2_PLACEMENT_3D ( 'NONE', #8571, #13282, #12223 ) ;
#323=DIRECTION ( 'NONE',  ( 0.000000000000000000, 0.000000000000000000, 1.000000000000000000 ) ) ;
#326=CARTESIAN_POINT ( 'NONE',  ( 4.309703551682574130, 1.729087785011442335, -0.6133796147049294101 ) ) ;
#327=VERTEX_POINT ( 'NONE', #12220 ) ;
#328=DIRECTION ( 'NONE',  ( 0.000000000000000000, 0.000000000000000000, 1.000000000000000000 ) ) ;
#331=VERTEX_POINT ( 'NONE', #646 ) ;
#332=DIRECTION ( 'NONE',  ( 0.000000000000000000, 0.000000000000000000, 1.000000000000000000 ) ) ;
#334=CIRCLE ( 'NONE', #14035, 2.000179419058113695 ) ;
#335=CARTESIAN_POINT ( 'NONE',  ( 3.426491571325181340, -2.360000000000016751, -0.9799999999999431388 ) ) ;
#337=CARTESIAN_POINT ( 'NONE',  ( 3.426491571325181340, 0.000000000000000000, 0.000000000000000000 ) ) ;
#339=DIRECTION ( 'NONE',  ( 0.7071067811865551223, 0.000000000000000000, -0.7071067811865400232 ) ) ;
#341=ADVANCED_FACE ( 'NONE', ( #14586 ), #4119, .F. ) ;
#344=CIRCLE ( 'NONE', #11853, 2.500000000000000444 ) ;
#345=DIRECTION ( 'NONE',  ( 0.000000000000000000, 0.000000000000000000, -1.000000000000000000 ) ) ;
#349=CARTESIAN_POINT ( 'NONE',  ( 3.707746441153773720, 1.919327537284637453, 0.7315114958933836009 ) ) ;
#351=ORIENTED_EDGE ( 'NONE', *, *, #3241, .T. ) ;
#352=DIRECTION ( 'NONE',  ( 1.000000000000000000, 0.000000000000000000, 0.000000000000000000 ) ) ;
#353=DIRECTION ( 'NONE',  ( 0.000000000000000000, 0.000000000000000000, 1.000000000000000000 ) ) ;
#355=VERTEX_POINT ( 'NONE', #1882 ) ;
#361=FACE_OUTER_BOUND ( 'NONE', #10619, .T. ) ;
#363=AXIS2_PLACEMENT_3D ( 'NONE', #408, #6258, #3029 ) ;
#384=DIRECTION ( 'NONE',  ( -1.000000000000000000, -0.000000000000000000, -0.000000000000000000 ) ) ;
#386=FACE_OUTER_BOUND ( 'NONE', #3561, .T. ) ;
#387=DIRECTION ( 'NONE',  ( 0.000000000000000000, 1.000000000000000000, 0.000000000000000000 ) ) ;
#391=VERTEX_POINT ( 'NONE', #5798 ) ;
#398=VECTOR ( 'NONE', #13183, 39.37007874015748143 ) ;
#399=CARTESIAN_POINT ( 'NONE',  ( 4.330797523564109852, 1.779041412359303020, -0.5988230613860490159 ) ) ;
#400=DIRECTION ( 'NONE',  ( -0.000000000000000000, 1.000000000000000000, 1.224646799147353207E-16 ) ) ;
#402=CARTESIAN_POINT ( 'NONE',  ( 4.468111723579847983, 1.731463736471003267, -0.4625016237982221279 ) ) ;
#404=ORIENTED_EDGE ( 'NONE', *, *, #6402, .T. ) ;
#405=ORIENTED_EDGE ( 'NONE', *, *, #14962, .F. ) ;
#408=CARTESIAN_POINT ( 'NONE',  ( 6.176491571325181340, 1.679378605318059492, 1.679378605318041506 ) ) ;
#411=EDGE_LOOP ( 'NONE', ( #4478, #9500, #8078, #9517 ) ) ;
#412=CARTESIAN_POINT ( 'NONE',  ( 6.826491571325181695, -1.679378605318048390, 2.054378605318054607 ) ) ;
#418=ADVANCED_FACE ( 'NONE', ( #3344 ), #2756, .F. ) ;
#419=FACE_BOUND ( 'NONE', #11728, .T. ) ;
#423=DIRECTION ( 'NONE',  ( 0.000000000000000000, 0.000000000000000000, -1.000000000000000000 ) ) ;
#424=CARTESIAN_POINT ( 'NONE',  ( 3.779260009907372098, 1.809000757605977894, 0.7955663742672792749 ) ) ;
#426=ORIENTED_EDGE ( 'NONE', *, *, #1651, .T. ) ;
#428=FACE_BOUND ( 'NONE', #2478, .T. ) ;
#430=CIRCLE ( 'NONE', #4372, 1.999999999999999334 ) ;
#433=CIRCLE ( 'NONE', #15106, 0.5000000000000001110 ) ;
#435=CARTESIAN_POINT ( 'NONE',  ( 3.426491571325181340, 2.360000000000015863, 1.574999999999999956 ) ) ;
#437=CIRCLE ( 'NONE', #2657, 0.1000000000000000194 ) ;
#439=AXIS2_PLACEMENT_3D ( 'NONE', #4419, #13876, #8096 ) ;
#444=ORIENTED_EDGE ( 'NONE', *, *, #8806, .T. ) ;
#445=AXIS2_PLACEMENT_3D ( 'NONE', #7590, #1692, #9968 ) ;
#449=ADVANCED_FACE ( 'NONE', ( #9398 ), #8141, .F. ) ;
#450=ORIENTED_EDGE ( 'NONE', *, *, #13190, .T. ) ;
#452=CARTESIAN_POINT ( 'NONE',  ( 3.426491571325181340, 3.137999999999999901, -0.2209981660730358233 ) ) ;
#455=DIRECTION ( 'NONE',  ( 1.000000000000000000, 0.000000000000000000, 0.000000000000000000 ) ) ;
#457=ADVANCED_FACE ( 'NONE', ( #2193 ), #10309, .T. ) ;
#458=DIRECTION ( 'NONE',  ( -0.000000000000000000, 1.000000000000000000, -0.000000000000000000 ) ) ;
#459=CIRCLE ( 'NONE', #8798, 0.4070000000000022489 ) ;
#464=ORIENTED_EDGE ( 'NONE', *, *, #6124, .F. ) ;
#470=CARTESIAN_POINT ( 'NONE',  ( 3.426491571325181340, 0.000000000000000000, 2.500000000000000444 ) ) ;
#471=CARTESIAN_POINT ( 'NONE',  ( 3.394491571325183088, -1.679378605318041950, 1.941878605318059003 ) ) ;
#474=CARTESIAN_POINT ( 'NONE',  ( 4.041559342806273492, 1.811112142523843005, 0.7320156718295878218 ) ) ;
#475=CARTESIAN_POINT ( 'NONE',  ( 4.249538226556600407, 1.782304664937925498, -0.6509308308851882163 ) ) ;
#477=EDGE_LOOP ( 'NONE', ( #13690, #3186, #11488, #1344 ) ) ;
#484=CARTESIAN_POINT ( 'NONE',  ( 6.208491571325183145, 1.679378605318059492, 1.304378605318041062 ) ) ;
#495=CARTESIAN_POINT ( 'NONE',  ( 3.370072511834198981, 1.982174769829836869, 0.6499189952005048898 ) ) ;
#496=ADVANCED_FACE ( 'NONE', ( #104 ), #9163, .F. ) ;
#499=EDGE_CURVE ( 'NONE', #1229, #14925, #2522, .T. ) ;
#501=EDGE_CURVE ( 'NONE', #1342, #114, #5947, .T. ) ;
#503=PLANE ( 'NONE',  #14800 ) ;
#504=VERTEX_POINT ( 'NONE', #9475 ) ;
#505=EDGE_LOOP ( 'NONE', ( #7717, #2716, #8517, #10389 ) ) ;
#516=ORIENTED_EDGE ( 'NONE', *, *, #4824, .F. ) ;
#521=EDGE_LOOP ( 'NONE', ( #12899, #4880, #11029, #14009, #13965, #2995, #9899, #2358 ) ) ;
#527=AXIS2_PLACEMENT_3D ( 'NONE', #12711, #14236, #2546 ) ;
#529=EDGE_CURVE ( 'NONE', #6474, #14724, #5304, .T. ) ;
#530=CARTESIAN_POINT ( 'NONE',  ( 3.426491571325181340, -1.679378605318041950, 1.679378605318059048 ) ) ;
#537=ORIENTED_EDGE ( 'NONE', *, *, #1029, .F. ) ;
#540=CIRCLE ( 'NONE', #13989, 1.000000000000000000 ) ;
#541=CARTESIAN_POINT ( 'NONE',  ( 3.426491571325181340, 0.000000000000000000, 0.000000000000000000 ) ) ;
#542=DIRECTION ( 'NONE',  ( 1.000000000000000000, 0.000000000000000000, 0.000000000000000000 ) ) ;
#544=CARTESIAN_POINT ( 'NONE',  ( 4.329246711911844514, 1.779530689460202320, 0.5984961127851674556 ) ) ;
#545=EDGE_CURVE ( 'NONE', #3991, #4965, #11057, .T. ) ;
#546=EDGE_CURVE ( 'NONE', #1773, #10754, #10215, .T. ) ;
#548=CIRCLE ( 'NONE', #11077, 1.000000000000000222 ) ;
#551=EDGE_LOOP ( 'NONE', ( #6863, #3717, #2455, #3329 ) ) ;
#555=CARTESIAN_POINT ( 'NONE',  ( 3.426491571325181340, 1.679378605318059048, 1.679378605318041506 ) ) ;
#560=DIRECTION ( 'NONE',  ( 0.000000000000000000, -1.000000000000000000, 0.000000000000000000 ) ) ;
#566=CIRCLE ( 'NONE', #9416, 2.500000000000000444 ) ;
#567=CARTESIAN_POINT ( 'NONE',  ( 4.418784802593074268, 1.729109169374164923, 0.5194219853913167873 ) ) ;
#569=EDGE_LOOP ( 'NONE', ( #13025, #1220 ) ) ;
#575=ORIENTED_EDGE ( 'NONE', *, *, #5776, .F. ) ;
#582=EDGE_CURVE ( 'NONE', #6020, #5479, #13980, .T. ) ;
#583=AXIS2_PLACEMENT_3D ( 'NONE', #12548, #3233, #6611 ) ;
#586=DIRECTION ( 'NONE',  ( 1.000000000000000000, 0.000000000000000000, 0.000000000000000000 ) ) ;
#591=ORIENTED_EDGE ( 'NONE', *, *, #11529, .T. ) ;
#592=CIRCLE ( 'NONE', #14054, 0.1000000000000000194 ) ;
#595=EDGE_LOOP ( 'NONE', ( #450, #9611, #14713, #14999 ) ) ;
#596=VECTOR ( 'NONE', #1390, 39.37007874015748143 ) ;
#597=AXIS2_PLACEMENT_3D ( 'NONE', #8204, #9276, #13832 ) ;
#613=DIRECTION ( 'NONE',  ( 0.000000000000000000, 0.000000000000000000, -1.000000000000000000 ) ) ;
#614=ORIENTED_EDGE ( 'NONE', *, *, #2822, .T. ) ;
#617=EDGE_CURVE ( 'NONE', #3063, #2897, #6417, .T. ) ;
#618=VECTOR ( 'NONE', #11913, 39.37007874015748854 ) ;
#624=CARTESIAN_POINT ( 'NONE',  ( 4.438984740194723777, 1.783484299094709291, -0.4967767970635435515 ) ) ;
#625=AXIS2_PLACEMENT_3D ( 'NONE', #5408, #7774, #1867 ) ;
#626=VERTEX_POINT ( 'NONE', #9128 ) ;
#628=VERTEX_POINT ( 'NONE', #13626 ) ;
#629=ORIENTED_EDGE ( 'NONE', *, *, #13918, .F. ) ;
#630=ADVANCED_FACE ( 'NONE', ( #11500 ), #13727, .F. ) ;
#631=ORIENTED_EDGE ( 'NONE', *, *, #11576, .F. ) ;
#634=CARTESIAN_POINT ( 'NONE',  ( 4.098661581315266922, 0.8939497136434934044, 0.4483968163765176818 ) ) ;
#638=VERTEX_POINT ( 'NONE', #10737 ) ;
#641=CARTESIAN_POINT ( 'NONE',  ( 6.176491571325181340, 3.649833176986403141E-16, 2.960629921259842146 ) ) ;
#645=B_SPLINE_CURVE_WITH_KNOTS ( 'NONE', 3,
 ( #5114, #3957, #11218, #6479, #7618, #8623, #9772, #634, #9841, #5040, #5331, #10007, #13340, #2878, #7549, #14493, #3889, #13422, #2956, #9922, #9699, #4029, #8696, #12208, #8561, #7698, #6404, #12357, #11059, #13199, #14576, #2736, #7406, #4105, #9880, #13609, #674, #12244, #14844, #7658, #6597, #4066, #5288, #11097, #7885, #8734, #7585, #9962, #4298, #8966, #13528, #5376 ),
 .UNSPECIFIED., .F., .F.,
 ( 4, 2, 2, 2, 2, 2, 2, 2, 2, 2, 2, 2, 2, 2, 2, 2, 2, 2, 2, 2, 2, 2, 2, 2, 2, 4 ),
 ( 0.04039358074926006209, 0.04165364880998905645, 0.04291371687071805774, 0.04543385299217604645, 0.04795398911363403516, 0.04921405717436303645, 0.05047412523509203081, 0.05299426135654999870, 0.05425432941727896530, 0.05551439747800793884, 0.05803453359946587897, 0.05929460166019485945, 0.06055466972092382605, 0.06181473778165279959, 0.06307480584238177312, 0.06559494196383972020, 0.06685501002456870068, 0.06811507808529766728, 0.06937514614602664775, 0.07063521420675561435, 0.07315535032821354755, 0.07441541838894250027, 0.07567548644967146687, 0.07819562257112942782, 0.07945569063185840830, 0.08071575869258738878 ),
 .UNSPECIFIED. ) ;
#646=CARTESIAN_POINT ( 'NONE',  ( 3.426491571325181340, -2.360000000000000320, 0.9799999999999999822 ) ) ;
#647=CARTESIAN_POINT ( 'NONE',  ( 4.110025962911500130, 1.748120791446346800, 0.7137006213478416239 ) ) ;
#648=CARTESIAN_POINT ( 'NONE',  ( 3.573617713061139067, 1.991675394285061129, -0.3996246112651613003 ) ) ;
#650=AXIS2_PLACEMENT_3D ( 'NONE', #530, #384, #3003 ) ;
#652=DIRECTION ( 'NONE',  ( 0.000000000000000000, 1.000000000000000000, 0.000000000000000000 ) ) ;
#654=ORIENTED_EDGE ( 'NONE', *, *, #7639, .T. ) ;
#661=LINE ( 'NONE', #6081, #596 ) ;
#663=AXIS2_PLACEMENT_3D ( 'NONE', #3116, #8851, #13492 ) ;
#665=CARTESIAN_POINT ( 'NONE',  ( 3.426491571325181340, -2.360000000000016751, -0.9799999999999431388 ) ) ;
#668=DIRECTION ( 'NONE',  ( 0.000000000000000000, 0.000000000000000000, -1.000000000000000000 ) ) ;
#670=CARTESIAN_POINT ( 'NONE',  ( 3.651563249442855597, 0.8939021589031062032, -0.4484876836904110875 ) ) ;
#671=VECTOR ( 'NONE', #5225, 39.37007874015748143 ) ;
#674=CARTESIAN_POINT ( 'NONE',  ( 4.271191871305239474, 0.9523025322212360644, -0.3054383546384628056 ) ) ;
#677=CIRCLE ( 'NONE', #9267, 0.1899999999999996136 ) ;
#680=EDGE_CURVE ( 'NONE', #14399, #13316, #9442, .T. ) ;
#694=VERTEX_POINT ( 'NONE', #6070 ) ;
#698=LINE ( 'NONE', #7680, #4065 ) ;
#699=ORIENTED_EDGE ( 'NONE', *, *, #10847, .T. ) ;
#700=EDGE_CURVE ( 'NONE', #4913, #6255, #9520, .T. ) ;
#704=AXIS2_PLACEMENT_3D ( 'NONE', #13464, #8666, #8821 ) ;
#705=FACE_OUTER_BOUND ( 'NONE', #12936, .T. ) ;
#707=CARTESIAN_POINT ( 'NONE',  ( 4.470587351505396434, 1.786057884980379873, 0.4605560640960539853 ) ) ;
#714=CARTESIAN_POINT ( 'NONE',  ( 6.176491571325181340, 1.934941942652818220E-16, 1.580000000000000071 ) ) ;
#716=DIRECTION ( 'NONE',  ( 0.000000000000000000, 0.000000000000000000, 1.000000000000000000 ) ) ;
#717=ORIENTED_EDGE ( 'NONE', *, *, #6431, .T. ) ;
#725=EDGE_CURVE ( 'NONE', #10222, #4107, #6183, .T. ) ;
#726=VECTOR ( 'NONE', #13880, 39.37007874015748143 ) ;
#727=CARTESIAN_POINT ( 'NONE',  ( 4.291638032986768714, 1.730033725795280697, 0.6249393708399010317 ) ) ;
#728=CARTESIAN_POINT ( 'NONE',  ( 3.874999999999999556, 3.105999999999998984, -1.130000000000000560 ) ) ;
#731=DIRECTION ( 'NONE',  ( -0.000000000000000000, -1.000000000000000000, -0.000000000000000000 ) ) ;
#738=DIRECTION ( 'NONE',  ( -1.000000000000000000, -0.000000000000000000, -0.000000000000000000 ) ) ;
#745=ADVANCED_FACE ( 'NONE', ( #14087 ), #226, .F. ) ;
#746=CARTESIAN_POINT ( 'NONE',  ( 6.787121492585022509, 0.000000000000000000, -1.000000000000000000 ) ) ;
#747=CARTESIAN_POINT ( 'NONE',  ( 3.490100261840733520, 1.973532854457274333, 0.3199934443535443207 ) ) ;
#749=ORIENTED_EDGE ( 'NONE', *, *, #5402, .T. ) ;
#755=DIRECTION ( 'NONE',  ( -1.000000000000000000, -0.000000000000000000, -0.000000000000000000 ) ) ;
#759=ORIENTED_EDGE ( 'NONE', *, *, #973, .F. ) ;
#764=ORIENTED_EDGE ( 'NONE', *, *, #13005, .T. ) ;
#765=CIRCLE ( 'NONE', #14467, 1.000000000000000000 ) ;
#768=DIRECTION ( 'NONE',  ( -1.000000000000000000, -0.000000000000000000, -0.000000000000000000 ) ) ;
#775=EDGE_CURVE ( 'NONE', #8481, #1001, #765, .T. ) ;
#779=CARTESIAN_POINT ( 'NONE',  ( 4.147377230984255370, 1.742726334417983081, -0.7003979466013926514 ) ) ;
#780=EDGE_LOOP ( 'NONE', ( #12883, #10333, #9108, #10071 ) ) ;
#783=ORIENTED_EDGE ( 'NONE', *, *, #3012, .F. ) ;
#788=VERTEX_POINT ( 'NONE', #6918 ) ;
#791=AXIS2_PLACEMENT_3D ( 'NONE', #1531, #10950, #4998 ) ;
#793=EDGE_CURVE ( 'NONE', #6575, #12377, #7154, .T. ) ;
#795=ADVANCED_FACE ( 'NONE', ( #11574 ), #1074, .T. ) ;
#797=CARTESIAN_POINT ( 'NONE',  ( 4.574008775633079615, 1.717466915705979646, 0.4004807778818798014 ) ) ;
#798=DIRECTION ( 'NONE',  ( 0.000000000000000000, 0.000000000000000000, -1.000000000000000000 ) ) ;
#803=VERTEX_POINT ( 'NONE', #9804 ) ;
#804=ORIENTED_EDGE ( 'NONE', *, *, #3082, .T. ) ;
#812=B_SPLINE_CURVE_WITH_KNOTS ( 'NONE', 3,
 ( #9229, #13867, #12153, #1661, #5194, #4045, #7170, #3565, #8088, #11824, #14025, #10448, #13028, #5868 ),
 .UNSPECIFIED., .F., .F.,
 ( 4, 2, 2, 2, 2, 2, 4 ),
 ( 0.000000000000000000, 0.0009187753074270573741, 0.001837550614854114748, 0.002296938268567648260, 0.002756325922281181989, 0.003215713575994715284, 0.003675101229708249012 ),
 .UNSPECIFIED. ) ;
#813=DIRECTION ( 'NONE',  ( 0.000000000000000000, 0.000000000000000000, -1.000000000000000000 ) ) ;
#816=DIRECTION ( 'NONE',  ( 0.000000000000000000, 0.000000000000000000, -1.000000000000000000 ) ) ;
#824=CARTESIAN_POINT ( 'NONE',  ( 6.794491571325179891, 1.679378605318035733, -1.679378605318065487 ) ) ;
#826=AXIS2_PLACEMENT_3D ( 'NONE', #13633, #4090, #13553 ) ;
#827=CYLINDRICAL_SURFACE ( 'NONE', #7196, 0.3750000000000007772 ) ;
#828=ORIENTED_EDGE ( 'NONE', *, *, #12802, .F. ) ;
#832=DIRECTION ( 'NONE',  ( 0.000000000000000000, 0.000000000000000000, -1.000000000000000000 ) ) ;
#833=LINE ( 'NONE', #11567, #4529 ) ;
#835=ORIENTED_EDGE ( 'NONE', *, *, #7606, .T. ) ;
#841=DIRECTION ( 'NONE',  ( 1.000000000000000000, 0.000000000000000000, 0.000000000000000000 ) ) ;
#843=VERTEX_POINT ( 'NONE', #2922 ) ;
#847=DIRECTION ( 'NONE',  ( 1.000000000000000000, 0.000000000000000000, 0.000000000000000000 ) ) ;
#854=DIRECTION ( 'NONE',  ( 1.000000000000000000, 0.000000000000000000, 0.000000000000000000 ) ) ;
#855=ORIENTED_EDGE ( 'NONE', *, *, #6620, .T. ) ;
#856=DIRECTION ( 'NONE',  ( 0.000000000000000000, 0.000000000000000000, 1.000000000000000000 ) ) ;
#870=CARTESIAN_POINT ( 'NONE',  ( 3.319143374005773861, 2.449058936906570061, -0.5026158830344926720 ) ) ;
#874=FACE_OUTER_BOUND ( 'NONE', #12768, .T. ) ;
#876=CARTESIAN_POINT ( 'NONE',  ( 4.465766375128255916, 1.731456125583728634, 0.4644050319404698368 ) ) ;
#877=DIRECTION ( 'NONE',  ( 0.000000000000000000, 0.000000000000000000, 1.000000000000000000 ) ) ;
#881=FACE_OUTER_BOUND ( 'NONE', #11882, .T. ) ;
#882=ORIENTED_EDGE ( 'NONE', *, *, #10381, .T. ) ;
#887=DIRECTION ( 'NONE',  ( 0.000000000000000000, 0.000000000000000000, -1.000000000000000000 ) ) ;
#891=LINE ( 'NONE', #9338, #9977 ) ;
#893=CARTESIAN_POINT ( 'NONE',  ( 3.921039573451326365, 1.873037145645487955, 0.4984214080510448452 ) ) ;
#894=DIRECTION ( 'NONE',  ( 1.000000000000000000, 0.000000000000000000, 0.000000000000000000 ) ) ;
#896=EDGE_CURVE ( 'NONE', #6953, #3491, #7435, .T. ) ;
#899=ORIENTED_EDGE ( 'NONE', *, *, #1393, .F. ) ;
#905=CARTESIAN_POINT ( 'NONE',  ( 2.774999999999999911, -0.9799999999999436939, 2.360000000000016307 ) ) ;
#906=VERTEX_POINT ( 'NONE', #7299 ) ;
#908=FACE_OUTER_BOUND ( 'NONE', #13181, .T. ) ;
#911=VECTOR ( 'NONE', #11865, 39.37007874015748143 ) ;
#917=AXIS2_PLACEMENT_3D ( 'NONE', #9344, #10631, #8199 ) ;
#918=ORIENTED_EDGE ( 'NONE', *, *, #7315, .T. ) ;
#919=CARTESIAN_POINT ( 'NONE',  ( 6.096491571325181269, 1.836970198721030181E-16, -1.500000000000000222 ) ) ;
#924=ORIENTED_EDGE ( 'NONE', *, *, #3817, .T. ) ;
#928=ORIENTED_EDGE ( 'NONE', *, *, #147, .T. ) ;
#933=AXIS2_PLACEMENT_3D ( 'NONE', #295, #6071, #11651 ) ;
#934=DIRECTION ( 'NONE',  ( 1.000000000000000000, 0.000000000000000000, 0.000000000000000000 ) ) ;
#935=CIRCLE ( 'NONE', #7791, 1.580000000000000071 ) ;
#936=CARTESIAN_POINT ( 'NONE',  ( 4.113165067732116320, 1.797094705958242722, -0.7133961233632938326 ) ) ;
#940=EDGE_CURVE ( 'NONE', #5002, #12407, #1270, .T. ) ;
#941=CARTESIAN_POINT ( 'NONE',  ( 3.589981441049234334, 1.905209480108689402, -0.6943159375963412483 ) ) ;
#943=ORIENTED_EDGE ( 'NONE', *, *, #13912, .T. ) ;
#946=FACE_OUTER_BOUND ( 'NONE', #13192, .T. ) ;
#954=CARTESIAN_POINT ( 'NONE',  ( 6.826491571325181695, 1.679378605318059492, 2.054378605318042172 ) ) ;
#959=CARTESIAN_POINT ( 'NONE',  ( 4.552750260792047143, 1.739117664213755576, -0.3249664550261794349 ) ) ;
#960=LINE ( 'NONE', #2031, #6707 ) ;
#962=ORIENTED_EDGE ( 'NONE', *, *, #7688, .F. ) ;
#964=ORIENTED_EDGE ( 'NONE', *, *, #2726, .T. ) ;
#973=EDGE_CURVE ( 'NONE', #6575, #638, #4002, .T. ) ;
#977=EDGE_CURVE ( 'NONE', #8165, #803, #10109, .T. ) ;
#978=DIRECTION ( 'NONE',  ( 0.000000000000000000, 1.000000000000000000, -0.000000000000000000 ) ) ;
#979=CARTESIAN_POINT ( 'NONE',  ( 3.499444649685982789, 0.9439035327204450265, -0.3304825201858028749 ) ) ;
#980=CARTESIAN_POINT ( 'NONE',  ( 3.464708039267614836, 1.935623382077672705, -0.7069089347666170919 ) ) ;
#981=CARTESIAN_POINT ( 'NONE',  ( 2.774999999999999911, 0.000000000000000000, 0.000000000000000000 ) ) ;
#982=LINE ( 'NONE', #14995, #3083 ) ;
#992=AXIS2_PLACEMENT_3D ( 'NONE', #11456, #4574, #6795 ) ;
#993=CARTESIAN_POINT ( 'NONE',  ( 3.394491571325183088, -1.679378605318041950, 1.679378605318059048 ) ) ;
#994=CARTESIAN_POINT ( 'NONE',  ( 2.774999999999999911, -2.360000000000016751, -0.9799999999999431388 ) ) ;
#1001=VERTEX_POINT ( 'NONE', #4150 ) ;
#1002=CARTESIAN_POINT ( 'NONE',  ( 5.567023771132172172, 1.836970198721030181E-16, -1.500000000000000222 ) ) ;
#1006=DIRECTION ( 'NONE',  ( 1.000000000000000000, 0.000000000000000000, 0.000000000000000000 ) ) ;
#1008=CARTESIAN_POINT ( 'NONE',  ( 3.426491571325181340, 2.360000000000015863, 0.9799999999999454703 ) ) ;
#1011=EDGE_CURVE ( 'NONE', #3810, #12377, #7828, .T. ) ;
#1012=CARTESIAN_POINT ( 'NONE',  ( 3.971366415850335230, 1.827788509831742347, -0.7443691409044070895 ) ) ;
#1015=CARTESIAN_POINT ( 'NONE',  ( 3.876040592281544850, 1.779390558749738060, -0.7983410256676741756 ) ) ;
#1016=EDGE_LOOP ( 'NONE', ( #4083, #3866 ) ) ;
#1020=CARTESIAN_POINT ( 'NONE',  ( 3.874999999999999556, 3.137999999999999901, 1.509999999999999787 ) ) ;
#1029=EDGE_CURVE ( 'NONE', #10024, #11969, #3447, .T. ) ;
#1033=CARTESIAN_POINT ( 'NONE',  ( 4.527597100494972437, 1.736431947037383683, -0.3728085656124198732 ) ) ;
#1035=DIRECTION ( 'NONE',  ( 0.000000000000000000, 0.000000000000000000, 1.000000000000000000 ) ) ;
#1043=VERTEX_POINT ( 'NONE', #2216 ) ;
#1045=CARTESIAN_POINT ( 'NONE',  ( 6.215861650065340527, 3.673940397442060361E-16, 3.000000000000000444 ) ) ;
#1057=CARTESIAN_POINT ( 'NONE',  ( 4.271292041023736274, 1.710010143222131740, 0.6913003412368600165 ) ) ;
#1061=ORIENTED_EDGE ( 'NONE', *, *, #6248, .F. ) ;
#1063=DIRECTION ( 'NONE',  ( -0.000000000000000000, -1.000000000000000000, -0.000000000000000000 ) ) ;
#1066=CYLINDRICAL_SURFACE ( 'NONE', #5370, 0.5000000000000002220 ) ;
#1074=CYLINDRICAL_SURFACE ( 'NONE', #2512, 0.5000000000000002220 ) ;
#1082=DIRECTION ( 'NONE',  ( -1.000000000000000000, -0.000000000000000000, -0.000000000000000000 ) ) ;
#1087=CARTESIAN_POINT ( 'NONE',  ( 3.995454032860411342, 1.821680253208853406, -0.7409104450711488932 ) ) ;
#1092=CARTESIAN_POINT ( 'NONE',  ( 3.898431109275737771, 1.794535650040266495, -0.7500217376237132694 ) ) ;
#1098=ORIENTED_EDGE ( 'NONE', *, *, #13912, .F. ) ;
#1100=CIRCLE ( 'NONE', #6245, 0.2944999999999987073 ) ;
#1103=CARTESIAN_POINT ( 'NONE',  ( 2.774999999999999911, -1.679378605318041950, 1.384878605318060174 ) ) ;
#1105=CARTESIAN_POINT ( 'NONE',  ( 3.263555662057198603, 2.462108353317236986, -0.4359725516674392565 ) ) ;
#1108=EDGE_CURVE ( 'NONE', #14200, #7033, #1666, .T. ) ;
#1109=CIRCLE ( 'NONE', #6756, 0.7849999999999983658 ) ;
#1111=TOROIDAL_SURFACE ( 'NONE', #6254, 0.0001794190581142465670, 1.999999999999999334 ) ;
#1113=CARTESIAN_POINT ( 'NONE',  ( 4.680319326871657637, 1.732346333260918803, -0.09359317111134475564 ) ) ;
#1115=CARTESIAN_POINT ( 'NONE',  ( 2.774999999999999911, 0.000000000000000000, 0.000000000000000000 ) ) ;
#1120=ORIENTED_EDGE ( 'NONE', *, *, #6402, .F. ) ;
#1124=DIRECTION ( 'NONE',  ( 0.000000000000000000, 0.000000000000000000, 1.000000000000000000 ) ) ;
#1125=ORIENTED_EDGE ( 'NONE', *, *, #1582, .F. ) ;
#1135=CARTESIAN_POINT ( 'NONE',  ( 4.660391722812436299, 1.729108088022653922, 0.1957348282867307776 ) ) ;
#1141=ORIENTED_EDGE ( 'NONE', *, *, #52, .T. ) ;
#1142=ORIENTED_EDGE ( 'NONE', *, *, #3481, .F. ) ;
#1145=ORIENTED_EDGE ( 'NONE', *, *, #42, .T. ) ;
#1148=CARTESIAN_POINT ( 'NONE',  ( 3.426491571325181340, 2.399999999999999911, -0.7000000000000007327 ) ) ;
#1150=CIRCLE ( 'NONE', #8730, 0.3750000000000004996 ) ;
#1151=VERTEX_POINT ( 'NONE', #8422 ) ;
#1152=CARTESIAN_POINT ( 'NONE',  ( 3.414222290118229974, 1.988642828590650780, -0.5921450265355728826 ) ) ;
#1154=DIRECTION ( 'NONE',  ( 0.000000000000000000, 0.000000000000000000, 1.000000000000000000 ) ) ;
#1156=DIRECTION ( 'NONE',  ( 1.000000000000000000, -0.000000000000000000, 1.224646799147353207E-16 ) ) ;
#1157=EDGE_CURVE ( 'NONE', #8481, #7135, #6351, .T. ) ;
#1164=DIRECTION ( 'NONE',  ( -0.7071067811865429098, 0.000000000000000000, 0.7071067811865521247 ) ) ;
#1165=CIRCLE ( 'NONE', #6318, 1.000000000000000888 ) ;
#1168=EDGE_CURVE ( 'NONE', #10132, #1043, #205, .T. ) ;
#1169=ADVANCED_FACE ( 'NONE', ( #4041 ), #1572, .F. ) ;
#1173=AXIS2_PLACEMENT_3D ( 'NONE', #6740, #11398, #668 ) ;
#1177=ORIENTED_EDGE ( 'NONE', *, *, #6713, .F. ) ;
#1183=CARTESIAN_POINT ( 'NONE',  ( 3.394491571325183088, 1.679378605318059048, 1.941878605318041462 ) ) ;
#1184=ORIENTED_EDGE ( 'NONE', *, *, #4862, .T. ) ;
#1187=LINE ( 'NONE', #954, #6791 ) ;
#1188=CARTESIAN_POINT ( 'NONE',  ( 3.875000000000000000, 1.112678268764263789, -0.4849999999999995981 ) ) ;
#1192=CARTESIAN_POINT ( 'NONE',  ( 4.587230667253597183, 1.743394675270711458, -0.2422858810294691856 ) ) ;
#1194=DIRECTION ( 'NONE',  ( -1.000000000000000000, -0.000000000000000000, -0.000000000000000000 ) ) ;
#1197=CARTESIAN_POINT ( 'NONE',  ( 5.546318247523970513, 0.000000000000000000, 1.502725933896874810 ) ) ;
#1199=CARTESIAN_POINT ( 'NONE',  ( 6.794491571325179891, 1.679378605318035733, -2.054378605318066153 ) ) ;
#1201=DIRECTION ( 'NONE',  ( 0.000000000000000000, 0.000000000000000000, -1.000000000000000000 ) ) ;
#1209=CARTESIAN_POINT ( 'NONE',  ( 6.208491571325183145, -1.679378605318048390, 2.054378605318054607 ) ) ;
#1213=CARTESIAN_POINT ( 'NONE',  ( 3.442233731549079412, 0.9679978390437318225, 0.2525149742857387691 ) ) ;
#1214=CARTESIAN_POINT ( 'NONE',  ( 4.666407739276771771, 1.730062807210744902, 0.1714704599012415176 ) ) ;
#1216=EDGE_LOOP ( 'NONE', ( #2848, #404, #9726, #8653 ) ) ;
#1218=DIRECTION ( 'NONE',  ( -1.000000000000000000, -0.000000000000000000, -0.000000000000000000 ) ) ;
#1220=ORIENTED_EDGE ( 'NONE', *, *, #9053, .T. ) ;
#1229=VERTEX_POINT ( 'NONE', #293 ) ;
#1234=CIRCLE ( 'NONE', #9570, 0.1899999999999996136 ) ;
#1235=CARTESIAN_POINT ( 'NONE',  ( 3.405153689607044232, 2.750000000000000000, 1.491010071662831171 ) ) ;
#1236=ORIENTED_EDGE ( 'NONE', *, *, #12925, .T. ) ;
#1242=CIRCLE ( 'NONE', #4437, 0.07999999999999996003 ) ;
#1244=DIRECTION ( 'NONE',  ( 0.000000000000000000, -0.7071067811865509034, -0.7071067811865441310 ) ) ;
#1245=CARTESIAN_POINT ( 'NONE',  ( 3.708475701238409528, 1.919230964417490748, -0.7311178887250847636 ) ) ;
#1249=DIRECTION ( 'NONE',  ( 1.000000000000000000, -0.000000000000000000, -0.000000000000000000 ) ) ;
#1256=CARTESIAN_POINT ( 'NONE',  ( 3.632032016703825583, 1.941006471662596322, -0.4371510339114678123 ) ) ;
#1260=DIRECTION ( 'NONE',  ( 0.000000000000000000, 0.000000000000000000, 1.000000000000000000 ) ) ;
#1261=DIRECTION ( 'NONE',  ( -0.000000000000000000, -1.000000000000000000, -0.000000000000000000 ) ) ;
#1263=CARTESIAN_POINT ( 'NONE',  ( 4.685225399282611392, 1.733178264597110552, -0.03635724695066767931 ) ) ;
#1265=CARTESIAN_POINT ( 'NONE',  ( 3.944129661530210385, 0.000000000000000000, 1.932031071636253650 ) ) ;
#1267=ORIENTED_EDGE ( 'NONE', *, *, #940, .T. ) ;
#1268=LINE ( 'NONE', #8266, #13818 ) ;
#1270=CIRCLE ( 'NONE', #8136, 0.2945000000000009277 ) ;
#1271=CYLINDRICAL_SURFACE ( 'NONE', #15075, 3.000000000000000444 ) ;
#1277=EDGE_CURVE ( 'NONE', #1362, #5506, #13882, .T. ) ;
#1285=CARTESIAN_POINT ( 'NONE',  ( 4.685864643020170917, 1.733287931739606380, 0.04932201671138494725 ) ) ;
#1289=FACE_OUTER_BOUND ( 'NONE', #8073, .T. ) ;
#1290=ORIENTED_EDGE ( 'NONE', *, *, #6124, .T. ) ;
#1291=EDGE_LOOP ( 'NONE', ( #2563, #9836, #6390, #2394 ) ) ;
#1293=CARTESIAN_POINT ( 'NONE',  ( 3.897879830116474320, 1.879038604582284666, 0.5000000000000002220 ) ) ;
#1295=ORIENTED_EDGE ( 'NONE', *, *, #8058, .F. ) ;
#1296=DIRECTION ( 'NONE',  ( 0.000000000000000000, 1.000000000000000000, 0.000000000000000000 ) ) ;
#1301=AXIS2_PLACEMENT_3D ( 'NONE', #15094, #14094, #3628 ) ;
#1302=ORIENTED_EDGE ( 'NONE', *, *, #9073, .T. ) ;
#1307=EDGE_LOOP ( 'NONE', ( #12654, #10142, #11894, #4155 ) ) ;
#1320=DIRECTION ( 'NONE',  ( -1.000000000000000000, -0.000000000000000000, -0.000000000000000000 ) ) ;
#1321=ORIENTED_EDGE ( 'NONE', *, *, #7727, .F. ) ;
#1334=FACE_OUTER_BOUND ( 'NONE', #477, .T. ) ;
#1338=AXIS2_PLACEMENT_3D ( 'NONE', #13018, #2555, #11162 ) ;
#1341=CIRCLE ( 'NONE', #7465, 0.2625000000000000111 ) ;
#1342=VERTEX_POINT ( 'NONE', #3923 ) ;
#1344=ORIENTED_EDGE ( 'NONE', *, *, #10558, .F. ) ;
#1347=DIRECTION ( 'NONE',  ( 1.000000000000000000, 0.000000000000000000, 0.000000000000000000 ) ) ;
#1349=DIRECTION ( 'NONE',  ( 0.000000000000000000, 0.000000000000000000, 1.000000000000000000 ) ) ;
#1351=AXIS2_PLACEMENT_3D ( 'NONE', #14861, #11653, #7986 ) ;
#1352=CARTESIAN_POINT ( 'NONE',  ( 3.793823152521890840, 1.884745230718079423, 0.7457052748579492407 ) ) ;
#1355=CYLINDRICAL_SURFACE ( 'NONE', #14795, 0.1899999999999996136 ) ;
#1358=EDGE_CURVE ( 'NONE', #12028, #12407, #2764, .T. ) ;
#1359=CARTESIAN_POINT ( 'NONE',  ( 4.609856173843976279, 1.721777932115673426, 0.3359333493936877413 ) ) ;
#1362=VERTEX_POINT ( 'NONE', #14311 ) ;
#1368=DIRECTION ( 'NONE',  ( 0.000000000000000000, 0.000000000000000000, -1.000000000000000000 ) ) ;
#1371=DIRECTION ( 'NONE',  ( -1.000000000000000000, -0.000000000000000000, -0.000000000000000000 ) ) ;
#1373=EDGE_CURVE ( 'NONE', #9926, #14596, #8810, .T. ) ;
#1377=ORIENTED_EDGE ( 'NONE', *, *, #8091, .F. ) ;
#1379=CARTESIAN_POINT ( 'NONE',  ( 3.341312140645306794, 1.997119961756267603, -0.6280817267650429248 ) ) ;
#1387=CIRCLE ( 'NONE', #14093, 1.500000000000000222 ) ;
#1388=CARTESIAN_POINT ( 'NONE',  ( 6.794491571325179891, -1.679378605318047946, -1.679378605318053497 ) ) ;
#1390=DIRECTION ( 'NONE',  ( -1.000000000000000000, -0.000000000000000000, -0.000000000000000000 ) ) ;
#1393=EDGE_CURVE ( 'NONE', #8887, #9027, #9003, .T. ) ;
#1397=LINE ( 'NONE', #4940, #6984 ) ;
#1400=ORIENTED_EDGE ( 'NONE', *, *, #12508, .T. ) ;
#1402=ORIENTED_EDGE ( 'NONE', *, *, #5015, .F. ) ;
#1405=DIRECTION ( 'NONE',  ( 0.000000000000000000, 0.000000000000000000, -1.000000000000000000 ) ) ;
#1407=ORIENTED_EDGE ( 'NONE', *, *, #8888, .F. ) ;
#1412=EDGE_CURVE ( 'NONE', #1001, #6235, #9956, .T. ) ;
#1415=AXIS2_PLACEMENT_3D ( 'NONE', #5157, #240, #4939 ) ;
#1419=DIRECTION ( 'NONE',  ( 0.000000000000000000, 1.000000000000000000, 0.000000000000000000 ) ) ;
#1420=ORIENTED_EDGE ( 'NONE', *, *, #12128, .T. ) ;
#1421=AXIS2_PLACEMENT_3D ( 'NONE', #7428, #5983, #10944 ) ;
#1427=CARTESIAN_POINT ( 'NONE',  ( 2.774999999999999911, 2.359999999999993214, -1.575000000000016831 ) ) ;
#1431=LINE ( 'NONE', #7410, #5606 ) ;
#1438=FACE_BOUND ( 'NONE', #2610, .T. ) ;
#1440=CARTESIAN_POINT ( 'NONE',  ( 3.563446790140585740, 1.891298529660668137, 0.7485675892123550002 ) ) ;
#1442=ORIENTED_EDGE ( 'NONE', *, *, #13709, .F. ) ;
#1449=( CONVERSION_BASED_UNIT ( 'INCH', #215 ) LENGTH_UNIT ( ) NAMED_UNIT ( #10871 ) );
#1457=VECTOR ( 'NONE', #6225, 39.37007874015748143 ) ;
#1461=CARTESIAN_POINT ( 'NONE',  ( 2.774999999999999911, 3.360000000000000320, -0.9800000000000012035 ) ) ;
#1469=ORIENTED_EDGE ( 'NONE', *, *, #14409, .T. ) ;
#1470=DIRECTION ( 'NONE',  ( -1.000000000000000000, -0.000000000000000000, -0.000000000000000000 ) ) ;
#1474=CARTESIAN_POINT ( 'NONE',  ( 3.944129661530210385, 1.761538328845252188, 0.7935532608319412207 ) ) ;
#1484=DIRECTION ( 'NONE',  ( 0.000000000000000000, 0.000000000000000000, 1.000000000000000000 ) ) ;
#1487=FACE_OUTER_BOUND ( 'NONE', #6810, .T. ) ;
#1489=( CONVERSION_BASED_UNIT ( 'INCH', #7745 ) LENGTH_UNIT ( ) NAMED_UNIT ( #3840 ) );
#1490=ADVANCED_FACE ( 'NONE', ( #3217 ), #9109, .T. ) ;
#1491=VECTOR ( 'NONE', #9688, 39.37007874015748143 ) ;
#1492=CARTESIAN_POINT ( 'NONE',  ( 4.427625859550793130, 1.707399566347088449, -0.5781646599430360078 ) ) ;
#1495=ORIENTED_EDGE ( 'NONE', *, *, #2305, .T. ) ;
#1497=DIRECTION ( 'NONE',  ( 1.000000000000000000, 0.000000000000000000, 0.000000000000000000 ) ) ;
#1504=CARTESIAN_POINT ( 'NONE',  ( 3.944129661530210385, 0.000000000000000000, 1.932031071636253650 ) ) ;
#1505=CARTESIAN_POINT ( 'NONE',  ( 3.876560711617219379, 2.749999999999999556, 0.7500000000000001110 ) ) ;
#1506=CONICAL_SURFACE ( 'NONE', #3475, 0.2624999999999997335, 0.7853981633974419507 ) ;
#1507=DIRECTION ( 'NONE',  ( 0.000000000000000000, 0.000000000000000000, -1.000000000000000000 ) ) ;
#1508=FACE_BOUND ( 'NONE', #8831, .T. ) ;
#1510=CARTESIAN_POINT ( 'NONE',  ( 3.612336255711126931, 1.963150234975052033, 0.7021133243488046904 ) ) ;
#1511=CARTESIAN_POINT ( 'NONE',  ( 3.426491571325181340, 2.399999999999999911, -0.7000000000000007327 ) ) ;
#1516=CYLINDRICAL_SURFACE ( 'NONE', #6025, 0.3750000000000007772 ) ;
#1517=ORIENTED_EDGE ( 'NONE', *, *, #15120, .F. ) ;
#1518=ORIENTED_EDGE ( 'NONE', *, *, #2556, .F. ) ;
#1519=DIRECTION ( 'NONE',  ( -1.000000000000000000, -0.000000000000000000, -0.000000000000000000 ) ) ;
#1521=DIRECTION ( 'NONE',  ( 1.000000000000000000, 0.000000000000000000, 0.000000000000000000 ) ) ;
#1527=VECTOR ( 'NONE', #13580, 39.37007874015748143 ) ;
#1531=CARTESIAN_POINT ( 'NONE',  ( 3.394491571325180423, -1.679378605318059048, -1.679378605318041950 ) ) ;
#1534=VERTEX_POINT ( 'NONE', #7652 ) ;
#1536=ORIENTED_EDGE ( 'NONE', *, *, #9240, .T. ) ;
#1539=CARTESIAN_POINT ( 'NONE',  ( 2.774999999999999911, -1.679378605318059048, -1.384878605318056399 ) ) ;
#1541=DIRECTION ( 'NONE',  ( 1.000000000000000000, 0.000000000000000000, 0.000000000000000000 ) ) ;
#1544=LINE ( 'NONE', #6086, #671 ) ;
#1545=CARTESIAN_POINT ( 'NONE',  ( 6.096491571325181269, 0.000000000000000000, 1.500000000000000222 ) ) ;
#1546=ORIENTED_EDGE ( 'NONE', *, *, #12964, .F. ) ;
#1555=DIRECTION ( 'NONE',  ( 0.000000000000000000, 1.000000000000000000, -0.000000000000000000 ) ) ;
#1560=( NAMED_UNIT ( * ) PLANE_ANGLE_UNIT ( ) SI_UNIT ( $, .RADIAN. ) );
#1561=ORIENTED_EDGE ( 'NONE', *, *, #9832, .T. ) ;
#1563=EDGE_LOOP ( 'NONE', ( #10739, #7868, #1, #12847 ) ) ;
#1571=ORIENTED_EDGE ( 'NONE', *, *, #3241, .F. ) ;
#1572=( BOUNDED_SURFACE ( )  B_SPLINE_SURFACE ( 3, 2, ( 
 ( #2820, #8706, #13352 ),
 ( #9573, #3966, #495 ),
 ( #2894, #12149, #12003 ),
 ( #12072, #7490, #14217 ),
 ( #2679, #13209, #5190 ),
 ( #7350, #7276, #11929 ),
 ( #1510, #14290, #1440 ),
 ( #6129, #10787, #275 ),
 ( #4978, #9644, #3828 ),
 ( #349, #8497, #10856 ),
 ( #5052, #9716, #14364 ),
 ( #3901, #2746, #1584 ),
 ( #6273, #10932, #424 ),
 ( #5127, #9783, #14439 ),
 ( #6573, #10019, #7711 ),
 ( #14673, #14745, #7629 ),
 ( #3270, #3199, #1726 ),
 ( #13501, #10239, #8789 ),
 ( #5570, #7862, #13433 ),
 ( #3126, #647, #11230 ),
 ( #2030, #10162, #7792 ),
 ( #5346, #4271, #14898 ),
 ( #9089, #4199, #13732 ),
 ( #14818, #727, #5423 ),
 ( #11069, #4121, #9934 ),
 ( #4347, #8863, #10090 ),
 ( #5495, #12369, #12512 ),
 ( #6716, #11378, #5263 ),
 ( #9022, #567, #13664 ),
 ( #3041, #13582, #8939 ),
 ( #7937, #876, #1883 ),
 ( #1802, #14588, #12445 ),
 ( #4424, #6413, #1962 ),
 ( #6645, #11298, #797 ),
 ( #2969, #12289, #6492 ),
 ( #11149, #8261, #10310 ),
 ( #8101, #3345, #12588 ),
 ( #2436, #2111, #106 ),
 ( #11765, #5723, #10461 ),
 ( #12741, #14123, #14041 ),
 ( #15050, #9246, #5948 ),
 ( #5800, #2267, #11607 ),
 ( #13961, #11532, #6951 ),
 ( #12898, #5883, #3496 ),
 ( #12671, #7115, #1263 ),
 ( #2350, #14970, #3663 ),
 ( #3581, #8022, #1113 ),
 ( #4496, #2194, #8177 ),
 ( #6879, #10539, #15126 ),
 ( #6796, #1192, #11458 ),
 ( #10611, #4807, #33 ),
 ( #4726, #959, #9400 ),
 ( #9166, #9476, #12818 ),
 ( #13810, #1033, #4652 ),
 ( #9322, #10385, #4575 ),
 ( #7032, #11691, #2503 ),
 ( #4889, #402, #12130 ),
 ( #8475, #9553, #13191 ),
 ( #9834, #14197, #1492 ),
 ( #9765, #2579, #10834 ),
 ( #7256, #326, #1636 ),
 ( #6328, #6110, #10986 ),
 ( #475, #1709, #10069 ),
 ( #8843, #14801, #7769 ),
 ( #4255, #7689, #7846 ),
 ( #12493, #779, #11051 ),
 ( #2014, #8917, #9913 ),
 ( #1947, #14569, #11515 ),
 ( #5864, #8242, #10367 ),
 ( #12648, #2252, #2411 ),
 ( #7918, #2176, #4558 ),
 ( #9306, #1092, #9225 ),
 ( #5705, #13789, #1015 ),
 ( #4409, #14881, #9382 ),
 ( #13944, #9070, #13863 ),
 ( #5635, #3559, #8084 ),
 ( #6932, #10445, #11588 ),
 ( #1245, #7999, #13716 ),
 ( #8159, #3250, #7096 ),
 ( #12799, #11435, #2330 ),
 ( #7014, #941, #14953 ),
 ( #11667, #10521, #18 ),
 ( #5918, #14166, #10426 ),
 ( #14004, #3538, #3621 ),
 ( #10656, #2470, #5990 ),
 ( #3390, #9519, #7152 ),
 ( #11802, #1152, #2235 ),
 ( #10576, #2310, #1379 ) ),
 .UNSPECIFIED., .F., .F., .F. ) 
 B_SPLINE_SURFACE_WITH_KNOTS ( ( 4, 2, 2, 2, 2, 2, 2, 2, 2, 2, 2, 2, 2, 2, 2, 2, 2, 2, 2, 2, 2, 2, 2, 2, 2, 2, 2, 2, 2, 2, 2, 2, 2, 2, 2, 2, 2, 2, 2, 2, 2, 2, 2, 4 ),
 ( 3, 3 ),
 ( 0.02004080291861797675, 0.02305506901397080116, 0.02606933510932362211, 0.02757646815700003085, 0.02908360120467644305, 0.03209786730002926747, 0.03360500034770567968, 0.03511213339538209188, 0.03812639949073490936, 0.04114066558608772683, 0.04415493168144055125, 0.04716919777679337566, 0.04867633082446978787, 0.05018346387214620008, 0.05319772996749902449, 0.05470486301517543670, 0.05621199606285184197, 0.05922626215820465945, 0.06224052825355748386, 0.06374766130123389607, 0.06525479434891030828, 0.06826906044426313269, 0.06977619349193953102, 0.07128332653961594323, 0.07429759263496876764, 0.07731185873032159206, 0.07881899177799800427, 0.08032612482567441647, 0.08334039092102724089, 0.08635465701638006530, 0.08936892311173288972, 0.09087605615940930193, 0.09238318920708571413, 0.09539745530243853855, 0.09841172139779136296, 0.09991885444546777517, 0.1014259874931441874, 0.1044402535884970118, 0.1059473866361734240, 0.1074545196838498362, 0.1104687857792026606, 0.1119759188268790728, 0.1134830518745554850, 0.1164973179699082956 ),
 ( 0.000000000000000000, 1.000000000000000000 ),
 .UNSPECIFIED. ) 
 GEOMETRIC_REPRESENTATION_ITEM ( )  RATIONAL_B_SPLINE_SURFACE ( (
 ( 1.000000000000000000, 0.7303619642676426604, 1.000000000000000000),
 ( 1.000000000000000000, 0.7391659050363718064, 1.000000000000000000),
 ( 1.000000000000000000, 0.7477864703932980417, 1.000000000000000000),
 ( 1.000000000000000000, 0.7644820136340396699, 1.000000000000000000),
 ( 1.000000000000000000, 0.7725576652621481966, 1.000000000000000000),
 ( 1.000000000000000000, 0.7841369972240639363, 1.000000000000000000),
 ( 1.000000000000000000, 0.7879067894510097814, 1.000000000000000000),
 ( 1.000000000000000000, 0.7951473863334842518, 1.000000000000000000),
 ( 1.000000000000000000, 0.7986319938952645137, 1.000000000000000000),
 ( 1.000000000000000000, 0.8086632967091734736, 1.000000000000000000),
 ( 1.000000000000000000, 0.8147886344311031648, 1.000000000000000000),
 ( 1.000000000000000000, 0.8230549922231803484, 1.000000000000000000),
 ( 1.000000000000000000, 0.8256565766521759553, 1.000000000000000000),
 ( 1.000000000000000000, 0.8305349661893675073, 1.000000000000000000),
 ( 1.000000000000000000, 0.8328179003807386627, 1.000000000000000000),
 ( 1.000000000000000000, 0.8391074215019772575, 1.000000000000000000),
 ( 1.000000000000000000, 0.8424994775394850643, 1.000000000000000000),
 ( 1.000000000000000000, 0.8477154134529806262, 1.000000000000000000),
 ( 1.000000000000000000, 0.8495388365352557480, 1.000000000000000000),
 ( 1.000000000000000000, 0.8516216512933566518, 1.000000000000000000),
 ( 1.000000000000000000, 0.8518656269916470292, 1.000000000000000000),
 ( 1.000000000000000000, 0.8508610807012660926, 1.000000000000000000),
 ( 1.000000000000000000, 0.8496312072233146440, 1.000000000000000000),
 ( 1.000000000000000000, 0.8468793023704244138, 1.000000000000000000),
 ( 1.000000000000000000, 0.8458107531247578414, 1.000000000000000000),
 ( 1.000000000000000000, 0.8434028339490304838, 1.000000000000000000),
 ( 1.000000000000000000, 0.8420586255985930135, 1.000000000000000000),
 ( 1.000000000000000000, 0.8377450007014299871, 1.000000000000000000),
 ( 1.000000000000000000, 0.8344806938985878109, 1.000000000000000000),
 ( 1.000000000000000000, 0.8292948692869647198, 1.000000000000000000),
 ( 1.000000000000000000, 0.8275179307216389279, 1.000000000000000000),
 ( 1.000000000000000000, 0.8239169748456836029, 1.000000000000000000),
 ( 1.000000000000000000, 0.8220876319902808982, 1.000000000000000000),
 ( 1.000000000000000000, 0.8166433934471487577, 1.000000000000000000),
 ( 1.000000000000000000, 0.8131103617266270955, 1.000000000000000000),
 ( 1.000000000000000000, 0.8066241410163590420, 1.000000000000000000),
 ( 1.000000000000000000, 0.8036703286668861468, 1.000000000000000000),
 ( 1.000000000000000000, 0.7999468164656692304, 1.000000000000000000),
 ( 1.000000000000000000, 0.7988220075153393829, 1.000000000000000000),
 ( 1.000000000000000000, 0.7968807107365607489, 1.000000000000000000),
 ( 1.000000000000000000, 0.7960588307793206031, 1.000000000000000000),
 ( 1.000000000000000000, 0.7940666135324694341, 1.000000000000000000),
 ( 1.000000000000000000, 0.7933721712197883136, 1.000000000000000000),
 ( 1.000000000000000000, 0.7933444941328147149, 1.000000000000000000),
 ( 1.000000000000000000, 0.7935036486169138037, 1.000000000000000000),
 ( 1.000000000000000000, 0.7941617368941129573, 1.000000000000000000),
 ( 1.000000000000000000, 0.7946641558677889350, 1.000000000000000000),
 ( 1.000000000000000000, 0.7966418117377881414, 1.000000000000000000),
 ( 1.000000000000000000, 0.7985862221323072330, 1.000000000000000000),
 ( 1.000000000000000000, 0.8034606050232417918, 1.000000000000000000),
 ( 1.000000000000000000, 0.8063907621180180785, 1.000000000000000000),
 ( 1.000000000000000000, 0.8112888969071575529, 1.000000000000000000),
 ( 1.000000000000000000, 0.8130019067800049459, 1.000000000000000000),
 ( 1.000000000000000000, 0.8164902207451381067, 1.000000000000000000),
 ( 1.000000000000000000, 0.8182717664989170858, 1.000000000000000000),
 ( 1.000000000000000000, 0.8236513966877028192, 1.000000000000000000),
 ( 1.000000000000000000, 0.8272847376777223705, 1.000000000000000000),
 ( 1.000000000000000000, 0.8342391892289522382, 1.000000000000000000),
 ( 1.000000000000000000, 0.8375729779648963813, 1.000000000000000000),
 ( 1.000000000000000000, 0.8433263320323867163, 1.000000000000000000),
 ( 1.000000000000000000, 0.8457747513117915839, 1.000000000000000000),
 ( 1.000000000000000000, 0.8485728704767122599, 1.000000000000000000),
 ( 1.000000000000000000, 0.8493599451720096338, 1.000000000000000000),
 ( 1.000000000000000000, 0.8506036242994673424, 1.000000000000000000),
 ( 1.000000000000000000, 0.8510608768027098092, 1.000000000000000000),
 ( 1.000000000000000000, 0.8518668280105339274, 1.000000000000000000),
 ( 1.000000000000000000, 0.8516595178598228566, 1.000000000000000000),
 ( 1.000000000000000000, 0.8496680361726848263, 1.000000000000000000),
 ( 1.000000000000000000, 0.8478847233904961422, 1.000000000000000000),
 ( 1.000000000000000000, 0.8439514783278239118, 1.000000000000000000),
 ( 1.000000000000000000, 0.8424398969624482536, 1.000000000000000000),
 ( 1.000000000000000000, 0.8390475808887900566, 1.000000000000000000),
 ( 1.000000000000000000, 0.8371639927170544393, 1.000000000000000000),
 ( 1.000000000000000000, 0.8309672570077345499, 1.000000000000000000),
 ( 1.000000000000000000, 0.8261093469114791921, 1.000000000000000000),
 ( 1.000000000000000000, 0.8177745008309323937, 1.000000000000000000),
 ( 1.000000000000000000, 0.8148147276102298830, 1.000000000000000000),
 ( 1.000000000000000000, 0.8086351537547810109, 1.000000000000000000),
 ( 1.000000000000000000, 0.8054072265268824582, 1.000000000000000000),
 ( 1.000000000000000000, 0.7953363259039076816, 1.000000000000000000),
 ( 1.000000000000000000, 0.7881068092093646005, 1.000000000000000000),
 ( 1.000000000000000000, 0.7765812923454467054, 1.000000000000000000),
 ( 1.000000000000000000, 0.7726257270913668984, 1.000000000000000000),
 ( 1.000000000000000000, 0.7645013318077583664, 1.000000000000000000),
 ( 1.000000000000000000, 0.7603508406709547085, 1.000000000000000000),
 ( 1.000000000000000000, 0.7477573469669197559, 1.000000000000000000),
 ( 1.000000000000000000, 0.7391362403695903582, 1.000000000000000000),
 ( 1.000000000000000000, 0.7303873157140532424, 1.000000000000000000) ) ) 
 REPRESENTATION_ITEM ( '' )  SURFACE ( )  );
#1574=CARTESIAN_POINT ( 'NONE',  ( 3.379935043499636027, 2.435578798916048893, 0.5650223589646659050 ) ) ;
#1575=DIRECTION ( 'NONE',  ( 0.000000000000000000, 1.000000000000000000, -4.591341165821855765E-15 ) ) ;
#1576=CARTESIAN_POINT ( 'NONE',  ( 6.826491571325181695, 0.000000000000000000, 3.000000000000000444 ) ) ;
#1579=CARTESIAN_POINT ( 'NONE',  ( 3.426491571325181340, -1.574999999999999956, 2.360000000000024745 ) ) ;
#1582=EDGE_CURVE ( 'NONE', #12204, #11537, #15071, .T. ) ;
#1583=DIRECTION ( 'NONE',  ( 1.000000000000000000, 0.000000000000000000, 0.000000000000000000 ) ) ;
#1584=CARTESIAN_POINT ( 'NONE',  ( 3.760602986904977740, 1.815251021643483176, 0.7937676298150420084 ) ) ;
#1585=CARTESIAN_POINT ( 'NONE',  ( 6.826491571325181695, 0.000000000000000000, 2.960629921259841257 ) ) ;
#1587=CARTESIAN_POINT ( 'NONE',  ( 2.774999999999999911, 0.9800000000000039790, 2.359999999999999876 ) ) ;
#1588=CARTESIAN_POINT ( 'NONE',  ( 3.426491571325181340, 0.000000000000000000, 0.000000000000000000 ) ) ;
#1593=VERTEX_POINT ( 'NONE', #9270 ) ;
#1605=CIRCLE ( 'NONE', #10179, 0.2219999999999999751 ) ;
#1609=ORIENTED_EDGE ( 'NONE', *, *, #13267, .F. ) ;
#1615=LINE ( 'NONE', #2634, #8299 ) ;
#1617=ADVANCED_FACE ( 'NONE', ( #3446 ), #7051, .F. ) ;
#1621=ORIENTED_EDGE ( 'NONE', *, *, #5490, .F. ) ;
#1629=CYLINDRICAL_SURFACE ( 'NONE', #5363, 0.3750000000000004996 ) ;
#1630=CARTESIAN_POINT ( 'NONE',  ( 3.971130012676523879, 1.827282607391995883, 0.7455485334240098405 ) ) ;
#1632=EDGE_CURVE ( 'NONE', #7301, #7267, #12420, .T. ) ;
#1635=CIRCLE ( 'NONE', #10211, 0.2624999999999997335 ) ;
#1636=CARTESIAN_POINT ( 'NONE',  ( 4.335720917399813246, 1.707353294205550487, -0.6508460809909353273 ) ) ;
#1637=ORIENTED_EDGE ( 'NONE', *, *, #6722, .T. ) ;
#1638=ORIENTED_EDGE ( 'NONE', *, *, #14739, .T. ) ;
#1641=CARTESIAN_POINT ( 'NONE',  ( 6.787121492585022509, 0.000000000000000000, 1.000000000000000000 ) ) ;
#1643=DIRECTION ( 'NONE',  ( -1.000000000000000000, -0.000000000000000000, -0.000000000000000000 ) ) ;
#1650=CARTESIAN_POINT ( 'NONE',  ( 3.426491571325181340, 3.137999999999999901, 0.2209981660730358233 ) ) ;
#1651=EDGE_CURVE ( 'NONE', #1686, #13105, #2712, .T. ) ;
#1661=CARTESIAN_POINT ( 'NONE',  ( 3.426491571325180452, 1.978105636280900193, 0.6428442102750744347 ) ) ;
#1663=ORIENTED_EDGE ( 'NONE', *, *, #13541, .T. ) ;
#1665=ORIENTED_EDGE ( 'NONE', *, *, #10203, .T. ) ;
#1666=CIRCLE ( 'NONE', #11947, 0.2219999999999999751 ) ;
#1667=EDGE_CURVE ( 'NONE', #6474, #13739, #8757, .T. ) ;
#1670=DIRECTION ( 'NONE',  ( -1.000000000000000000, -0.000000000000000000, -0.000000000000000000 ) ) ;
#1681=DIRECTION ( 'NONE',  ( 0.000000000000000000, 0.000000000000000000, -1.000000000000000000 ) ) ;
#1686=VERTEX_POINT ( 'NONE', #7519 ) ;
#1687=AXIS2_PLACEMENT_3D ( 'NONE', #5024, #9690, #3492 ) ;
#1688=CYLINDRICAL_SURFACE ( 'NONE', #8701, 0.2624999999999852451 ) ;
#1692=DIRECTION ( 'NONE',  ( -0.000000000000000000, -1.000000000000000000, -0.000000000000000000 ) ) ;
#1695=LINE ( 'NONE', #6156, #6855 ) ;
#1696=VECTOR ( 'NONE', #14543, 39.37007874015748143 ) ;
#1697=CARTESIAN_POINT ( 'NONE',  ( 6.794491571325179891, -1.679378605318047946, -1.679378605318053497 ) ) ;
#1699=LINE ( 'NONE', #10894, #8923 ) ;
#1703=VERTEX_POINT ( 'NONE', #7313 ) ;
#1707=CARTESIAN_POINT ( 'NONE',  ( 6.826491571325181695, 0.000000000000000000, 0.000000000000000000 ) ) ;
#1708=CARTESIAN_POINT ( 'NONE',  ( 4.586453973344011281, 1.802653555183125755, 0.2432409261222566454 ) ) ;
#1709=CARTESIAN_POINT ( 'NONE',  ( 4.247411616490353481, 1.732648565181565070, -0.6521631700520624797 ) ) ;
#1710=ORIENTED_EDGE ( 'NONE', *, *, #11233, .F. ) ;
#1712=ORIENTED_EDGE ( 'NONE', *, *, #10067, .T. ) ;
#1714=EDGE_CURVE ( 'NONE', #5032, #1043, #1544, .T. ) ;
#1716=CYLINDRICAL_SURFACE ( 'NONE', #2584, 0.2625000000000000111 ) ;
#1721=FACE_OUTER_BOUND ( 'NONE', #9981, .T. ) ;
#1726=CARTESIAN_POINT ( 'NONE',  ( 3.931979536481067683, 1.764175763689243670, 0.7956254023616837756 ) ) ;
#1732=ORIENTED_EDGE ( 'NONE', *, *, #11459, .T. ) ;
#1742=CARTESIAN_POINT ( 'NONE',  ( 6.176491571325181340, 0.000000000000000000, -1.580000000000000071 ) ) ;
#1746=ADVANCED_FACE ( 'NONE', ( #386 ), #7384, .F. ) ;
#1747=ORIENTED_EDGE ( 'NONE', *, *, #1011, .T. ) ;
#1753=LINE ( 'NONE', #12393, #6996 ) ;
#1755=ORIENTED_EDGE ( 'NONE', *, *, #10453, .F. ) ;
#1756=CARTESIAN_POINT ( 'NONE',  ( 3.426491571325181340, 2.426945040795776443, -0.5999481385559803925 ) ) ;
#1765=EDGE_CURVE ( 'NONE', #788, #4442, #3784, .T. ) ;
#1766=LINE ( 'NONE', #11109, #6231 ) ;
#1769=EDGE_CURVE ( 'NONE', #12651, #10812, #1615, .T. ) ;
#1771=CARTESIAN_POINT ( 'NONE',  ( 6.826491571325181695, -1.679378605318047946, -1.304378605318053053 ) ) ;
#1773=VERTEX_POINT ( 'NONE', #1474 ) ;
#1776=VERTEX_POINT ( 'NONE', #8667 ) ;
#1780=PLANE ( 'NONE',  #3898 ) ;
#1781=CARTESIAN_POINT ( 'NONE',  ( 4.587994488202223664, 1.802825568755139996, -0.2425064940794559032 ) ) ;
#1795=DIRECTION ( 'NONE',  ( 0.000000000000000000, 0.000000000000000000, 1.000000000000000000 ) ) ;
#1796=CARTESIAN_POINT ( 'NONE',  ( 3.233755863391478247, 2.469910769216284940, 0.3874905525801941031 ) ) ;
#1802=CARTESIAN_POINT ( 'NONE',  ( 4.485621383300165022, 1.787868003613383161, 0.4380272511281654291 ) ) ;
#1804=ORIENTED_EDGE ( 'NONE', *, *, #8532, .F. ) ;
#1809=EDGE_LOOP ( 'NONE', ( #12192, #14198, #4340, #6562 ) ) ;
#1810=DIRECTION ( 'NONE',  ( 0.000000000000000000, -0.000000000000000000, -1.000000000000000000 ) ) ;
#1816=CARTESIAN_POINT ( 'NONE',  ( 3.426491571325181340, -1.679378605318059048, -1.679378605318041950 ) ) ;
#1820=EDGE_CURVE ( 'NONE', #11264, #14935, #430, .T. ) ;
#1824=EDGE_CURVE ( 'NONE', #3063, #7156, #12254, .T. ) ;
#1826=CARTESIAN_POINT ( 'NONE',  ( 3.475375010813855248, 1.976875583815957071, 0.3014176176147594366 ) ) ;
#1827=DIRECTION ( 'NONE',  ( 1.000000000000000000, 0.000000000000000000, 0.000000000000000000 ) ) ;
#1829=CIRCLE ( 'NONE', #11373, 0.7849999999999983658 ) ;
#1833=CIRCLE ( 'NONE', #13796, 1.039370078740158965 ) ;
#1834=CIRCLE ( 'NONE', #9434, 0.2625000000000000111 ) ;
#1847=CARTESIAN_POINT ( 'NONE',  ( 3.426491571325181340, -3.360000000000016751, -0.9799999999999434719 ) ) ;
#1850=CARTESIAN_POINT ( 'NONE',  ( 3.426491571325181340, -2.359999999999984333, 1.575000000000016387 ) ) ;
#1853=VECTOR ( 'NONE', #12516, 39.37007874015748143 ) ;
#1854=ORIENTED_EDGE ( 'NONE', *, *, #9770, .T. ) ;
#1855=CARTESIAN_POINT ( 'NONE',  ( 3.944129661530210385, 2.366055667732568841E-16, -1.932031071636253650 ) ) ;
#1859=ADVANCED_FACE ( 'NONE', ( #3231 ), #6825, .T. ) ;
#1862=ORIENTED_EDGE ( 'NONE', *, *, #529, .F. ) ;
#1864=ORIENTED_EDGE ( 'NONE', *, *, #8532, .T. ) ;
#1867=DIRECTION ( 'NONE',  ( 0.000000000000000000, 0.000000000000000000, 1.000000000000000000 ) ) ;
#1868=CARTESIAN_POINT ( 'NONE',  ( 3.875000000000000000, 1.885381157978845312, 0.5000000000000002220 ) ) ;
#1873=ORIENTED_EDGE ( 'NONE', *, *, #3850, .T. ) ;
#1874=CARTESIAN_POINT ( 'NONE',  ( 3.875000000000000000, 3.137999999999999901, -0.5000000000000002220 ) ) ;
#1881=CARTESIAN_POINT ( 'NONE',  ( 2.774999999999999911, -2.360000000000021636, -1.574999999999999734 ) ) ;
#1882=CARTESIAN_POINT ( 'NONE',  ( 2.774999999999999911, 1.679378605318059048, 1.384878605318040856 ) ) ;
#1883=CARTESIAN_POINT ( 'NONE',  ( 4.505898589230239004, 1.711421573918742833, 0.4949957780824733589 ) ) ;
#1884=CARTESIAN_POINT ( 'NONE',  ( 3.851496678973868271, 1.891896550263048038, -0.5000000000000002220 ) ) ;
#1890=ORIENTED_EDGE ( 'NONE', *, *, #1373, .F. ) ;
#1891=AXIS2_PLACEMENT_3D ( 'NONE', #2753, #4049, #8717 ) ;
#1892=DIRECTION ( 'NONE',  ( 0.7071067811865460184, 0.000000000000000000, -0.7071067811865490160 ) ) ;
#1900=CARTESIAN_POINT ( 'NONE',  ( 2.774999999999999911, -1.679378605318041950, 1.679378605318059048 ) ) ;
#1904=CARTESIAN_POINT ( 'NONE',  ( 3.381634859058371578, 0.9966950651981517639, 0.08284753930692498325 ) ) ;
#1905=VECTOR ( 'NONE', #3519, 39.37007874015748854 ) ;
#1906=CARTESIAN_POINT ( 'NONE',  ( 4.393322081076587615, 1.706995504219652737, -0.6070895335983141905 ) ) ;
#1908=CIRCLE ( 'NONE', #6327, 0.1000000000000000194 ) ;
#1911=ORIENTED_EDGE ( 'NONE', *, *, #6818, .F. ) ;
#1912=CONICAL_SURFACE ( 'NONE', #439, 0.3750000000000004996, 0.7853981633974547183 ) ;
#1913=DIRECTION ( 'NONE',  ( -1.000000000000000000, -0.000000000000000000, -0.000000000000000000 ) ) ;
#1914=EDGE_LOOP ( 'NONE', ( #9355, #9384, #9462, #9325 ) ) ;
#1920=CARTESIAN_POINT ( 'NONE',  ( 3.426491571325181340, 2.062169880637645836, -0.5999481385559802815 ) ) ;
#1922=( LENGTH_UNIT ( ) NAMED_UNIT ( * ) SI_UNIT ( $, .METRE. ) );
#1929=DIRECTION ( 'NONE',  ( -1.000000000000000000, -0.000000000000000000, -0.000000000000000000 ) ) ;
#1932=ORIENTED_EDGE ( 'NONE', *, *, #977, .F. ) ;
#1933=ORIENTED_EDGE ( 'NONE', *, *, #973, .T. ) ;
#1940=AXIS2_PLACEMENT_3D ( 'NONE', #8894, #6523, #8976 ) ;
#1946=CIRCLE ( 'NONE', #9301, 2.500000000000000000 ) ;
#1947=CARTESIAN_POINT ( 'NONE',  ( 4.051235613900670884, 1.808866337081830311, -0.7302300179307213979 ) ) ;
#1952=CARTESIAN_POINT ( 'NONE',  ( 3.897980617091954869, 1.879010665267595304, -0.5000000000000002220 ) ) ;
#1953=DIRECTION ( 'NONE',  ( 0.000000000000000000, 0.000000000000000000, -1.000000000000000000 ) ) ;
#1956=ORIENTED_EDGE ( 'NONE', *, *, #2136, .F. ) ;
#1957=LINE ( 'NONE', #2102, #8319 ) ;
#1960=DIRECTION ( 'NONE',  ( 0.000000000000000000, 0.000000000000000000, -1.000000000000000000 ) ) ;
#1961=AXIS2_PLACEMENT_3D ( 'NONE', #9620, #11183, #6247 ) ;
#1962=CARTESIAN_POINT ( 'NONE',  ( 4.541376298268983369, 1.714299675483434982, 0.4487873714220094734 ) ) ;
#1968=ORIENTED_EDGE ( 'NONE', *, *, #529, .T. ) ;
#1969=VERTEX_POINT ( 'NONE', #5987 ) ;
#1974=DIRECTION ( 'NONE',  ( -0.000000000000000000, 1.000000000000000000, -0.000000000000000000 ) ) ;
#1980=CARTESIAN_POINT ( 'NONE',  ( 3.510247954615316246, 0.9396455958913839668, -0.3423636469962711981 ) ) ;
#1984=LINE ( 'NONE', #14619, #13797 ) ;
#1988=ORIENTED_EDGE ( 'NONE', *, *, #2996, .T. ) ;
#1996=ORIENTED_EDGE ( 'NONE', *, *, #8488, .T. ) ;
#1998=VECTOR ( 'NONE', #2700, 39.37007874015748143 ) ;
#1999=DIRECTION ( 'NONE',  ( -0.000000000000000000, -1.000000000000000000, -0.000000000000000000 ) ) ;
#2001=CARTESIAN_POINT ( 'NONE',  ( 2.814370078740158210, 0.000000000000000000, 1.000000000000000000 ) ) ;
#2004=AXIS2_PLACEMENT_3D ( 'NONE', #13432, #5345, #14671 ) ;
#2009=DIRECTION ( 'NONE',  ( -1.000000000000000000, -0.000000000000000000, -0.000000000000000000 ) ) ;
#2014=CARTESIAN_POINT ( 'NONE',  ( 4.119080202121599754, 1.796483476452471972, -0.7105853202116764189 ) ) ;
#2023=EDGE_LOOP ( 'NONE', ( #13714, #5234, #13749, #918 ) ) ;
#2024=CARTESIAN_POINT ( 'NONE',  ( 3.162550611401342415, 2.489436539607832621, 0.2300036551928836270 ) ) ;
#2027=VECTOR ( 'NONE', #1063, 39.37007874015748143 ) ;
#2030=CARTESIAN_POINT ( 'NONE',  ( 4.150492928931191372, 1.791887721204809214, 0.6990997386737194397 ) ) ;
#2031=CARTESIAN_POINT ( 'NONE',  ( 3.405153689607044232, 3.137999999999999901, 1.491010071662831171 ) ) ;
#2032=ORIENTED_EDGE ( 'NONE', *, *, #3818, .T. ) ;
#2034=AXIS2_PLACEMENT_3D ( 'NONE', #14943, #3141, #813 ) ;
#2039=CARTESIAN_POINT ( 'NONE',  ( 3.874999999999999556, 3.137999999999999901, 1.320000000000000062 ) ) ;
#2041=DIRECTION ( 'NONE',  ( 0.000000000000000000, 0.000000000000000000, 1.000000000000000000 ) ) ;
#2047=CIRCLE ( 'NONE', #10617, 1.000000000000000222 ) ;
#2052=CARTESIAN_POINT ( 'NONE',  ( 3.852151642586534308, 1.889461949475109925, 0.5000000000000286438 ) ) ;
#2054=CARTESIAN_POINT ( 'NONE',  ( 2.774999999999999911, 2.360000000000015863, 1.574999999999999956 ) ) ;
#2055=DIRECTION ( 'NONE',  ( 0.000000000000000000, 0.7071067811865509034, 0.7071067811865441310 ) ) ;
#2060=CARTESIAN_POINT ( 'NONE',  ( 3.426491571325181340, 1.954234464180151676, 0.6847610993685215863 ) ) ;
#2064=EDGE_CURVE ( 'NONE', #9791, #4426, #11702, .T. ) ;
#2065=EDGE_CURVE ( 'NONE', #1001, #8481, #15102, .T. ) ;
#2070=ORIENTED_EDGE ( 'NONE', *, *, #4974, .T. ) ;
#2071=CIRCLE ( 'NONE', #6980, 0.2624999999999997335 ) ;
#2072=DIRECTION ( 'NONE',  ( 0.000000000000000000, 1.000000000000000000, 0.000000000000000000 ) ) ;
#2073=DIRECTION ( 'NONE',  ( 0.000000000000000000, 1.000000000000000000, 0.000000000000000000 ) ) ;
#2083=CONICAL_SURFACE ( 'NONE', #14299, 0.4070000000000025264, 0.7853981633974557175 ) ;
#2087=CARTESIAN_POINT ( 'NONE',  ( 3.449073513670800839, 2.047967394769590666, 0.2629493547202494952 ) ) ;
#2092=ORIENTED_EDGE ( 'NONE', *, *, #4474, .T. ) ;
#2099=LINE ( 'NONE', #6786, #13646 ) ;
#2102=CARTESIAN_POINT ( 'NONE',  ( 6.826491571325181695, 1.679378605318059492, 1.304378605318041062 ) ) ;
#2111=CARTESIAN_POINT ( 'NONE',  ( 4.601389648059055482, 1.745381240488223629, 0.1935210130979204968 ) ) ;
#2112=CARTESIAN_POINT ( 'NONE',  ( 6.826491571325181695, 0.000000000000000000, 0.000000000000000000 ) ) ;
#2113=EDGE_LOOP ( 'NONE', ( #10769, #4278, #3503, #5803 ) ) ;
#2116=CARTESIAN_POINT ( 'NONE',  ( 3.426491571325181340, 0.000000000000000000, 0.000000000000000000 ) ) ;
#2117=ORIENTED_EDGE ( 'NONE', *, *, #5961, .T. ) ;
#2121=DIRECTION ( 'NONE',  ( 1.000000000000000000, 0.000000000000000000, 0.000000000000000000 ) ) ;
#2122=EDGE_LOOP ( 'NONE', ( #899, #5832, #13565, #8919 ) ) ;
#2126=CONICAL_SURFACE ( 'NONE', #8001, 0.2945000000000009277, 0.7853981633974503884 ) ;
#2128=FACE_OUTER_BOUND ( 'NONE', #2113, .T. ) ;
#2133=CARTESIAN_POINT ( 'NONE',  ( 3.712234661458500007, 0.8810498532991303255, -0.4730558837152146201 ) ) ;
#2135=CARTESIAN_POINT ( 'NONE',  ( 3.968383684466501915, 1.755580462719493973, -0.7909561288026154546 ) ) ;
#2136=EDGE_CURVE ( 'NONE', #6629, #11132, #6367, .T. ) ;
#2137=DIRECTION ( 'NONE',  ( 0.000000000000000000, 0.000000000000000000, -1.000000000000000000 ) ) ;
#2143=EDGE_LOOP ( 'NONE', ( #7259, #9599, #13875, #13158 ) ) ;
#2145=VECTOR ( 'NONE', #5684, 39.37007874015748143 ) ;
#2148=CYLINDRICAL_SURFACE ( 'NONE', #5320, 0.7849999999999991429 ) ;
#2149=AXIS2_PLACEMENT_3D ( 'NONE', #12762, #11478, #2290 ) ;
#2151=ORIENTED_EDGE ( 'NONE', *, *, #793, .F. ) ;
#2152=DIRECTION ( 'NONE',  ( 0.000000000000000000, 0.000000000000000000, -1.000000000000000000 ) ) ;
#2154=ORIENTED_EDGE ( 'NONE', *, *, #12110, .T. ) ;
#2156=DIRECTION ( 'NONE',  ( 0.000000000000000000, 0.000000000000000000, -1.000000000000000000 ) ) ;
#2157=CARTESIAN_POINT ( 'NONE',  ( 3.874999999999999556, 3.137999999999999901, -1.820000000000000284 ) ) ;
#2159=DIRECTION ( 'NONE',  ( 0.000000000000000000, 0.000000000000000000, -1.000000000000000000 ) ) ;
#2160=ADVANCED_BREP_SHAPE_REPRESENTATION ( '', ( #10609, #5584, #8424 ), #9397 ) ;
#2164=ORIENTED_EDGE ( 'NONE', *, *, #8583, .F. ) ;
#2171=AXIS2_PLACEMENT_3D ( 'NONE', #10846, #5045, #8566 ) ;
#2173=LINE ( 'NONE', #11890, #13616 ) ;
#2176=CARTESIAN_POINT ( 'NONE',  ( 3.934394892992688408, 1.784885785108176748, -0.7480858108736904155 ) ) ;
#2181=LINE ( 'NONE', #13437, #7472 ) ;
#2187=CYLINDRICAL_SURFACE ( 'NONE', #5589, 0.5000000000000002220 ) ;
#2188=VERTEX_POINT ( 'NONE', #5069 ) ;
#2189=CARTESIAN_POINT ( 'NONE',  ( 3.128620250494149158, 2.499382783242935169, -0.05744091823031614169 ) ) ;
#2191=LINE ( 'NONE', #5339, #14425 ) ;
#2193=FACE_OUTER_BOUND ( 'NONE', #8185, .T. ) ;
#2194=CARTESIAN_POINT ( 'NONE',  ( 4.614277204963975976, 1.747273315043324615, -0.1397865401030924659 ) ) ;
#2196=ORIENTED_EDGE ( 'NONE', *, *, #11253, .F. ) ;
#2199=EDGE_LOOP ( 'NONE', ( #2971, #11575 ) ) ;
#2207=LINE ( 'NONE', #7874, #12820 ) ;
#2208=CARTESIAN_POINT ( 'NONE',  ( 2.774999999999999911, 2.400000000000011458, 0.6999999999999614309 ) ) ;
#2209=CARTESIAN_POINT ( 'NONE',  ( 3.874999999999999556, 3.137999999999999901, 1.098000000000000087 ) ) ;
#2210=CARTESIAN_POINT ( 'NONE',  ( 2.774999999999999911, -1.679378605318059048, -1.384878605318056399 ) ) ;
#2212=AXIS2_PLACEMENT_3D ( 'NONE', #11604, #7111, #182 ) ;
#2216=CARTESIAN_POINT ( 'NONE',  ( 2.774999999999999911, 1.575000000000000178, -2.360000000000018971 ) ) ;
#2219=EDGE_CURVE ( 'NONE', #13739, #7714, #4921, .T. ) ;
#2221=CARTESIAN_POINT ( 'NONE',  ( 3.394491571325182644, 1.679378605318042395, -1.941878605318058337 ) ) ;
#2224=ORIENTED_EDGE ( 'NONE', *, *, #4492, .F. ) ;
#2229=ADVANCED_FACE ( 'NONE', ( #14386 ), #7086, .F. ) ;
#2232=DIRECTION ( 'NONE',  ( -1.000000000000000000, -0.000000000000000000, -0.000000000000000000 ) ) ;
#2233=DIRECTION ( 'NONE',  ( 0.000000000000000000, -1.000000000000000000, 0.000000000000000000 ) ) ;
#2235=CARTESIAN_POINT ( 'NONE',  ( 3.369979506347997589, 1.982223984522141658, -0.6498426228982311370 ) ) ;
#2236=AXIS2_PLACEMENT_3D ( 'NONE', #7902, #9062, #10207 ) ;
#2238=ORIENTED_EDGE ( 'NONE', *, *, #3192, .F. ) ;
#2239=CARTESIAN_POINT ( 'NONE',  ( 3.394491571325180423, -1.679378605318059048, -1.941878605318027251 ) ) ;
#2241=CYLINDRICAL_SURFACE ( 'NONE', #6632, 0.2625000000000000111 ) ;
#2249=CARTESIAN_POINT ( 'NONE',  ( 3.572691639587101342, 1.991786753997381032, 0.4009351690867059559 ) ) ;
#2252=CARTESIAN_POINT ( 'NONE',  ( 3.952519222920175324, 1.780293626097628312, -0.7464614403131658582 ) ) ;
#2254=ORIENTED_EDGE ( 'NONE', *, *, #10137, .T. ) ;
#2265=EDGE_CURVE ( 'NONE', #4893, #9885, #11208, .T. ) ;
#2267=CARTESIAN_POINT ( 'NONE',  ( 4.623972717631986029, 1.748760572069723906, 0.07156785328136136548 ) ) ;
#2282=AXIS2_PLACEMENT_3D ( 'NONE', #8970, #4156, #13459 ) ;
#2283=DIRECTION ( 'NONE',  ( 0.000000000000000000, -1.000000000000000000, 0.000000000000000000 ) ) ;
#2290=DIRECTION ( 'NONE',  ( 0.000000000000000000, 0.000000000000000000, 1.000000000000000000 ) ) ;
#2291=CARTESIAN_POINT ( 'NONE',  ( 3.544764658934682178, 0.9266133244050206441, 0.3767952779536547503 ) ) ;
#2292=CARTESIAN_POINT ( 'NONE',  ( 4.680957888034550152, 1.732455423116393334, -0.08709515200038929483 ) ) ;
#2294=EDGE_LOOP ( 'NONE', ( #2980, #10743, #9660, #12572 ) ) ;
#2295=CARTESIAN_POINT ( 'NONE',  ( 3.426491571325181340, -0.9799999999999986500, -3.359999999999999876 ) ) ;
#2296=CARTESIAN_POINT ( 'NONE',  ( 6.176491571325181340, -1.679378605318048390, 1.272378605318051914 ) ) ;
#2303=EDGE_CURVE ( 'NONE', #6443, #843, #13521, .T. ) ;
#2305=EDGE_CURVE ( 'NONE', #391, #5032, #10730, .T. ) ;
#2310=CARTESIAN_POINT ( 'NONE',  ( 3.389094372952905942, 2.001744261784617951, -0.5707014325286834389 ) ) ;
#2312=DIRECTION ( 'NONE',  ( -0.000000000000000000, -1.000000000000000000, 0.000000000000000000 ) ) ;
#2313=EDGE_LOOP ( 'NONE', ( #10259, #11212, #13436, #962 ) ) ;
#2316=DIRECTION ( 'NONE',  ( 0.000000000000000000, 0.000000000000000000, 1.000000000000000000 ) ) ;
#2318=CARTESIAN_POINT ( 'NONE',  ( 3.426491571325181340, 1.679378605318059048, 1.679378605318041506 ) ) ;
#2323=CARTESIAN_POINT ( 'NONE',  ( 6.208491571325183145, 1.679378605318035733, -1.679378605318065487 ) ) ;
#2324=CARTESIAN_POINT ( 'NONE',  ( 2.806999999999999940, -1.679378605318059048, -1.679378605318041950 ) ) ;
#2325=AXIS2_PLACEMENT_3D ( 'NONE', #9410, #4899, #1124 ) ;
#2327=CONICAL_SURFACE ( 'NONE', #1338, 1.932031071636253650, 0.2617993877991429685 ) ;
#2330=CARTESIAN_POINT ( 'NONE',  ( 3.598300749230342710, 1.876349019058903611, -0.7608587385032532513 ) ) ;
#2338=AXIS2_PLACEMENT_3D ( 'NONE', #12524, #12752, #2041 ) ;
#2339=CIRCLE ( 'NONE', #2348, 0.07999999999999996003 ) ;
#2348=AXIS2_PLACEMENT_3D ( 'NONE', #10790, #9789, #2825 ) ;
#2350=CARTESIAN_POINT ( 'NONE',  ( 4.623480434945832052, 1.809913863617587104, -0.07025183563157885724 ) ) ;
#2351=ORIENTED_EDGE ( 'NONE', *, *, #4610, .F. ) ;
#2353=ORIENTED_EDGE ( 'NONE', *, *, #7924, .T. ) ;
#2357=VERTEX_POINT ( 'NONE', #12838 ) ;
#2358=ORIENTED_EDGE ( 'NONE', *, *, #6508, .F. ) ;
#2360=DIRECTION ( 'NONE',  ( 0.000000000000000000, 0.000000000000000000, -1.000000000000000000 ) ) ;
#2362=AXIS2_PLACEMENT_3D ( 'NONE', #2826, #10862, #11154 ) ;
#2364=EDGE_LOOP ( 'NONE', ( #11571, #13014, #9703, #3204 ) ) ;
#2365=CARTESIAN_POINT ( 'NONE',  ( 2.774999999999999911, 1.679378605318042395, -1.679378605318058604 ) ) ;
#2368=VECTOR ( 'NONE', #10171, 39.37007874015748143 ) ;
#2369=CARTESIAN_POINT ( 'NONE',  ( 6.176491571325181340, -1.679378605318048390, 2.086378605318056412 ) ) ;
#2370=LINE ( 'NONE', #7048, #9195 ) ;
#2371=DIRECTION ( 'NONE',  ( 0.000000000000000000, 0.000000000000000000, -1.000000000000000000 ) ) ;
#2374=CARTESIAN_POINT ( 'NONE',  ( 3.610061643217520988, 0.9055534390348793927, 0.4243489690802683678 ) ) ;
#2375=CARTESIAN_POINT ( 'NONE',  ( 4.431846745274908628, 1.707674138507286443, 0.5735374726554932634 ) ) ;
#2377=CARTESIAN_POINT ( 'NONE',  ( 3.426491571325181340, -1.679378605318041950, 1.679378605318059048 ) ) ;
#2378=VECTOR ( 'NONE', #11522, 39.37007874015748143 ) ;
#2381=EDGE_LOOP ( 'NONE', ( #6537, #1267 ) ) ;
#2384=ORIENTED_EDGE ( 'NONE', *, *, #12791, .T. ) ;
#2385=DIRECTION ( 'NONE',  ( -0.000000000000000000, -1.000000000000000000, -0.000000000000000000 ) ) ;
#2388=DIRECTION ( 'NONE',  ( 0.000000000000000000, 0.000000000000000000, -1.000000000000000000 ) ) ;
#2393=DIRECTION ( 'NONE',  ( 8.659560562354816994E-17, -0.7071067811865568986, 0.7071067811865381358 ) ) ;
#2394=ORIENTED_EDGE ( 'NONE', *, *, #2726, .F. ) ;
#2399=CARTESIAN_POINT ( 'NONE',  ( 4.344846310392954436, 2.750000000000000000, -1.491010071662831171 ) ) ;
#2404=AXIS2_PLACEMENT_3D ( 'NONE', #8879, #3065, #14917 ) ;
#2407=CIRCLE ( 'NONE', #6073, 0.2219999999999999751 ) ;
#2408=AXIS2_PLACEMENT_3D ( 'NONE', #218, #13076, #2757 ) ;
#2411=CARTESIAN_POINT ( 'NONE',  ( 3.952950666365288690, 1.759291877752760414, -0.7927856782489325349 ) ) ;
#2421=CARTESIAN_POINT ( 'NONE',  ( 3.426491571325181340, 0.9799999999999438050, -2.360000000000016307 ) ) ;
#2436=CARTESIAN_POINT ( 'NONE',  ( 4.600670465018250610, 1.805329134815081504, 0.1961885608909609002 ) ) ;
#2439=ORIENTED_EDGE ( 'NONE', *, *, #3765, .F. ) ;
#2443=CARTESIAN_POINT ( 'NONE',  ( 2.774999999999999911, -2.359999999999979892, 1.575000000000016387 ) ) ;
#2445=ORIENTED_EDGE ( 'NONE', *, *, #6925, .T. ) ;
#2448=DIRECTION ( 'NONE',  ( 0.000000000000000000, 1.000000000000000000, -0.000000000000000000 ) ) ;
#2453=CARTESIAN_POINT ( 'NONE',  ( 3.624016768725874638, 0.9015561565218271900, 0.4327462728766410249 ) ) ;
#2454=FACE_BOUND ( 'NONE', #7143, .T. ) ;
#2455=ORIENTED_EDGE ( 'NONE', *, *, #5490, .T. ) ;
#2458=ORIENTED_EDGE ( 'NONE', *, *, #13986, .F. ) ;
#2464=ORIENTED_EDGE ( 'NONE', *, *, #6240, .F. ) ;
#2470=CARTESIAN_POINT ( 'NONE',  ( 3.484027466210578794, 1.954031737839658334, -0.6398539634642703700 ) ) ;
#2478=EDGE_LOOP ( 'NONE', ( #1747, #6310 ) ) ;
#2480=ORIENTED_EDGE ( 'NONE', *, *, #6699, .T. ) ;
#2486=FACE_OUTER_BOUND ( 'NONE', #595, .T. ) ;
#2487=ORIENTED_EDGE ( 'NONE', *, *, #2947, .F. ) ;
#2492=AXIS2_PLACEMENT_3D ( 'NONE', #8925, #13569, #1953 ) ;
#2495=DIRECTION ( 'NONE',  ( -1.000000000000000000, -0.000000000000000000, -0.000000000000000000 ) ) ;
#2496=EDGE_LOOP ( 'NONE', ( #11790, #11232, #4640, #166 ) ) ;
#2497=CARTESIAN_POINT ( 'NONE',  ( 3.426491571325181340, 1.987932976489903636, -0.2209981660730357955 ) ) ;
#2499=CARTESIAN_POINT ( 'NONE',  ( 3.426491571325181340, -1.575000000000027489, -2.359999999999986109 ) ) ;
#2502=EDGE_CURVE ( 'NONE', #4426, #8247, #2370, .T. ) ;
#2503=CARTESIAN_POINT ( 'NONE',  ( 4.532079842494805000, 1.713382837086246058, -0.4627352718838613765 ) ) ;
#2505=CARTESIAN_POINT ( 'NONE',  ( 2.774999999999999911, 3.360000000000016751, 0.9799999999999461364 ) ) ;
#2509=ORIENTED_EDGE ( 'NONE', *, *, #3481, .T. ) ;
#2512=AXIS2_PLACEMENT_3D ( 'NONE', #8729, #3771, #6438 ) ;
#2513=DIRECTION ( 'NONE',  ( 0.000000000000000000, 0.000000000000000000, 1.000000000000000000 ) ) ;
#2518=DIRECTION ( 'NONE',  ( 0.000000000000000000, 0.000000000000000000, -1.000000000000000000 ) ) ;
#2519=CARTESIAN_POINT ( 'NONE',  ( 3.426491571325181340, -2.400000000000011902, -0.6999999999999596545 ) ) ;
#2522=CIRCLE ( 'NONE', #12040, 0.4070000000000000839 ) ;
#2523=B_SPLINE_CURVE_WITH_KNOTS ( 'NONE', 3,
 ( #10626, #6267, #10928, #11850, #4904, #9779, #4822, #9492, #14140, #12986, #1352, #9568, #3748, #7704 ),
 .UNSPECIFIED., .F., .F.,
 ( 4, 2, 2, 2, 2, 2, 4 ),
 ( 1.868354362588067661E-17, 0.003338103516181846215, 0.005007155274272739182, 0.006676207032363632582, 0.01001431054854545408, 0.01168336230663636482, 0.01335241406472727557 ),
 .UNSPECIFIED. ) ;
#2524=DIRECTION ( 'NONE',  ( 0.000000000000000000, 0.000000000000000000, -1.000000000000000000 ) ) ;
#2526=DIRECTION ( 'NONE',  ( -1.000000000000000000, -0.000000000000000000, -0.000000000000000000 ) ) ;
#2528=CONICAL_SURFACE ( 'NONE', #7412, 1.039370078740158965, 0.7853981633974517207 ) ;
#2532=ORIENTED_EDGE ( 'NONE', *, *, #9832, .F. ) ;
#2534=CARTESIAN_POINT ( 'NONE',  ( 2.980731298636167370, 3.137999999999999901, -0.3249191361593797844 ) ) ;
#2538=EDGE_CURVE ( 'NONE', #9885, #4893, #123, .T. ) ;
#2539=DIRECTION ( 'NONE',  ( 1.000000000000000000, 0.000000000000000000, 0.000000000000000000 ) ) ;
#2541=DIRECTION ( 'NONE',  ( 1.000000000000000000, 0.000000000000000000, 0.000000000000000000 ) ) ;
#2542=CIRCLE ( 'NONE', #302, 0.3750000000000004996 ) ;
#2544=DIRECTION ( 'NONE',  ( 0.000000000000000000, 0.000000000000000000, 1.000000000000000000 ) ) ;
#2546=DIRECTION ( 'NONE',  ( 0.000000000000000000, 0.000000000000000000, -1.000000000000000000 ) ) ;
#2547=DIRECTION ( 'NONE',  ( 0.000000000000000000, 0.000000000000000000, 1.000000000000000000 ) ) ;
#2555=DIRECTION ( 'NONE',  ( -1.000000000000000000, -0.000000000000000000, -0.000000000000000000 ) ) ;
#2556=EDGE_CURVE ( 'NONE', #1593, #6459, #3825, .T. ) ;
#2557=ADVANCED_FACE ( 'NONE', ( #3964, #7347, #9712, #1438, #1508, #419 ), #203, .T. ) ;
#2560=B_SPLINE_CURVE_WITH_KNOTS ( 'NONE', 3,
 ( #8847, #1952, #3112, #3189 ),
 .UNSPECIFIED., .F., .F.,
 ( 4, 4 ),
 ( 0.01473257324215802161, 0.01653313341413566867 ),
 .UNSPECIFIED. ) ;
#2563=ORIENTED_EDGE ( 'NONE', *, *, #11459, .F. ) ;
#2564=VERTEX_POINT ( 'NONE', #9641 ) ;
#2568=CARTESIAN_POINT ( 'NONE',  ( 4.315797241329101475, 2.750000000000000000, 1.570821732971949825 ) ) ;
#2569=DIRECTION ( 'NONE',  ( -1.000000000000000000, -0.000000000000000000, -0.000000000000000000 ) ) ;
#2577=DIRECTION ( 'NONE',  ( -1.000000000000000000, -0.000000000000000000, -0.000000000000000000 ) ) ;
#2579=CARTESIAN_POINT ( 'NONE',  ( 4.339042227135573526, 1.728400208608292576, -0.5915559626296543749 ) ) ;
#2584=AXIS2_PLACEMENT_3D ( 'NONE', #555, #1643, #10921 ) ;
#2587=ORIENTED_EDGE ( 'NONE', *, *, #5028, .F. ) ;
#2588=EDGE_CURVE ( 'NONE', #6001, #11537, #12107, .T. ) ;
#2589=ADVANCED_FACE ( 'NONE', ( #4975 ), #1355, .F. ) ;
#2590=DIRECTION ( 'NONE',  ( -1.000000000000000000, -0.000000000000000000, -0.000000000000000000 ) ) ;
#2592=ORIENTED_EDGE ( 'NONE', *, *, #8020, .F. ) ;
#2604=CARTESIAN_POINT ( 'NONE',  ( 4.572381542873881877, 1.717371224058993340, -0.4020716753058218296 ) ) ;
#2606=VERTEX_POINT ( 'NONE', #5125 ) ;
#2610=EDGE_LOOP ( 'NONE', ( #10486, #5324 ) ) ;
#2612=CARTESIAN_POINT ( 'NONE',  ( 3.875000000000000000, 1.112678268764263789, 0.4849999999999995981 ) ) ;
#2617=DIRECTION ( 'NONE',  ( -1.000000000000000000, -0.000000000000000000, -0.000000000000000000 ) ) ;
#2620=ORIENTED_EDGE ( 'NONE', *, *, #2538, .F. ) ;
#2627=ORIENTED_EDGE ( 'NONE', *, *, #4803, .T. ) ;
#2632=VECTOR ( 'NONE', #339, 39.37007874015748143 ) ;
#2634=CARTESIAN_POINT ( 'NONE',  ( 3.426491571325181340, -2.360000000000016751, -0.9799999999999431388 ) ) ;
#2635=CARTESIAN_POINT ( 'NONE',  ( 2.774999999999999911, -1.575000000000027489, -2.359999999999989218 ) ) ;
#2640=ORIENTED_EDGE ( 'NONE', *, *, #3537, .T. ) ;
#2648=CARTESIAN_POINT ( 'NONE',  ( 3.851988768209213987, 1.889494746496508393, -0.4996036056591527941 ) ) ;
#2657=AXIS2_PLACEMENT_3D ( 'NONE', #9521, #4696, #1154 ) ;
#2659=CYLINDRICAL_SURFACE ( 'NONE', #7418, 0.2625000000000000111 ) ;
#2668=ORIENTED_EDGE ( 'NONE', *, *, #7606, .F. ) ;
#2673=CARTESIAN_POINT ( 'NONE',  ( 6.826491571325181695, -1.679378605318047946, -1.679378605318053497 ) ) ;
#2678=CARTESIAN_POINT ( 'NONE',  ( 6.176491571325181340, -1.679378605318047946, -1.679378605318053497 ) ) ;
#2679=CARTESIAN_POINT ( 'NONE',  ( 3.550764771811983245, 1.993778310833772105, 0.6763632542489218524 ) ) ;
#2680=CARTESIAN_POINT ( 'NONE',  ( 2.774999999999999911, -0.9799999999999436939, 3.360000000000016751 ) ) ;
#2681=VERTEX_POINT ( 'NONE', #1881 ) ;
#2683=FACE_BOUND ( 'NONE', #11984, .T. ) ;
#2685=ORIENTED_EDGE ( 'NONE', *, *, #12432, .T. ) ;
#2688=( NAMED_UNIT ( * ) PLANE_ANGLE_UNIT ( ) SI_UNIT ( $, .RADIAN. ) );
#2690=VERTEX_POINT ( 'NONE', #10365 ) ;
#2696=ADVANCED_FACE ( 'NONE', ( #11514 ), #3038, .F. ) ;
#2700=DIRECTION ( 'NONE',  ( 0.7071067811865429098, 0.000000000000000000, -0.7071067811865521247 ) ) ;
#2701=DIRECTION ( 'NONE',  ( 0.000000000000000000, 0.000000000000000000, -1.000000000000000000 ) ) ;
#2709=DIRECTION ( 'NONE',  ( -1.000000000000000000, -0.000000000000000000, -0.000000000000000000 ) ) ;
#2710=CARTESIAN_POINT ( 'NONE',  ( 3.874999999999999556, 3.105999999999998984, 1.509999999999999787 ) ) ;
#2711=DIRECTION ( 'NONE',  ( 0.000000000000000000, 0.000000000000000000, -1.000000000000000000 ) ) ;
#2712=LINE ( 'NONE', #2854, #12650 ) ;
#2716=ORIENTED_EDGE ( 'NONE', *, *, #9923, .F. ) ;
#2717=ORIENTED_EDGE ( 'NONE', *, *, #9399, .F. ) ;
#2723=CARTESIAN_POINT ( 'NONE',  ( 3.426491571325181340, -1.679378605318059048, -1.416878605318056872 ) ) ;
#2725=CARTESIAN_POINT ( 'NONE',  ( 6.787121492585022509, 0.000000000000000000, 0.000000000000000000 ) ) ;
#2726=EDGE_CURVE ( 'NONE', #9791, #628, #3712, .T. ) ;
#2730=AXIS2_PLACEMENT_3D ( 'NONE', #2864, #1555, #1484 ) ;
#2731=ORIENTED_EDGE ( 'NONE', *, *, #10258, .T. ) ;
#2733=ORIENTED_EDGE ( 'NONE', *, *, #10286, .F. ) ;
#2736=CARTESIAN_POINT ( 'NONE',  ( 4.329878488001781101, 0.9782040126189885942, -0.2082197225034957411 ) ) ;
#2746=CARTESIAN_POINT ( 'NONE',  ( 3.772736115549563340, 1.833816802295039849, 0.7431948924224894837 ) ) ;
#2753=CARTESIAN_POINT ( 'NONE',  ( 3.873439288382781065, 2.750000000000000000, 6.065921084684207584E-32 ) ) ;
#2756=CONICAL_SURFACE ( 'NONE', #992, 0.2945000000000006501, 0.7853981633974503884 ) ;
#2757=DIRECTION ( 'NONE',  ( 0.000000000000000000, 0.000000000000000000, -1.000000000000000000 ) ) ;
#2759=ADVANCED_FACE ( 'NONE', ( #3642 ), #2835, .T. ) ;
#2764=LINE ( 'NONE', #7434, #9505 ) ;
#2772=ORIENTED_EDGE ( 'NONE', *, *, #8012, .T. ) ;
#2774=( CONVERSION_BASED_UNIT ( 'INCH', #13234 ) LENGTH_UNIT ( ) NAMED_UNIT ( #12236 ) );
#2778=CARTESIAN_POINT ( 'NONE',  ( 2.806999999999999940, -1.679378605318059048, -1.941878605318027251 ) ) ;
#2781=CLOSED_SHELL ( 'NONE', ( #2759, #10821, #1746, #795, #9814, #5799, #13934, #5060 ) ) ;
#2789=ORIENTED_EDGE ( 'NONE', *, *, #13488, .T. ) ;
#2792=DIRECTION ( 'NONE',  ( 1.000000000000000000, 0.000000000000000000, 0.000000000000000000 ) ) ;
#2793=DIRECTION ( 'NONE',  ( 0.000000000000000000, 0.000000000000000000, 1.000000000000000000 ) ) ;
#2794=CARTESIAN_POINT ( 'NONE',  ( 3.426491571325181340, -0.9799999999999436939, 2.360000000000016307 ) ) ;
#2795=CARTESIAN_POINT ( 'NONE',  ( 4.146569453972532848, 1.792765056676476121, 0.6998195859356590720 ) ) ;
#2798=ADVANCED_FACE ( 'NONE', ( #2486 ), #8157, .F. ) ;
#2805=AXIS2_PLACEMENT_3D ( 'NONE', #4001, #5086, #8670 ) ;
#2806=VECTOR ( 'NONE', #2617, 39.37007874015748143 ) ;
#2808=DIRECTION ( 'NONE',  ( 0.000000000000000000, 1.000000000000000000, -0.000000000000000000 ) ) ;
#2810=DIRECTION ( 'NONE',  ( 0.000000000000000000, 0.000000000000000000, -1.000000000000000000 ) ) ;
#2815=AXIS2_PLACEMENT_3D ( 'NONE', #2039, #10473, #10622 ) ;
#2816=DIRECTION ( 'NONE',  ( 1.000000000000000000, 0.000000000000000000, 0.000000000000000000 ) ) ;
#2820=CARTESIAN_POINT ( 'NONE',  ( 3.411537114321682385, 2.070878521370026704, 0.5884327097963867326 ) ) ;
#2821=DIRECTION ( 'NONE',  ( -0.7071067811865425767, 0.000000000000000000, 0.7071067811865523467 ) ) ;
#2822=EDGE_CURVE ( 'NONE', #10976, #3309, #11817, .T. ) ;
#2825=DIRECTION ( 'NONE',  ( 0.000000000000000000, 0.000000000000000000, -1.000000000000000000 ) ) ;
#2826=CARTESIAN_POINT ( 'NONE',  ( 3.394491571325183088, 1.679378605318059048, 1.679378605318041506 ) ) ;
#2827=EDGE_LOOP ( 'NONE', ( #654, #1518, #9071, #5555 ) ) ;
#2833=CARTESIAN_POINT ( 'NONE',  ( 2.774999999999999911, -2.399999999999999911, 0.7000000000000007327 ) ) ;
#2835=TOROIDAL_SURFACE ( 'NONE', #7247, 0.5849999999999996314, 0.1000000000000000056 ) ;
#2838=DIRECTION ( 'NONE',  ( -1.000000000000000000, -0.000000000000000000, -0.000000000000000000 ) ) ;
#2842=DIRECTION ( 'NONE',  ( 0.000000000000000000, 0.000000000000000000, -1.000000000000000000 ) ) ;
#2848=ORIENTED_EDGE ( 'NONE', *, *, #5411, .T. ) ;
#2849=CYLINDRICAL_SURFACE ( 'NONE', #12927, 0.7849999999999958122 ) ;
#2850=CIRCLE ( 'NONE', #6275, 0.4070000000000025264 ) ;
#2854=CARTESIAN_POINT ( 'NONE',  ( 6.176491571325181340, 1.679378605318035733, -1.272378605318063016 ) ) ;
#2855=CARTESIAN_POINT ( 'NONE',  ( 3.426491571325181340, 1.679378605318042395, -1.679378605318058604 ) ) ;
#2857=DIRECTION ( 'NONE',  ( 0.000000000000000000, 0.000000000000000000, -1.000000000000000000 ) ) ;
#2862=CARTESIAN_POINT ( 'NONE',  ( 2.774999999999999911, 1.679378605318042395, -1.679378605318058604 ) ) ;
#2864=CARTESIAN_POINT ( 'NONE',  ( 3.875000000000000000, 3.137999999999999901, 0.000000000000000000 ) ) ;
#2866=CARTESIAN_POINT ( 'NONE',  ( 3.394491571325183088, 1.679378605318059048, 1.416878605318041551 ) ) ;
#2868=CARTESIAN_POINT ( 'NONE',  ( 3.426491571325180452, 2.038249570078020767, -0.6032545795923431875 ) ) ;
#2871=CIRCLE ( 'NONE', #14851, 1.580000000000000071 ) ;
#2872=EDGE_CURVE ( 'NONE', #10222, #4965, #1397, .T. ) ;
#2874=VERTEX_POINT ( 'NONE', #306 ) ;
#2878=CARTESIAN_POINT ( 'NONE',  ( 4.251234628174230146, 0.9439865100702572454, 0.3308754778004969754 ) ) ;
#2882=ORIENTED_EDGE ( 'NONE', *, *, #11350, .T. ) ;
#2884=CARTESIAN_POINT ( 'NONE',  ( 2.774999999999999911, -1.679378605318041950, 1.384878605318060174 ) ) ;
#2885=VECTOR ( 'NONE', #6652, 39.37007874015748854 ) ;
#2887=CYLINDRICAL_SURFACE ( 'NONE', #13355, 2.500000000000000000 ) ;
#2889=AXIS2_PLACEMENT_3D ( 'NONE', #9496, #11783, #2371 ) ;
#2890=AXIS2_PLACEMENT_3D ( 'NONE', #14482, #8681, #13011 ) ;
#2894=CARTESIAN_POINT ( 'NONE',  ( 3.464768837743798180, 2.040166567261363806, 0.6277031159343403610 ) ) ;
#2897=VERTEX_POINT ( 'NONE', #1545 ) ;
#2899=DIRECTION ( 'NONE',  ( 0.000000000000000000, 0.000000000000000000, 1.000000000000000000 ) ) ;
#2904=EDGE_CURVE ( 'NONE', #8207, #504, #1699, .T. ) ;
#2910=CARTESIAN_POINT ( 'NONE',  ( 2.774999999999999911, -3.360000000000016751, -0.9799999999999434719 ) ) ;
#2914=DIRECTION ( 'NONE',  ( -1.000000000000000000, -0.000000000000000000, -0.000000000000000000 ) ) ;
#2915=AXIS2_PLACEMENT_3D ( 'NONE', #12442, #5489, #14502 ) ;
#2916=ADVANCED_FACE ( 'NONE', ( #5226 ), #6476, .F. ) ;
#2922=CARTESIAN_POINT ( 'NONE',  ( 2.774999999999999911, 1.679378605318059048, 1.973878605318042156 ) ) ;
#2923=AXIS2_PLACEMENT_3D ( 'NONE', #5169, #4015, #8682 ) ;
#2929=CARTESIAN_POINT ( 'NONE',  ( 3.426491571325181340, -1.679378605318041950, 1.679378605318059048 ) ) ;
#2930=CIRCLE ( 'NONE', #14652, 0.2624999999999852451 ) ;
#2931=EDGE_CURVE ( 'NONE', #4332, #12765, #13314, .T. ) ;
#2938=VERTEX_POINT ( 'NONE', #6306 ) ;
#2943=DIRECTION ( 'NONE',  ( -0.7071067811865450192, 8.659560562354962440E-17, -0.7071067811865499042 ) ) ;
#2946=CARTESIAN_POINT ( 'NONE',  ( 4.309129212023187883, 1.779759191753760961, 0.6131832303403281781 ) ) ;
#2947=EDGE_CURVE ( 'NONE', #9323, #1534, #9893, .T. ) ;
#2948=ORIENTED_EDGE ( 'NONE', *, *, #10453, .T. ) ;
#2951=ORIENTED_EDGE ( 'NONE', *, *, #9987, .T. ) ;
#2956=CARTESIAN_POINT ( 'NONE',  ( 4.329787394125403921, 0.9781619162179171489, 0.2084057614748135445 ) ) ;
#2960=CARTESIAN_POINT ( 'NONE',  ( 3.338341192736666851, 2.444564215954430964, 0.5254738313631823754 ) ) ;
#2969=CARTESIAN_POINT ( 'NONE',  ( 4.542752038648298907, 1.795296830498517737, 0.3463584498708582871 ) ) ;
#2971=ORIENTED_EDGE ( 'NONE', *, *, #7389, .T. ) ;
#2972=VERTEX_POINT ( 'NONE', #12190 ) ;
#2974=CYLINDRICAL_SURFACE ( 'NONE', #5295, 1.000000000000000000 ) ;
#2975=EDGE_LOOP ( 'NONE', ( #9136, #6309 ) ) ;
#2977=CARTESIAN_POINT ( 'NONE',  ( 3.426491571325181340, 2.360000000000015863, 0.9799999999999454703 ) ) ;
#2980=ORIENTED_EDGE ( 'NONE', *, *, #4972, .F. ) ;
#2984=CARTESIAN_POINT ( 'NONE',  ( 3.875000000000000000, 1.059999999999999165, -0.5000000000000002220 ) ) ;
#2989=CARTESIAN_POINT ( 'NONE',  ( 3.760993142307637704, 1.910979010964881430, 0.4873726947928629927 ) ) ;
#2993=CARTESIAN_POINT ( 'NONE',  ( 6.096491571325181269, 0.000000000000000000, -1.580000000000000071 ) ) ;
#2995=ORIENTED_EDGE ( 'NONE', *, *, #546, .F. ) ;
#2996=EDGE_CURVE ( 'NONE', #11615, #12467, #1766, .T. ) ;
#2998=ORIENTED_EDGE ( 'NONE', *, *, #5600, .F. ) ;
#3001=DIRECTION ( 'NONE',  ( 0.000000000000000000, 0.000000000000000000, -1.000000000000000000 ) ) ;
#3003=DIRECTION ( 'NONE',  ( 0.000000000000000000, 0.000000000000000000, 1.000000000000000000 ) ) ;
#3005=ORIENTED_EDGE ( 'NONE', *, *, #14572, .T. ) ;
#3006=CARTESIAN_POINT ( 'NONE',  ( 3.874999999999999556, 3.105999999999998984, -1.320000000000000062 ) ) ;
#3012=EDGE_CURVE ( 'NONE', #2938, #13105, #6717, .T. ) ;
#3015=AXIS2_PLACEMENT_3D ( 'NONE', #7753, #1419, #328 ) ;
#3019=LINE ( 'NONE', #9995, #6103 ) ;
#3022=CIRCLE ( 'NONE', #4993, 0.4070000000000022489 ) ;
#3024=VERTEX_POINT ( 'NONE', #6161 ) ;
#3026=ORIENTED_EDGE ( 'NONE', *, *, #775, .F. ) ;
#3028=CARTESIAN_POINT ( 'NONE',  ( 3.426491571325181340, 0.6999999999999599876, -2.400000000000011458 ) ) ;
#3029=DIRECTION ( 'NONE',  ( 0.000000000000000000, 0.000000000000000000, 1.000000000000000000 ) ) ;
#3034=DIRECTION ( 'NONE',  ( 0.000000000000000000, 0.000000000000000000, -1.000000000000000000 ) ) ;
#3035=DIRECTION ( 'NONE',  ( -1.000000000000000000, -0.000000000000000000, -0.000000000000000000 ) ) ;
#3038=CYLINDRICAL_SURFACE ( 'NONE', #6505, 1.000000000000000222 ) ;
#3041=CARTESIAN_POINT ( 'NONE',  ( 4.452635031260724574, 1.784628384941731039, 0.4805815215727117229 ) ) ;
#3043=CARTESIAN_POINT ( 'NONE',  ( 3.592218582573752261, 1.983838869798021154, -0.4129877013736156788 ) ) ;
#3048=DIRECTION ( 'NONE',  ( 0.000000000000000000, 0.000000000000000000, 1.000000000000000000 ) ) ;
#3057=EDGE_CURVE ( 'NONE', #12243, #5479, #7671, .T. ) ;
#3059=AXIS2_PLACEMENT_3D ( 'NONE', #2855, #9751, #6453 ) ;
#3062=CARTESIAN_POINT ( 'NONE',  ( 2.774999999999999911, 1.679378605318059048, 1.973878605318042156 ) ) ;
#3063=VERTEX_POINT ( 'NONE', #919 ) ;
#3064=CARTESIAN_POINT ( 'NONE',  ( 3.874999999999999556, 3.137999999999999901, 1.098000000000000087 ) ) ;
#3065=DIRECTION ( 'NONE',  ( -1.000000000000000000, -0.000000000000000000, -0.000000000000000000 ) ) ;
#3066=CARTESIAN_POINT ( 'NONE',  ( 3.375824834555410270, 0.9995867961477209462, 0.03321238156889033677 ) ) ;
#3067=ADVANCED_FACE ( 'NONE', ( #9056 ), #10872, .F. ) ;
#3068=CARTESIAN_POINT ( 'NONE',  ( 4.271198831181767908, 1.710003382540315808, -0.6913879080909109964 ) ) ;
#3069=ORIENTED_EDGE ( 'NONE', *, *, #617, .T. ) ;
#3070=AXIS2_PLACEMENT_3D ( 'NONE', #13091, #9447, #4772 ) ;
#3071=EDGE_CURVE ( 'NONE', #10523, #14399, #4774, .T. ) ;
#3073=LINE ( 'NONE', #452, #13321 ) ;
#3076=AXIS2_PLACEMENT_3D ( 'NONE', #8285, #6976, #2137 ) ;
#3081=CARTESIAN_POINT ( 'NONE',  ( 3.492022057095982568, 2.024959266993827889, -0.6451503923273511631 ) ) ;
#3082=EDGE_CURVE ( 'NONE', #12843, #6091, #11609, .T. ) ;
#3083=VECTOR ( 'NONE', #6746, 39.37007874015748143 ) ;
#3087=CIRCLE ( 'NONE', #10159, 0.3750000000000004996 ) ;
#3091=CARTESIAN_POINT ( 'NONE',  ( 3.587393574774031979, 1.880815582072911551, 0.7577781223979582759 ) ) ;
#3101=CARTESIAN_POINT ( 'NONE',  ( 4.525278585568729639, 1.792793477108324485, -0.3771970452947643881 ) ) ;
#3103=EDGE_CURVE ( 'NONE', #9683, #13623, #7695, .T. ) ;
#3105=VERTEX_POINT ( 'NONE', #7898 ) ;
#3107=VECTOR ( 'NONE', #3811, 39.37007874015748143 ) ;
#3108=ORIENTED_EDGE ( 'NONE', *, *, #5685, .F. ) ;
#3112=CARTESIAN_POINT ( 'NONE',  ( 3.921022896101461708, 1.873041151412256911, -0.4984237362096384794 ) ) ;
#3115=AXIS2_PLACEMENT_3D ( 'NONE', #541, #6314, #8548 ) ;
#3116=CARTESIAN_POINT ( 'NONE',  ( 3.874999999999999556, 3.105999999999998984, -1.320000000000000062 ) ) ;
#3119=CARTESIAN_POINT ( 'NONE',  ( 6.794491571325181667, 1.679378605318059492, 1.679378605318041506 ) ) ;
#3126=CARTESIAN_POINT ( 'NONE',  ( 4.116403661786756096, 1.796907475018162392, 0.7114969261561383540 ) ) ;
#3127=CARTESIAN_POINT ( 'NONE',  ( 3.759442893977343658, 1.920756169463178509, -0.4870029225387685345 ) ) ;
#3139=FACE_OUTER_BOUND ( 'NONE', #10716, .T. ) ;
#3140=VECTOR ( 'NONE', #2495, 39.37007874015748143 ) ;
#3141=DIRECTION ( 'NONE',  ( -1.000000000000000000, -0.000000000000000000, -0.000000000000000000 ) ) ;
#3150=CARTESIAN_POINT ( 'NONE',  ( 3.532925020153219631, 0.9310773776131279211, -0.3650227795079680759 ) ) ;
#3152=CARTESIAN_POINT ( 'NONE',  ( 3.629047196404351805, 1.863650056189079418, -0.7701527217475101494 ) ) ;
#3153=CIRCLE ( 'NONE', #6096, 0.2624999999999852451 ) ;
#3166=EDGE_CURVE ( 'NONE', #12504, #12651, #14034, .T. ) ;
#3170=CARTESIAN_POINT ( 'NONE',  ( 2.774999999999999911, -1.679378605318059048, -1.973878605318027724 ) ) ;
#3174=ORIENTED_EDGE ( 'NONE', *, *, #3071, .F. ) ;
#3184=AXIS2_PLACEMENT_3D ( 'NONE', #14283, #14210, #5047 ) ;
#3186=ORIENTED_EDGE ( 'NONE', *, *, #3057, .T. ) ;
#3187=ADVANCED_FACE ( 'NONE', ( #11265 ), #7451, .F. ) ;
#3188=VERTEX_POINT ( 'NONE', #161 ) ;
#3189=CARTESIAN_POINT ( 'NONE',  ( 3.944129661530210385, 1.867491090171841339, -0.4951980309903490363 ) ) ;
#3190=CARTESIAN_POINT ( 'NONE',  ( 3.426491571325181340, 0.000000000000000000, 0.000000000000000000 ) ) ;
#3192=EDGE_CURVE ( 'NONE', #12451, #1686, #13294, .T. ) ;
#3195=CARTESIAN_POINT ( 'NONE',  ( 3.129894412017060201, 2.499001391242224202, -0.07213773670819455253 ) ) ;
#3199=CARTESIAN_POINT ( 'NONE',  ( 3.932805631546712810, 1.785024703590347261, 0.7488574126153495492 ) ) ;
#3200=CARTESIAN_POINT ( 'NONE',  ( 6.176491571325181340, -1.679378605318047946, -2.086378605318055968 ) ) ;
#3201=ORIENTED_EDGE ( 'NONE', *, *, #11142, .T. ) ;
#3203=FACE_BOUND ( 'NONE', #6181, .T. ) ;
#3204=ORIENTED_EDGE ( 'NONE', *, *, #12724, .F. ) ;
#3209=ORIENTED_EDGE ( 'NONE', *, *, #5326, .F. ) ;
#3212=CONICAL_SURFACE ( 'NONE', #6393, 0.2944999999999856066, 0.7853981633974514986 ) ;
#3213=CARTESIAN_POINT ( 'NONE',  ( 3.394491571325180423, -1.679378605318059048, -1.679378605318041950 ) ) ;
#3217=FACE_OUTER_BOUND ( 'NONE', #6637, .T. ) ;
#3218=CARTESIAN_POINT ( 'NONE',  ( 3.448855552202333197, 1.982883164696786382, 0.2625902165005476463 ) ) ;
#3220=AXIS2_PLACEMENT_3D ( 'NONE', #993, #7979, #832 ) ;
#3221=DIRECTION ( 'NONE',  ( 0.000000000000000000, 0.000000000000000000, -1.000000000000000000 ) ) ;
#3225=CARTESIAN_POINT ( 'NONE',  ( 2.774999999999999911, -2.400000000000011902, -0.6999999999999596545 ) ) ;
#3226=EDGE_LOOP ( 'NONE', ( #5403, #13145, #4222, #14376 ) ) ;
#3228=CYLINDRICAL_SURFACE ( 'NONE', #7332, 0.9499999999999992895 ) ;
#3229=FACE_OUTER_BOUND ( 'NONE', #2294, .T. ) ;
#3231=FACE_OUTER_BOUND ( 'NONE', #14748, .T. ) ;
#3232=ORIENTED_EDGE ( 'NONE', *, *, #2064, .T. ) ;
#3233=DIRECTION ( 'NONE',  ( -1.000000000000000000, -0.000000000000000000, -0.000000000000000000 ) ) ;
#3236=ORIENTED_EDGE ( 'NONE', *, *, #6439, .F. ) ;
#3237=EDGE_CURVE ( 'NONE', #1686, #12451, #14304, .T. ) ;
#3238=EDGE_CURVE ( 'NONE', #6179, #8878, #4860, .T. ) ;
#3241=EDGE_CURVE ( 'NONE', #11167, #12941, #3851, .T. ) ;
#3246=CARTESIAN_POINT ( 'NONE',  ( 3.875000000000000000, 1.885381157978845312, 0.5000000000000002220 ) ) ;
#3247=VECTOR ( 'NONE', #11037, 39.37007874015748143 ) ;
#3249=VECTOR ( 'NONE', #13628, 39.37007874015748854 ) ;
#3250=CARTESIAN_POINT ( 'NONE',  ( 3.671600895815123167, 1.871391630887606405, -0.7219642105703503177 ) ) ;
#3255=CARTESIAN_POINT ( 'NONE',  ( 2.774999999999999911, -0.9799999999999986500, -3.359999999999999876 ) ) ;
#3260=FACE_OUTER_BOUND ( 'NONE', #10345, .T. ) ;
#3265=CARTESIAN_POINT ( 'NONE',  ( 3.394491571325182644, 1.679378605318042395, -1.679378605318058604 ) ) ;
#3266=EDGE_CURVE ( 'NONE', #4777, #2897, #8213, .T. ) ;
#3270=CARTESIAN_POINT ( 'NONE',  ( 3.945347773489349397, 1.834617440766652230, 0.7476453199387252946 ) ) ;
#3271=CARTESIAN_POINT ( 'NONE',  ( 2.774999999999999911, -3.360000000000000320, 0.9799999999999999822 ) ) ;
#3274=CIRCLE ( 'NONE', #320, 1.039370078740158965 ) ;
#3277=ORIENTED_EDGE ( 'NONE', *, *, #12305, .F. ) ;
#3293=CARTESIAN_POINT ( 'NONE',  ( 3.875000000000000000, 0.8660254037844385966, -0.5000000000000002220 ) ) ;
#3300=ORIENTED_EDGE ( 'NONE', *, *, #4420, .F. ) ;
#3301=DIRECTION ( 'NONE',  ( 0.000000000000000000, 0.000000000000000000, -1.000000000000000000 ) ) ;
#3303=AXIS2_PLACEMENT_3D ( 'NONE', #12404, #6608, #4387 ) ;
#3304=LINE ( 'NONE', #12625, #4253 ) ;
#3309=VERTEX_POINT ( 'NONE', #14015 ) ;
#3314=AXIS2_PLACEMENT_3D ( 'NONE', #9191, #8053, #12928 ) ;
#3316=FACE_OUTER_BOUND ( 'NONE', #13552, .T. ) ;
#3320=ORIENTED_EDGE ( 'NONE', *, *, #3528, .T. ) ;
#3323=CYLINDRICAL_SURFACE ( 'NONE', #5123, 0.5000000000000001110 ) ;
#3325=CARTESIAN_POINT ( 'NONE',  ( 2.774999999999999911, 1.679378605318059048, 1.384878605318040856 ) ) ;
#3329=ORIENTED_EDGE ( 'NONE', *, *, #14090, .F. ) ;
#3335=DIRECTION ( 'NONE',  ( 0.000000000000000000, 0.000000000000000000, 1.000000000000000000 ) ) ;
#3337=CARTESIAN_POINT ( 'NONE',  ( 3.126632629065664748, 2.499978424780176400, 0.05909466466767844539 ) ) ;
#3339=DIRECTION ( 'NONE',  ( -0.000000000000000000, 1.000000000000000000, -0.000000000000000000 ) ) ;
#3342=EDGE_CURVE ( 'NONE', #13623, #9683, #6736, .T. ) ;
#3344=FACE_OUTER_BOUND ( 'NONE', #11274, .T. ) ;
#3345=CARTESIAN_POINT ( 'NONE',  ( 4.586364424524735028, 1.743277076888124277, 0.2448609443050739909 ) ) ;
#3351=ORIENTED_EDGE ( 'NONE', *, *, #7380, .F. ) ;
#3356=CARTESIAN_POINT ( 'NONE',  ( 6.176491571325181340, 1.679378605318035733, -2.086378605318067958 ) ) ;
#3359=DIRECTION ( 'NONE',  ( 0.000000000000000000, 0.000000000000000000, -1.000000000000000000 ) ) ;
#3361=VECTOR ( 'NONE', #8853, 39.37007874015748143 ) ;
#3366=CARTESIAN_POINT ( 'NONE',  ( 3.874999999999999556, 3.137999999999999901, -1.320000000000000062 ) ) ;
#3373=LINE ( 'NONE', #905, #7244 ) ;
#3375=ORIENTED_EDGE ( 'NONE', *, *, #7592, .T. ) ;
#3380=AXIS2_PLACEMENT_3D ( 'NONE', #9510, #10647, #6210 ) ;
#3385=AXIS2_PLACEMENT_3D ( 'NONE', #8219, #6914, #2388 ) ;
#3388=ORIENTED_EDGE ( 'NONE', *, *, #1011, .F. ) ;
#3390=CARTESIAN_POINT ( 'NONE',  ( 3.464667047197554250, 2.040221276569372133, -0.6276463482411095418 ) ) ;
#3393=CIRCLE ( 'NONE', #13394, 0.1899999999999996136 ) ;
#3395=VERTEX_POINT ( 'NONE', #3709 ) ;
#3398=ORIENTED_EDGE ( 'NONE', *, *, #12642, .F. ) ;
#3400=CARTESIAN_POINT ( 'NONE',  ( 3.921117472075024146, 1.873018435015763927, -0.4984105334006085908 ) ) ;
#3406=CARTESIAN_POINT ( 'NONE',  ( 3.828581658748513306, 1.898678166888137842, 0.4983806998886662343 ) ) ;
#3415=DIRECTION ( 'NONE',  ( 0.3420201433256623846, 0.000000000000000000, -0.9396926207859106484 ) ) ;
#3418=ORIENTED_EDGE ( 'NONE', *, *, #6233, .F. ) ;
#3420=CARTESIAN_POINT ( 'NONE',  ( 3.339098075141892163, 2.444574610142927096, -0.5239010158726820077 ) ) ;
#3431=ADVANCED_FACE ( 'NONE', ( #5361 ), #2327, .F. ) ;
#3436=EDGE_CURVE ( 'NONE', #13119, #8503, #1833, .T. ) ;
#3439=CARTESIAN_POINT ( 'NONE',  ( 3.875000000000000000, 0.8660254037844384856, 0.5000000000000002220 ) ) ;
#3446=FACE_OUTER_BOUND ( 'NONE', #14295, .T. ) ;
#3447=LINE ( 'NONE', #15148, #7320 ) ;
#3448=CARTESIAN_POINT ( 'NONE',  ( 4.531286706020566157, 1.713376479792114049, 0.4628985212650200687 ) ) ;
#3450=CARTESIAN_POINT ( 'NONE',  ( 2.807000000000000384, 1.679378605318059048, 1.679378605318041506 ) ) ;
#3459=DIRECTION ( 'NONE',  ( 1.000000000000000000, 0.000000000000000000, 0.000000000000000000 ) ) ;
#3467=EDGE_LOOP ( 'NONE', ( #4892, #4858, #8658, #10636 ) ) ;
#3472=CARTESIAN_POINT ( 'NONE',  ( 5.546318247523970513, 0.000000000000000000, 0.000000000000000000 ) ) ;
#3474=CARTESIAN_POINT ( 'NONE',  ( 3.875000000000000444, 1.884022191776434152, -0.5000000000000002220 ) ) ;
#3475=AXIS2_PLACEMENT_3D ( 'NONE', #3265, #14968, #11225 ) ;
#3480=EDGE_CURVE ( 'NONE', #11008, #327, #11870, .T. ) ;
#3481=EDGE_CURVE ( 'NONE', #4487, #12451, #661, .T. ) ;
#3489=( LENGTH_UNIT ( ) NAMED_UNIT ( * ) SI_UNIT ( $, .METRE. ) );
#3491=VERTEX_POINT ( 'NONE', #13292 ) ;
#3492=DIRECTION ( 'NONE',  ( 0.000000000000000000, 0.000000000000000000, -1.000000000000000000 ) ) ;
#3493=AXIS2_PLACEMENT_3D ( 'NONE', #12111, #1261, #7449 ) ;
#3495=DIRECTION ( 'NONE',  ( 0.000000000000000000, 0.000000000000000000, 1.000000000000000000 ) ) ;
#3496=CARTESIAN_POINT ( 'NONE',  ( 4.685892362381063769, 1.733292669144359976, -0.01737435135451124296 ) ) ;
#3499=VERTEX_POINT ( 'NONE', #2833 ) ;
#3503=ORIENTED_EDGE ( 'NONE', *, *, #6248, .T. ) ;
#3504=CYLINDRICAL_SURFACE ( 'NONE', #9710, 2.500000000000000000 ) ;
#3506=CARTESIAN_POINT ( 'NONE',  ( 3.875000000000000000, 3.137999999999999901, -0.5000000000000002220 ) ) ;
#3508=AXIS2_PLACEMENT_3D ( 'NONE', #9130, #4317, #4394 ) ;
#3512=FACE_OUTER_BOUND ( 'NONE', #551, .T. ) ;
#3519=DIRECTION ( 'NONE',  ( 0.000000000000000000, 0.7071067811865509034, 0.7071067811865441310 ) ) ;
#3521=CARTESIAN_POINT ( 'NONE',  ( 4.374625251963650818, 1.706956914788115842, 0.6219410930580085983 ) ) ;
#3528=EDGE_CURVE ( 'NONE', #14976, #10812, #4538, .T. ) ;
#3531=FACE_OUTER_BOUND ( 'NONE', #13889, .T. ) ;
#3532=AXIS2_PLACEMENT_3D ( 'NONE', #5191, #9855, #6415 ) ;
#3537=EDGE_CURVE ( 'NONE', #6615, #12114, #8036, .T. ) ;
#3538=CARTESIAN_POINT ( 'NONE',  ( 3.498666114443761188, 1.947009193665356408, -0.6486007100584754159 ) ) ;
#3544=CARTESIAN_POINT ( 'NONE',  ( 6.794491571325181667, 1.679378605318059492, 1.679378605318041506 ) ) ;
#3545=ORIENTED_EDGE ( 'NONE', *, *, #10103, .F. ) ;
#3551=EDGE_CURVE ( 'NONE', #11593, #4577, #10176, .T. ) ;
#3552=CARTESIAN_POINT ( 'NONE',  ( 3.944129661530210385, 1.867491090171841339, -0.4951980309903490363 ) ) ;
#3553=CARTESIAN_POINT ( 'NONE',  ( 3.426491571325181340, 1.575000000000016387, 2.359999999999999876 ) ) ;
#3554=ADVANCED_FACE ( 'NONE', ( #4285 ), #13557, .F. ) ;
#3555=VECTOR ( 'NONE', #8645, 39.37007874015748143 ) ;
#3559=CARTESIAN_POINT ( 'NONE',  ( 3.739718906115036212, 1.845510024168589558, -0.7378645487154772420 ) ) ;
#3561=EDGE_LOOP ( 'NONE', ( #4475, #3905, #2789, #11302 ) ) ;
#3564=CONICAL_SURFACE ( 'NONE', #1351, 0.4070000000000022489, 0.7853981633974547183 ) ;
#3565=CARTESIAN_POINT ( 'NONE',  ( 3.426491571325181784, 2.015787472269954694, 0.6125935857979679655 ) ) ;
#3566=ORIENTED_EDGE ( 'NONE', *, *, #13826, .F. ) ;
#3570=CARTESIAN_POINT ( 'NONE',  ( 3.874999999999999556, 2.750000000000000000, 1.320000000000000062 ) ) ;
#3575=EDGE_CURVE ( 'NONE', #10219, #13623, #2207, .T. ) ;
#3579=CIRCLE ( 'NONE', #12119, 1.999999999999999334 ) ;
#3581=CARTESIAN_POINT ( 'NONE',  ( 4.621558427459308227, 1.809512430825229501, -0.08833967945055898330 ) ) ;
#3582=ORIENTED_EDGE ( 'NONE', *, *, #13787, .F. ) ;
#3601=DIRECTION ( 'NONE',  ( 0.000000000000000000, 1.000000000000000000, -0.000000000000000000 ) ) ;
#3603=DIRECTION ( 'NONE',  ( -1.000000000000000000, -0.000000000000000000, -0.000000000000000000 ) ) ;
#3604=CARTESIAN_POINT ( 'NONE',  ( 3.426491571325181340, 2.062169880637645836, 0.5999481385559802815 ) ) ;
#3606=FACE_OUTER_BOUND ( 'NONE', #2496, .T. ) ;
#3608=ORIENTED_EDGE ( 'NONE', *, *, #11734, .F. ) ;
#3619=ORIENTED_EDGE ( 'NONE', *, *, #7363, .F. ) ;
#3621=CARTESIAN_POINT ( 'NONE',  ( 3.463409033965894945, 1.936472266768732631, -0.7051516699459041693 ) ) ;
#3622=CARTESIAN_POINT ( 'NONE',  ( 3.426491571325181340, -1.575000000000027489, -2.359999999999989218 ) ) ;
#3628=DIRECTION ( 'NONE',  ( 0.000000000000000000, 0.000000000000000000, -1.000000000000000000 ) ) ;
#3629=ORIENTED_EDGE ( 'NONE', *, *, #9770, .F. ) ;
#3639=EDGE_CURVE ( 'NONE', #4204, #7643, #5815, .T. ) ;
#3640=TOROIDAL_SURFACE ( 'NONE', #3380, 0.5849999999999996314, 0.1000000000000000056 ) ;
#3641=EDGE_CURVE ( 'NONE', #12635, #11468, #4359, .T. ) ;
#3642=FACE_OUTER_BOUND ( 'NONE', #8211, .T. ) ;
#3643=ORIENTED_EDGE ( 'NONE', *, *, #4667, .F. ) ;
#3644=ORIENTED_EDGE ( 'NONE', *, *, #10305, .T. ) ;
#3650=AXIS2_PLACEMENT_3D ( 'NONE', #14832, #10401, #14985 ) ;
#3651=DIRECTION ( 'NONE',  ( -0.000000000000000000, -1.000000000000000000, -0.000000000000000000 ) ) ;
#3659=AXIS2_PLACEMENT_3D ( 'NONE', #11491, #6910, #11562 ) ;
#3660=EDGE_CURVE ( 'NONE', #12028, #3309, #1635, .T. ) ;
#3663=CARTESIAN_POINT ( 'NONE',  ( 4.682446348489560428, 1.732706346088367821, -0.07442871938619251282 ) ) ;
#3676=CARTESIAN_POINT ( 'NONE',  ( 2.774999999999999911, 0.7000000000000026201, 2.400000000000000355 ) ) ;
#3677=VECTOR ( 'NONE', #3710, 39.37007874015748143 ) ;
#3678=CYLINDRICAL_SURFACE ( 'NONE', #7112, 0.3750000000000004996 ) ;
#3682=CARTESIAN_POINT ( 'NONE',  ( 4.111704219024688634, 1.727819528799023008, 0.7588929890255357025 ) ) ;
#3686=ORIENTED_EDGE ( 'NONE', *, *, #545, .T. ) ;
#3691=LINE ( 'NONE', #11792, #13361 ) ;
#3693=FACE_OUTER_BOUND ( 'NONE', #1307, .T. ) ;
#3700=DIRECTION ( 'NONE',  ( 1.000000000000000000, 0.000000000000000000, 0.000000000000000000 ) ) ;
#3708=ORIENTED_EDGE ( 'NONE', *, *, #15120, .T. ) ;
#3709=CARTESIAN_POINT ( 'NONE',  ( 3.426491571325181340, 2.058905028113295455, 0.2209981660730358233 ) ) ;
#3710=DIRECTION ( 'NONE',  ( 0.000000000000000000, -1.000000000000000000, 4.591341165822195764E-16 ) ) ;
#3712=LINE ( 'NONE', #11747, #3823 ) ;
#3717=ORIENTED_EDGE ( 'NONE', *, *, #1824, .T. ) ;
#3720=VECTOR ( 'NONE', #14931, 39.37007874015748143 ) ;
#3726=ORIENTED_EDGE ( 'NONE', *, *, #6804, .F. ) ;
#3729=DIRECTION ( 'NONE',  ( 0.000000000000000000, 0.000000000000000000, -1.000000000000000000 ) ) ;
#3730=DIRECTION ( 'NONE',  ( 0.000000000000000000, 0.000000000000000000, 1.000000000000000000 ) ) ;
#3732=ADVANCED_FACE ( 'NONE', ( #8351 ), #2126, .F. ) ;
#3733=VERTEX_POINT ( 'NONE', #9636 ) ;
#3734=LINE ( 'NONE', #1771, #10343 ) ;
#3738=ORIENTED_EDGE ( 'NONE', *, *, #725, .T. ) ;
#3739=AXIS2_PLACEMENT_3D ( 'NONE', #3622, #4925, #8223 ) ;
#3742=PLANE ( 'NONE',  #2325 ) ;
#3748=CARTESIAN_POINT ( 'NONE',  ( 3.855580484743782232, 1.862622002527129617, 0.7500000000000002220 ) ) ;
#3752=DIRECTION ( 'NONE',  ( 0.000000000000000000, 0.000000000000000000, 1.000000000000000000 ) ) ;
#3753=CARTESIAN_POINT ( 'NONE',  ( 3.426491571325181340, -3.360000000000016751, -0.9799999999999434719 ) ) ;
#3754=EDGE_LOOP ( 'NONE', ( #3973, #5459, #11643, #4358 ) ) ;
#3755=AXIS2_PLACEMENT_3D ( 'NONE', #5390, #8830, #13470 ) ;
#3765=EDGE_CURVE ( 'NONE', #8027, #2681, #11777, .T. ) ;
#3771=DIRECTION ( 'NONE',  ( 0.000000000000000000, 1.000000000000000000, 0.000000000000000000 ) ) ;
#3772=CARTESIAN_POINT ( 'NONE',  ( 3.876560711617219379, 2.749999999999999556, 0.000000000000000000 ) ) ;
#3773=ORIENTED_EDGE ( 'NONE', *, *, #10847, .F. ) ;
#3780=CARTESIAN_POINT ( 'NONE',  ( 2.807000000000000828, 1.679378605318042395, -1.416878605318058870 ) ) ;
#3781=EDGE_CURVE ( 'NONE', #12504, #14976, #10624, .T. ) ;
#3784=LINE ( 'NONE', #3933, #11198 ) ;
#3786=CARTESIAN_POINT ( 'NONE',  ( 3.875000000000000000, 3.085321731235734610, 0.000000000000000000 ) ) ;
#3787=EDGE_LOOP ( 'NONE', ( #9795, #10789, #13530, #749 ) ) ;
#3789=ORIENTED_EDGE ( 'NONE', *, *, #8615, .T. ) ;
#3794=LINE ( 'NONE', #10828, #8294 ) ;
#3795=CARTESIAN_POINT ( 'NONE',  ( 3.783120606456237045, 1.905778818417516396, -0.4920270134196029210 ) ) ;
#3797=AXIS2_PLACEMENT_3D ( 'NONE', #12475, #1929, #2152 ) ;
#3801=DIRECTION ( 'NONE',  ( 0.000000000000000000, 0.000000000000000000, 1.000000000000000000 ) ) ;
#3809=DIRECTION ( 'NONE',  ( -0.000000000000000000, -1.000000000000000000, 0.000000000000000000 ) ) ;
#3810=VERTEX_POINT ( 'NONE', #14664 ) ;
#3811=DIRECTION ( 'NONE',  ( 0.000000000000000000, -8.723548215061523903E-15, -1.000000000000000000 ) ) ;
#3813=DIRECTION ( 'NONE',  ( 0.000000000000000000, 0.000000000000000000, -1.000000000000000000 ) ) ;
#3814=ORIENTED_EDGE ( 'NONE', *, *, #4974, .F. ) ;
#3817=EDGE_CURVE ( 'NONE', #9590, #13687, #8565, .T. ) ;
#3818=EDGE_CURVE ( 'NONE', #7544, #4913, #1150, .T. ) ;
#3820=CARTESIAN_POINT ( 'NONE',  ( 2.774999999999999911, 1.679378605318042395, -1.384878605318057732 ) ) ;
#3822=LINE ( 'NONE', #1576, #11581 ) ;
#3823=VECTOR ( 'NONE', #1244, 39.37007874015748143 ) ;
#3825=LINE ( 'NONE', #1579, #8689 ) ;
#3827=ADVANCED_FACE ( 'NONE', ( #9927 ), #9723, .F. ) ;
#3828=CARTESIAN_POINT ( 'NONE',  ( 3.615813188930276034, 1.869365972618699745, 0.7654627819274841816 ) ) ;
#3831=ORIENTED_EDGE ( 'NONE', *, *, #2931, .T. ) ;
#3832=DIRECTION ( 'NONE',  ( -1.000000000000000000, -0.000000000000000000, -0.000000000000000000 ) ) ;
#3840=DIMENSIONAL_EXPONENTS ( 1.000000000000000000, 0.000000000000000000, 0.000000000000000000, 0.000000000000000000, 0.000000000000000000, 0.000000000000000000, 0.000000000000000000 ) ;
#3844=EDGE_CURVE ( 'NONE', #9226, #9926, #11670, .T. ) ;
#3850=EDGE_CURVE ( 'NONE', #2690, #1229, #10845, .T. ) ;
#3851=B_SPLINE_CURVE_WITH_KNOTS ( 'NONE', 3,
 ( #3474, #14175, #3400, #3552 ),
 .UNSPECIFIED., .F., .F.,
 ( 4, 4 ),
 ( 0.01431391205243922465, 0.01610857355353898304 ),
 .UNSPECIFIED. ) ;
#3856=VECTOR ( 'NONE', #10600, 39.37007874015748143 ) ;
#3858=ORIENTED_EDGE ( 'NONE', *, *, #6805, .F. ) ;
#3866=ORIENTED_EDGE ( 'NONE', *, *, #5081, .T. ) ;
#3871=LINE ( 'NONE', #9826, #398 ) ;
#3873=DIRECTION ( 'NONE',  ( 0.7071067811865460184, 8.659560562354951347E-17, 0.7071067811865490160 ) ) ;
#3874=AXIS2_PLACEMENT_3D ( 'NONE', #11365, #7854, #14890 ) ;
#3875=FACE_OUTER_BOUND ( 'NONE', #2827, .T. ) ;
#3880=AXIS2_PLACEMENT_3D ( 'NONE', #5742, #4515, #10408 ) ;
#3882=ORIENTED_EDGE ( 'NONE', *, *, #7195, .F. ) ;
#3888=DIRECTION ( 'NONE',  ( -0.3420201433256623846, 0.000000000000000000, 0.9396926207859106484 ) ) ;
#3889=CARTESIAN_POINT ( 'NONE',  ( 4.307277324112376959, 0.9678925435312534242, 0.2517985120128621856 ) ) ;
#3891=CYLINDRICAL_SURFACE ( 'NONE', #8680, 0.7849999999999983658 ) ;
#3898=AXIS2_PLACEMENT_3D ( 'NONE', #2794, #8614, #6465 ) ;
#3901=CARTESIAN_POINT ( 'NONE',  ( 3.790489445559355630, 1.886052406415659410, 0.7452351935336294364 ) ) ;
#3903=LINE ( 'NONE', #3200, #5985 ) ;
#3905=ORIENTED_EDGE ( 'NONE', *, *, #12184, .T. ) ;
#3911=ORIENTED_EDGE ( 'NONE', *, *, #793, .T. ) ;
#3916=ORIENTED_EDGE ( 'NONE', *, *, #7592, .F. ) ;
#3921=AXIS2_PLACEMENT_3D ( 'NONE', #12754, #2283, #6966 ) ;
#3923=CARTESIAN_POINT ( 'NONE',  ( 3.394491571325180423, -1.679378605318059048, -1.416878605318056872 ) ) ;
#3928=VERTEX_POINT ( 'NONE', #12212 ) ;
#3930=CARTESIAN_POINT ( 'NONE',  ( 6.176491571325181340, -1.679378605318048390, 1.679378605318054163 ) ) ;
#3931=EDGE_CURVE ( 'NONE', #7544, #6090, #13344, .T. ) ;
#3932=FACE_OUTER_BOUND ( 'NONE', #2143, .T. ) ;
#3933=CARTESIAN_POINT ( 'NONE',  ( 3.426491571325181340, -2.359999999999979892, 1.575000000000016387 ) ) ;
#3937=CARTESIAN_POINT ( 'NONE',  ( 3.394491571325180423, -1.679378605318059048, -1.416878605318056872 ) ) ;
#3942=DIRECTION ( 'NONE',  ( 0.000000000000000000, 0.000000000000000000, -1.000000000000000000 ) ) ;
#3945=DIRECTION ( 'NONE',  ( 0.000000000000000000, 0.000000000000000000, -1.000000000000000000 ) ) ;
#3946=CIRCLE ( 'NONE', #13941, 0.5000000000000001110 ) ;
#3957=CARTESIAN_POINT ( 'NONE',  ( 3.891549542033483355, 0.8660254037844384856, 0.5000000000000000000 ) ) ;
#3959=PLANE ( 'NONE',  #7773 ) ;
#3964=FACE_OUTER_BOUND ( 'NONE', #4912, .T. ) ;
#3966=CARTESIAN_POINT ( 'NONE',  ( 3.414300654442014693, 1.988601236139950545, 0.5922175483633206339 ) ) ;
#3971=FACE_BOUND ( 'NONE', #9914, .T. ) ;
#3973=ORIENTED_EDGE ( 'NONE', *, *, #9098, .F. ) ;
#3974=FACE_OUTER_BOUND ( 'NONE', #411, .T. ) ;
#3985=AXIS2_PLACEMENT_3D ( 'NONE', #4200, #6797, #10020 ) ;
#3990=DIRECTION ( 'NONE',  ( -1.000000000000000000, -0.000000000000000000, -0.000000000000000000 ) ) ;
#3991=VERTEX_POINT ( 'NONE', #1874 ) ;
#3995=CYLINDRICAL_SURFACE ( 'NONE', #704, 0.1899999999999996136 ) ;
#4001=CARTESIAN_POINT ( 'NONE',  ( 6.176491571325181340, -1.679378605318047946, -1.679378605318053497 ) ) ;
#4002=B_SPLINE_CURVE_WITH_KNOTS ( 'NONE', 3,
 ( #7961, #2052, #10262, #4444, #2989, #9110, #6741, #8811, #11399, #747, #1826, #3218, #5516, #13452 ),
 .UNSPECIFIED., .F., .F.,
 ( 4, 2, 2, 2, 2, 2, 4 ),
 ( 0.001800564375689165265, 0.003589287776566951402, 0.005378011177444737105, 0.008955457979200349278, 0.01253290478095596232, 0.01432162818183375236, 0.01611035158271154066 ),
 .UNSPECIFIED. ) ;
#4004=EDGE_CURVE ( 'NONE', #4107, #4727, #4757, .T. ) ;
#4007=VERTEX_POINT ( 'NONE', #6136 ) ;
#4008=ORIENTED_EDGE ( 'NONE', *, *, #9987, .F. ) ;
#4015=DIRECTION ( 'NONE',  ( 1.000000000000000000, 0.000000000000000000, 0.000000000000000000 ) ) ;
#4016=CARTESIAN_POINT ( 'NONE',  ( 4.247253441970699761, 1.781917319165590818, 0.6538529083206351400 ) ) ;
#4018=VERTEX_POINT ( 'NONE', #11866 ) ;
#4024=ORIENTED_EDGE ( 'NONE', *, *, #2219, .F. ) ;
#4027=VECTOR ( 'NONE', #11334, 39.37007874015748143 ) ;
#4029=CARTESIAN_POINT ( 'NONE',  ( 4.368325430995946945, 0.9966752972897022778, 0.08311465223410480219 ) ) ;
#4030=EDGE_CURVE ( 'NONE', #4777, #6416, #2871, .T. ) ;
#4034=CARTESIAN_POINT ( 'NONE',  ( 3.874999999999999556, 2.782000000000000917, -1.320000000000000062 ) ) ;
#4036=AXIS2_PLACEMENT_3D ( 'NONE', #8349, #12909, #3813 ) ;
#4039=AXIS2_PLACEMENT_3D ( 'NONE', #10265, #4447, #11485 ) ;
#4041=FACE_OUTER_BOUND ( 'NONE', #521, .T. ) ;
#4042=LINE ( 'NONE', #8707, #10129 ) ;
#4045=CARTESIAN_POINT ( 'NONE',  ( 3.426491571325181784, 2.000448480535557128, 0.6224710308823616645 ) ) ;
#4046=DIRECTION ( 'NONE',  ( 0.000000000000000000, 0.000000000000000000, -1.000000000000000000 ) ) ;
#4047=ORIENTED_EDGE ( 'NONE', *, *, #545, .F. ) ;
#4049=DIRECTION ( 'NONE',  ( 0.000000000000000000, 1.000000000000000000, -0.000000000000000000 ) ) ;
#4052=CARTESIAN_POINT ( 'NONE',  ( 3.426491571325181340, -0.9799999999999986500, -3.359999999999999876 ) ) ;
#4060=ORIENTED_EDGE ( 'NONE', *, *, #9917, .T. ) ;
#4061=VECTOR ( 'NONE', #6977, 39.37007874015748143 ) ;
#4063=CARTESIAN_POINT ( 'NONE',  ( 2.774999999999999911, 1.679378605318042395, -1.679378605318058604 ) ) ;
#4065=VECTOR ( 'NONE', #12483, 39.37007874015748143 ) ;
#4066=CARTESIAN_POINT ( 'NONE',  ( 4.140646859253616974, 0.9057630807910989068, -0.4238992791336257393 ) ) ;
#4070=VERTEX_POINT ( 'NONE', #12999 ) ;
#4079=DIRECTION ( 'NONE',  ( 0.7071067811865512365, 8.659560562354884787E-17, 0.7071067811865436870 ) ) ;
#4080=AXIS2_PLACEMENT_3D ( 'NONE', #9769, #3809, #14426 ) ;
#4083=ORIENTED_EDGE ( 'NONE', *, *, #255, .T. ) ;
#4085=ORIENTED_EDGE ( 'NONE', *, *, #13997, .T. ) ;
#4090=DIRECTION ( 'NONE',  ( 0.000000000000000000, -1.000000000000000000, 9.641816448226552334E-15 ) ) ;
#4096=CARTESIAN_POINT ( 'NONE',  ( 4.559113081901449149, 1.797916179321159769, 0.3118124478677711808 ) ) ;
#4097=CIRCLE ( 'NONE', #9522, 1.000000000000000222 ) ;
#4099=AXIS2_PLACEMENT_3D ( 'NONE', #13288, #1519, #4131 ) ;
#4100=VERTEX_POINT ( 'NONE', #2534 ) ;
#4105=CARTESIAN_POINT ( 'NONE',  ( 4.307237825407486120, 0.9678748784477505529, -0.2518665318215109195 ) ) ;
#4107=VERTEX_POINT ( 'NONE', #2612 ) ;
#4109=CARTESIAN_POINT ( 'NONE',  ( 3.875000000000000000, 3.137999999999999901, -0.5000000000000002220 ) ) ;
#4110=LINE ( 'NONE', #1650, #7080 ) ;
#4117=DIRECTION ( 'NONE',  ( -1.000000000000000000, 0.000000000000000000, 0.000000000000000000 ) ) ;
#4119=CYLINDRICAL_SURFACE ( 'NONE', #2004, 1.000000000000000000 ) ;
#4121=CARTESIAN_POINT ( 'NONE',  ( 4.306829794387749821, 1.729417409056954291, 0.6145795567947273108 ) ) ;
#4128=AXIS2_PLACEMENT_3D ( 'NONE', #12385, #5283, #6589 ) ;
#4129=ORIENTED_EDGE ( 'NONE', *, *, #14591, .T. ) ;
#4131=DIRECTION ( 'NONE',  ( 0.000000000000000000, 0.000000000000000000, -1.000000000000000000 ) ) ;
#4150=CARTESIAN_POINT ( 'NONE',  ( 6.787121492585022509, 1.224646799147353207E-16, -1.000000000000000000 ) ) ;
#4152=ORIENTED_EDGE ( 'NONE', *, *, #11852, .F. ) ;
#4153=DIRECTION ( 'NONE',  ( 0.7071067811865523467, 0.000000000000000000, -0.7071067811865425767 ) ) ;
#4155=ORIENTED_EDGE ( 'NONE', *, *, #12989, .F. ) ;
#4156=DIRECTION ( 'NONE',  ( -1.000000000000000000, -0.000000000000000000, -0.000000000000000000 ) ) ;
#4160=CIRCLE ( 'NONE', #5382, 0.2944999999999987073 ) ;
#4163=ORIENTED_EDGE ( 'NONE', *, *, #5961, .F. ) ;
#4165=EDGE_CURVE ( 'NONE', #8481, #9027, #3691, .T. ) ;
#4166=DIRECTION ( 'NONE',  ( -1.000000000000000000, -0.000000000000000000, -0.000000000000000000 ) ) ;
#4171=ORIENTED_EDGE ( 'NONE', *, *, #13515, .F. ) ;
#4174=DIRECTION ( 'NONE',  ( -0.7071067811865557884, 0.000000000000000000, 0.7071067811865392461 ) ) ;
#4177=CARTESIAN_POINT ( 'NONE',  ( 4.512342262853154651, 1.791038700169719444, 0.3986247651315083518 ) ) ;
#4189=ORIENTED_EDGE ( 'NONE', *, *, #940, .F. ) ;
#4190=CARTESIAN_POINT ( 'NONE',  ( 2.527624975756972425, 3.137999999999999901, -0.9199802545633498640 ) ) ;
#4191=CARTESIAN_POINT ( 'NONE',  ( 3.874999999999999556, 2.782000000000002693, 1.320000000000000062 ) ) ;
#4199=CARTESIAN_POINT ( 'NONE',  ( 4.245121452821247310, 1.732603396039932520, 0.6542235875937751910 ) ) ;
#4200=CARTESIAN_POINT ( 'NONE',  ( 2.806999999999999496, -1.679378605318041950, 1.679378605318059048 ) ) ;
#4204=VERTEX_POINT ( 'NONE', #14599 ) ;
#4212=CARTESIAN_POINT ( 'NONE',  ( 2.774999999999999911, 0.000000000000000000, 0.000000000000000000 ) ) ;
#4214=EDGE_CURVE ( 'NONE', #13739, #6474, #14598, .T. ) ;
#4219=CARTESIAN_POINT ( 'NONE',  ( 3.378341036178184265, 0.9983173952992376865, -0.06652291956437350606 ) ) ;
#4220=CARTESIAN_POINT ( 'NONE',  ( 3.944129661530210385, 1.761538328845252188, -0.7935532608319411096 ) ) ;
#4221=EDGE_CURVE ( 'NONE', #803, #9092, #8515, .T. ) ;
#4222=ORIENTED_EDGE ( 'NONE', *, *, #14850, .T. ) ;
#4224=DIRECTION ( 'NONE',  ( 0.000000000000000000, 0.000000000000000000, 1.000000000000000000 ) ) ;
#4226=DIRECTION ( 'NONE',  ( 0.000000000000000000, 0.000000000000000000, 1.000000000000000000 ) ) ;
#4227=EDGE_LOOP ( 'NONE', ( #537, #2772, #12825, #13403 ) ) ;
#4230=ADVANCED_FACE ( 'NONE', ( #3974 ), #13441, .F. ) ;
#4236=CARTESIAN_POINT ( 'NONE',  ( 0.000000000000000000, 1.836970198721030181E-16, -1.500000000000000222 ) ) ;
#4237=ORIENTED_EDGE ( 'NONE', *, *, #1765, .F. ) ;
#4239=CARTESIAN_POINT ( 'NONE',  ( 3.897807165016460740, 1.773345575131051621, 0.7975644729706475866 ) ) ;
#4245=CARTESIAN_POINT ( 'NONE',  ( 2.774999999999999911, 0.000000000000000000, 0.000000000000000000 ) ) ;
#4250=CARTESIAN_POINT ( 'NONE',  ( 4.616842326592714763, 1.808536722254569629, -0.1228515035735000954 ) ) ;
#4253=VECTOR ( 'NONE', #11493, 39.37007874015748143 ) ;
#4254=AXIS2_PLACEMENT_3D ( 'NONE', #12851, #8291, #65 ) ;
#4255=CARTESIAN_POINT ( 'NONE',  ( 4.201664376791202749, 1.786179860254142104, -0.6761149289075030211 ) ) ;
#4261=CARTESIAN_POINT ( 'NONE',  ( 3.426491571325181340, -0.6999999999999587663, 2.400000000000012790 ) ) ;
#4266=LINE ( 'NONE', #2884, #7078 ) ;
#4271=CARTESIAN_POINT ( 'NONE',  ( 4.212694554283068271, 1.735282967767267426, 0.6714771266614066869 ) ) ;
#4274=ORIENTED_EDGE ( 'NONE', *, *, #3551, .F. ) ;
#4277=FACE_BOUND ( 'NONE', #6079, .T. ) ;
#4278=ORIENTED_EDGE ( 'NONE', *, *, #13418, .F. ) ;
#4284=EDGE_CURVE ( 'NONE', #6179, #1969, #14978, .T. ) ;
#4285=FACE_OUTER_BOUND ( 'NONE', #11578, .T. ) ;
#4289=AXIS2_PLACEMENT_3D ( 'NONE', #2295, #5746, #4600 ) ;
#4296=CARTESIAN_POINT ( 'NONE',  ( 3.851998792340888933, 1.785879153954030851, -0.7996516825436228437 ) ) ;
#4298=CARTESIAN_POINT ( 'NONE',  ( 3.941974925529625473, 0.8684515238967140949, -0.4957779064694355919 ) ) ;
#4300=ORIENTED_EDGE ( 'NONE', *, *, #11529, .F. ) ;
#4303=FACE_OUTER_BOUND ( 'NONE', #9580, .T. ) ;
#4305=LINE ( 'NONE', #8192, #10026 ) ;
#4307=CARTESIAN_POINT ( 'NONE',  ( 2.774999999999999911, -0.6999999999999989564, -2.399999999999999911 ) ) ;
#4314=DIRECTION ( 'NONE',  ( -1.000000000000000000, -0.000000000000000000, -0.000000000000000000 ) ) ;
#4315=CARTESIAN_POINT ( 'NONE',  ( 3.426491571325181340, 1.954234464180151676, 0.6847610993685215863 ) ) ;
#4317=DIRECTION ( 'NONE',  ( 1.000000000000000000, 0.000000000000000000, 0.000000000000000000 ) ) ;
#4325=CARTESIAN_POINT ( 'NONE',  ( 2.774999999999999911, 1.679378605318042395, -1.973878605318059698 ) ) ;
#4327=CIRCLE ( 'NONE', #625, 0.5000000000000002220 ) ;
#4332=VERTEX_POINT ( 'NONE', #12597 ) ;
#4335=CARTESIAN_POINT ( 'NONE',  ( 2.774999999999999911, -2.359999999999984333, 1.575000000000016387 ) ) ;
#4340=ORIENTED_EDGE ( 'NONE', *, *, #4346, .T. ) ;
#4341=CARTESIAN_POINT ( 'NONE',  ( 3.134971565885993794, 2.497487542101918923, -0.1157722030434289312 ) ) ;
#4346=EDGE_CURVE ( 'NONE', #10024, #4007, #10317, .T. ) ;
#4347=CARTESIAN_POINT ( 'NONE',  ( 4.336468708500340163, 1.779575802716562016, 0.5927141824020646377 ) ) ;
#4348=DIRECTION ( 'NONE',  ( -0.000000000000000000, -1.000000000000000000, -0.000000000000000000 ) ) ;
#4351=ORIENTED_EDGE ( 'NONE', *, *, #2265, .T. ) ;
#4352=FACE_BOUND ( 'NONE', #2975, .T. ) ;
#4353=ORIENTED_EDGE ( 'NONE', *, *, #2556, .T. ) ;
#4358=ORIENTED_EDGE ( 'NONE', *, *, #6925, .F. ) ;
#4359=LINE ( 'NONE', #1045, #10939 ) ;
#4363=LINE ( 'NONE', #12604, #14261 ) ;
#4372=AXIS2_PLACEMENT_3D ( 'NONE', #5300, #12406, #4458 ) ;
#4373=CARTESIAN_POINT ( 'NONE',  ( 3.375021911746136194, 0.9999890441286871656, -0.03364778508493743853 ) ) ;
#4378=DIRECTION ( 'NONE',  ( 0.000000000000000000, 0.000000000000000000, -1.000000000000000000 ) ) ;
#4387=DIRECTION ( 'NONE',  ( 0.000000000000000000, 0.000000000000000000, 1.000000000000000000 ) ) ;
#4389=EDGE_CURVE ( 'NONE', #12451, #2938, #6728, .T. ) ;
#4393=DIRECTION ( 'NONE',  ( 1.000000000000000000, 0.000000000000000000, 0.000000000000000000 ) ) ;
#4394=DIRECTION ( 'NONE',  ( 0.000000000000000000, 0.000000000000000000, -1.000000000000000000 ) ) ;
#4400=CARTESIAN_POINT ( 'NONE',  ( 2.774999999999999911, -1.679378605318041950, 1.973878605318057700 ) ) ;
#4403=VECTOR ( 'NONE', #13975, 39.37007874015748854 ) ;
#4404=DIRECTION ( 'NONE',  ( 0.000000000000000000, 0.000000000000000000, -1.000000000000000000 ) ) ;
#4408=DIRECTION ( 'NONE',  ( -1.000000000000000000, -0.000000000000000000, -0.000000000000000000 ) ) ;
#4409=CARTESIAN_POINT ( 'NONE',  ( 3.843202889607961303, 1.866619761049737702, -0.7500470051816043870 ) ) ;
#4419=CARTESIAN_POINT ( 'NONE',  ( 6.794491571325179891, -1.679378605318048390, 1.679378605318054163 ) ) ;
#4420=EDGE_CURVE ( 'NONE', #7408, #9092, #5732, .T. ) ;
#4423=DIRECTION ( 'NONE',  ( -1.000000000000000000, -0.000000000000000000, -0.000000000000000000 ) ) ;
#4424=CARTESIAN_POINT ( 'NONE',  ( 4.496007498000189173, 1.789057273259985203, 0.4232163064126445162 ) ) ;
#4426=VERTEX_POINT ( 'NONE', #8347 ) ;
#4427=ORIENTED_EDGE ( 'NONE', *, *, #3266, .F. ) ;
#4437=AXIS2_PLACEMENT_3D ( 'NONE', #4886, #400, #11907 ) ;
#4438=CARTESIAN_POINT ( 'NONE',  ( 3.875000000000619504, 1.884022191776286714, 0.5000000000000002220 ) ) ;
#4439=DIRECTION ( 'NONE',  ( 0.000000000000000000, 0.000000000000000000, -1.000000000000000000 ) ) ;
#4442=VERTEX_POINT ( 'NONE', #2443 ) ;
#4443=DIRECTION ( 'NONE',  ( 0.7071067811865450192, 0.000000000000000000, -0.7071067811865499042 ) ) ;
#4444=CARTESIAN_POINT ( 'NONE',  ( 3.783833682798621201, 1.905610919832175787, 0.4921549320435091301 ) ) ;
#4445=CARTESIAN_POINT ( 'NONE',  ( 3.761567849157291921, 1.814885103198726313, -0.7939663826119651713 ) ) ;
#4447=DIRECTION ( 'NONE',  ( -1.000000000000000000, -0.000000000000000000, -0.000000000000000000 ) ) ;
#4449=ORIENTED_EDGE ( 'NONE', *, *, #6068, .T. ) ;
#4454=FACE_OUTER_BOUND ( 'NONE', #9650, .T. ) ;
#4455=DIRECTION ( 'NONE',  ( -1.000000000000000000, -0.000000000000000000, -0.000000000000000000 ) ) ;
#4457=CARTESIAN_POINT ( 'NONE',  ( 3.874999999999999556, 2.782000000000000917, -1.320000000000000062 ) ) ;
#4458=DIRECTION ( 'NONE',  ( 0.000000000000000000, 0.000000000000000000, -1.000000000000000000 ) ) ;
#4459=ORIENTED_EDGE ( 'NONE', *, *, #3818, .F. ) ;
#4464=VECTOR ( 'NONE', #14612, 39.37007874015748143 ) ;
#4466=EDGE_LOOP ( 'NONE', ( #8818, #11285 ) ) ;
#4470=ADVANCED_FACE ( 'NONE', ( #5809 ), #1271, .T. ) ;
#4472=CARTESIAN_POINT ( 'NONE',  ( 3.715407914194799766, 1.936056580808199312, 0.4744061610882758240 ) ) ;
#4474=EDGE_CURVE ( 'NONE', #5449, #4107, #7020, .T. ) ;
#4475=ORIENTED_EDGE ( 'NONE', *, *, #8058, .T. ) ;
#4477=CIRCLE ( 'NONE', #6199, 1.039370078740158965 ) ;
#4478=ORIENTED_EDGE ( 'NONE', *, *, #5401, .T. ) ;
#4487=VERTEX_POINT ( 'NONE', #1199 ) ;
#4490=CONICAL_SURFACE ( 'NONE', #791, 0.2624999999999852451, 0.7853981633974428389 ) ;
#4492=EDGE_CURVE ( 'NONE', #6235, #7135, #5797, .T. ) ;
#4496=CARTESIAN_POINT ( 'NONE',  ( 4.613894443967907044, 1.807937564491455262, -0.1419188128446503272 ) ) ;
#4499=ADVANCED_FACE ( 'NONE', ( #10621 ), #8269, .T. ) ;
#4506=DIRECTION ( 'NONE',  ( 0.000000000000000000, 0.000000000000000000, 1.000000000000000000 ) ) ;
#4508=DIRECTION ( 'NONE',  ( 0.000000000000000000, 0.000000000000000000, -1.000000000000000000 ) ) ;
#4510=DIRECTION ( 'NONE',  ( 0.7071067811865523467, 8.659560562354873694E-17, 0.7071067811865425767 ) ) ;
#4515=DIRECTION ( 'NONE',  ( -0.000000000000000000, -1.000000000000000000, 0.000000000000000000 ) ) ;
#4517=CARTESIAN_POINT ( 'NONE',  ( 3.652526911380074903, 0.8940386994653520825, 0.4480710255186519109 ) ) ;
#4520=FACE_OUTER_BOUND ( 'NONE', #5132, .T. ) ;
#4522=ORIENTED_EDGE ( 'NONE', *, *, #12317, .F. ) ;
#4523=EDGE_LOOP ( 'NONE', ( #1637, #7905, #3174, #9326 ) ) ;
#4529=VECTOR ( 'NONE', #2232, 39.37007874015748143 ) ;
#4535=CIRCLE ( 'NONE', #10402, 0.3750000000000004996 ) ;
#4538=CIRCLE ( 'NONE', #13077, 0.9999999999999998890 ) ;
#4540=EDGE_LOOP ( 'NONE', ( #4658, #4645, #13026, #12282 ) ) ;
#4541=LINE ( 'NONE', #2239, #3249 ) ;
#4542=ADVANCED_FACE ( 'NONE', ( #10546 ), #149, .F. ) ;
#4544=CARTESIAN_POINT ( 'NONE',  ( 3.426491571325181340, -1.679378605318041950, 1.973878605318057700 ) ) ;
#4546=EDGE_LOOP ( 'NONE', ( #14768, #13484 ) ) ;
#4552=CARTESIAN_POINT ( 'NONE',  ( 6.794491571325179891, 1.679378605318035733, -2.054378605318066153 ) ) ;
#4554=ADVANCED_FACE ( 'NONE', ( #7188 ), #3504, .T. ) ;
#4556=CIRCLE ( 'NONE', #13096, 0.9499999999999992895 ) ;
#4558=CARTESIAN_POINT ( 'NONE',  ( 3.933597127675186211, 1.764057874260432701, -0.7948317876848067787 ) ) ;
#4559=VERTEX_POINT ( 'NONE', #6478 ) ;
#4569=CARTESIAN_POINT ( 'NONE',  ( 3.154159632798697377, 2.491856171652469421, 0.2021108258708759486 ) ) ;
#4574=DIRECTION ( 'NONE',  ( -1.000000000000000000, -0.000000000000000000, -0.000000000000000000 ) ) ;
#4575=CARTESIAN_POINT ( 'NONE',  ( 4.564206621729743674, 1.716523463454355358, -0.4148897219068747311 ) ) ;
#4577=VERTEX_POINT ( 'NONE', #7475 ) ;
#4581=ORIENTED_EDGE ( 'NONE', *, *, #12163, .F. ) ;
#4585=DIRECTION ( 'NONE',  ( 1.000000000000000000, 0.000000000000000000, 0.000000000000000000 ) ) ;
#4586=ORIENTED_EDGE ( 'NONE', *, *, #12770, .T. ) ;
#4590=EDGE_CURVE ( 'NONE', #1534, #9323, #12860, .T. ) ;
#4595=DIRECTION ( 'NONE',  ( 0.000000000000000000, 0.000000000000000000, 1.000000000000000000 ) ) ;
#4596=CARTESIAN_POINT ( 'NONE',  ( 3.874999999999999556, 3.137999999999999901, 1.542000000000000037 ) ) ;
#4600=DIRECTION ( 'NONE',  ( 0.000000000000000000, 0.000000000000000000, 1.000000000000000000 ) ) ;
#4602=ORIENTED_EDGE ( 'NONE', *, *, #8488, .F. ) ;
#4606=AXIS2_PLACEMENT_3D ( 'NONE', #10763, #317, #2793 ) ;
#4607=CARTESIAN_POINT ( 'NONE',  ( 3.875000000000000000, 3.137999999999999901, 0.000000000000000000 ) ) ;
#4610=EDGE_CURVE ( 'NONE', #12651, #8027, #14348, .T. ) ;
#4612=DIRECTION ( 'NONE',  ( 0.000000000000000000, 1.000000000000000000, 0.000000000000000000 ) ) ;
#4616=CIRCLE ( 'NONE', #917, 1.502725933896874810 ) ;
#4618=AXIS2_PLACEMENT_3D ( 'NONE', #10579, #7155, #11880 ) ;
#4621=ORIENTED_EDGE ( 'NONE', *, *, #3817, .F. ) ;
#4631=AXIS2_PLACEMENT_3D ( 'NONE', #13033, #4799, #252 ) ;
#4632=CARTESIAN_POINT ( 'NONE',  ( 4.203919238849069373, 1.786011173657954476, -0.6749003061560150396 ) ) ;
#4640=ORIENTED_EDGE ( 'NONE', *, *, #12110, .F. ) ;
#4642=CARTESIAN_POINT ( 'NONE',  ( 4.315797241329101475, 3.137999999999999901, 1.570821732971949825 ) ) ;
#4645=ORIENTED_EDGE ( 'NONE', *, *, #6743, .F. ) ;
#4646=CARTESIAN_POINT ( 'NONE',  ( 3.150340687203102341, 2.492967108137689181, 0.1879335863375432569 ) ) ;
#4647=EDGE_CURVE ( 'NONE', #6033, #12028, #5330, .T. ) ;
#4652=CARTESIAN_POINT ( 'NONE',  ( 4.574338115621504386, 1.717610331383472744, -0.3985571411410331333 ) ) ;
#4658=ORIENTED_EDGE ( 'NONE', *, *, #10181, .T. ) ;
#4659=ORIENTED_EDGE ( 'NONE', *, *, #4030, .T. ) ;
#4662=FACE_OUTER_BOUND ( 'NONE', #9856, .T. ) ;
#4667=EDGE_CURVE ( 'NONE', #14527, #4100, #8622, .T. ) ;
#4671=STYLED_ITEM('',(#15171),#5584);
#4676=CARTESIAN_POINT ( 'NONE',  ( 4.449790221757562669, 1.708297502301393544, 0.5563949201538650469 ) ) ;
#4679=DIRECTION ( 'NONE',  ( 0.000000000000000000, 0.000000000000000000, -1.000000000000000000 ) ) ;
#4685=LINE ( 'NONE', #9431, #2027 ) ;
#4689=LINE ( 'NONE', #8217, #7940 ) ;
#4696=DIRECTION ( 'NONE',  ( -1.000000000000000000, 0.000000000000000000, 0.000000000000000000 ) ) ;
#4698=CARTESIAN_POINT ( 'NONE',  ( 6.176491571325181340, 0.000000000000000000, 0.000000000000000000 ) ) ;
#4699=ORIENTED_EDGE ( 'NONE', *, *, #13488, .F. ) ;
#4703=DIRECTION ( 'NONE',  ( 0.000000000000000000, 1.000000000000000000, -1.224646799147353207E-16 ) ) ;
#4705=DIRECTION ( 'NONE',  ( 1.000000000000000000, 0.000000000000000000, 0.000000000000000000 ) ) ;
#4706=APPLICATION_CONTEXT ( 'automotive_design' ) ;
#4709=ORIENTED_EDGE ( 'NONE', *, *, #7315, .F. ) ;
#4719=VERTEX_POINT ( 'NONE', #10151 ) ;
#4721=VECTOR ( 'NONE', #4079, 39.37007874015748854 ) ;
#4723=CARTESIAN_POINT ( 'NONE',  ( 2.774999999999999911, 2.360000000000015863, 0.9799999999999454703 ) ) ;
#4726=CARTESIAN_POINT ( 'NONE',  ( 4.551166761458199872, 1.796655256677337942, -0.3282260880885092269 ) ) ;
#4727=VERTEX_POINT ( 'NONE', #5641 ) ;
#4729=ORIENTED_EDGE ( 'NONE', *, *, #2872, .T. ) ;
#4736=ORIENTED_EDGE ( 'NONE', *, *, #7036, .T. ) ;
#4742=CARTESIAN_POINT ( 'NONE',  ( 3.426491571325181340, 0.7000000000000026201, 2.400000000000000355 ) ) ;
#4745=AXIS2_PLACEMENT_3D ( 'NONE', #1816, #2914, #12306 ) ;
#4757=LINE ( 'NONE', #7212, #911 ) ;
#4759=VERTEX_POINT ( 'NONE', #7852 ) ;
#4762=VECTOR ( 'NONE', #13434, 39.37007874015748143 ) ;
#4763=DIRECTION ( 'NONE',  ( 0.000000000000000000, -1.000000000000000000, 0.000000000000000000 ) ) ;
#4768=CARTESIAN_POINT ( 'NONE',  ( 3.875000000000000000, 1.059999999999999165, 0.5000000000000002220 ) ) ;
#4772=DIRECTION ( 'NONE',  ( 0.000000000000000000, 0.000000000000000000, -1.000000000000000000 ) ) ;
#4773=ORIENTED_EDGE ( 'NONE', *, *, #14539, .T. ) ;
#4774=CIRCLE ( 'NONE', #7228, 1.000000000000000222 ) ;
#4775=AXIS2_PLACEMENT_3D ( 'NONE', #8849, #2808, #12136 ) ;
#4776=DIRECTION ( 'NONE',  ( 0.000000000000000000, 0.000000000000000000, -1.000000000000000000 ) ) ;
#4777=VERTEX_POINT ( 'NONE', #714 ) ;
#4781=AXIS2_PLACEMENT_3D ( 'NONE', #9633, #14279, #5894 ) ;
#4782=CARTESIAN_POINT ( 'NONE',  ( 6.176491571325181340, 0.000000000000000000, -2.960629921259842146 ) ) ;
#4783=AXIS2_PLACEMENT_3D ( 'NONE', #13855, #4703, #7004 ) ;
#4792=CARTESIAN_POINT ( 'NONE',  ( 3.426491571325181340, 2.426945040795776443, 0.5999481385559803925 ) ) ;
#4796=DIRECTION ( 'NONE',  ( 0.000000000000000000, 0.000000000000000000, 1.000000000000000000 ) ) ;
#4799=DIRECTION ( 'NONE',  ( -0.000000000000000000, -1.000000000000000000, 0.000000000000000000 ) ) ;
#4801=CARTESIAN_POINT ( 'NONE',  ( 2.774999999999999911, -1.679378605318059048, -1.973878605318027724 ) ) ;
#4802=ADVANCED_FACE ( 'NONE', ( #6868 ), #8259, .F. ) ;
#4803=EDGE_CURVE ( 'NONE', #14441, #391, #13653, .T. ) ;
#4807=CARTESIAN_POINT ( 'NONE',  ( 4.575011402338617472, 1.741756125272902356, -0.2756533241654208211 ) ) ;
#4811=EDGE_LOOP ( 'NONE', ( #13968, #8586 ) ) ;
#4813=ORIENTED_EDGE ( 'NONE', *, *, #13986, .T. ) ;
#4814=DIRECTION ( 'NONE',  ( 0.000000000000000000, 0.000000000000000000, -1.000000000000000000 ) ) ;
#4815=CIRCLE ( 'NONE', #2362, 0.2625000000000000111 ) ;
#4822=CARTESIAN_POINT ( 'NONE',  ( 3.618221289802627805, 1.960281491129935993, 0.7043865181403778930 ) ) ;
#4824=EDGE_CURVE ( 'NONE', #13527, #14941, #8980, .T. ) ;
#4829=FACE_OUTER_BOUND ( 'NONE', #5498, .T. ) ;
#4830=EDGE_LOOP ( 'NONE', ( #11238, #12878, #8220, #5973 ) ) ;
#4833=VERTEX_POINT ( 'NONE', #1868 ) ;
#4835=AXIS2_PLACEMENT_3D ( 'NONE', #13899, #14831, #11544 ) ;
#4849=DIRECTION ( 'NONE',  ( 0.000000000000000000, -1.000000000000000000, 0.000000000000000000 ) ) ;
#4854=CARTESIAN_POINT ( 'NONE',  ( 3.426491571325181340, -3.360000000000000320, 0.9799999999999999822 ) ) ;
#4856=AXIS2_PLACEMENT_3D ( 'NONE', #5011, #5861, #12875 ) ;
#4858=ORIENTED_EDGE ( 'NONE', *, *, #4803, .F. ) ;
#4860=LINE ( 'NONE', #1008, #10892 ) ;
#4862=EDGE_CURVE ( 'NONE', #11468, #4070, #12731, .T. ) ;
#4866=CONICAL_SURFACE ( 'NONE', #3874, 0.2624999999999997335, 0.7853981633974419507 ) ;
#4871=VECTOR ( 'NONE', #4907, 39.37007874015748143 ) ;
#4876=FACE_OUTER_BOUND ( 'NONE', #5181, .T. ) ;
#4880=ORIENTED_EDGE ( 'NONE', *, *, #12348, .F. ) ;
#4882=CARTESIAN_POINT ( 'NONE',  ( 3.716581572976743075, 1.921374764163736426, -0.4747933410505347229 ) ) ;
#4886=CARTESIAN_POINT ( 'NONE',  ( 5.567023771132172172, 1.934941942652818220E-16, -1.580000000000000071 ) ) ;
#4889=CARTESIAN_POINT ( 'NONE',  ( 4.466174989829828412, 1.785706766368954757, -0.4649126563571552295 ) ) ;
#4892=ORIENTED_EDGE ( 'NONE', *, *, #12869, .T. ) ;
#4893=VERTEX_POINT ( 'NONE', #13871 ) ;
#4896=EDGE_CURVE ( 'NONE', #4559, #4577, #5787, .T. ) ;
#4897=DIRECTION ( 'NONE',  ( -0.000000000000000000, -1.000000000000000000, -0.000000000000000000 ) ) ;
#4899=DIRECTION ( 'NONE',  ( 0.000000000000000000, 1.000000000000000000, -0.000000000000000000 ) ) ;
#4900=ORIENTED_EDGE ( 'NONE', *, *, #1769, .F. ) ;
#4902=DIRECTION ( 'NONE',  ( 0.7071067811865429098, 8.659560562354987092E-17, 0.7071067811865521247 ) ) ;
#4903=AXIS2_PLACEMENT_3D ( 'NONE', #12251, #5297, #12182 ) ;
#4904=CARTESIAN_POINT ( 'NONE',  ( 3.562689364900068156, 1.987812937981572770, 0.6814576478706133589 ) ) ;
#4906=DIRECTION ( 'NONE',  ( 1.000000000000000000, 0.000000000000000000, 0.000000000000000000 ) ) ;
#4907=DIRECTION ( 'NONE',  ( -1.000000000000000000, -0.000000000000000000, -0.000000000000000000 ) ) ;
#4908=CARTESIAN_POINT ( 'NONE',  ( 4.618921047797687862, 1.723044742589275646, -0.3137129605234482699 ) ) ;
#4912=EDGE_LOOP ( 'NONE', ( #12617, #8905 ) ) ;
#4913=VERTEX_POINT ( 'NONE', #9466 ) ;
#4915=ADVANCED_FACE ( 'NONE', ( #14110 ), #10527, .F. ) ;
#4920=CARTESIAN_POINT ( 'NONE',  ( 6.176491571325181340, -1.679378605318048390, 1.679378605318054163 ) ) ;
#4921=LINE ( 'NONE', #8514, #12666 ) ;
#4925=DIRECTION ( 'NONE',  ( -0.000000000000000000, 1.836536466328828134E-14, 1.000000000000000000 ) ) ;
#4929=CONICAL_SURFACE ( 'NONE', #12235, 0.2944999999999987073, 0.7853981633974366217 ) ;
#4930=CARTESIAN_POINT ( 'NONE',  ( 3.875000000000000000, 3.085321731235734610, -0.5849999999999996314 ) ) ;
#4931=VERTEX_POINT ( 'NONE', #12806 ) ;
#4938=CONICAL_SURFACE ( 'NONE', #8100, 0.3750000000000004996, 0.7853981633974547183 ) ;
#4939=DIRECTION ( 'NONE',  ( 0.000000000000000000, 0.000000000000000000, 1.000000000000000000 ) ) ;
#4940=CARTESIAN_POINT ( 'NONE',  ( 3.875000000000000000, 1.059999999999999165, 0.5000000000000002220 ) ) ;
#4941=ORIENTED_EDGE ( 'NONE', *, *, #5816, .T. ) ;
#4945=ADVANCED_FACE ( 'NONE', ( #9389 ), #14028, .F. ) ;
#4954=CARTESIAN_POINT ( 'NONE',  ( 3.473767154576092864, 1.977251034363303628, -0.3019842868889652809 ) ) ;
#4955=EDGE_CURVE ( 'NONE', #628, #8247, #6902, .T. ) ;
#4958=ADVANCED_FACE ( 'NONE', ( #4876 ), #10681, .F. ) ;
#4959=DIRECTION ( 'NONE',  ( -1.000000000000000000, -0.000000000000000000, -0.000000000000000000 ) ) ;
#4965=VERTEX_POINT ( 'NONE', #13952 ) ;
#4966=VECTOR ( 'NONE', #8142, 39.37007874015748143 ) ;
#4968=CYLINDRICAL_SURFACE ( 'NONE', #4781, 1.000000000000000222 ) ;
#4969=ORIENTED_EDGE ( 'NONE', *, *, #4955, .T. ) ;
#4972=EDGE_CURVE ( 'NONE', #9226, #5697, #9232, .T. ) ;
#4974=EDGE_CURVE ( 'NONE', #5730, #9564, #13950, .T. ) ;
#4975=FACE_OUTER_BOUND ( 'NONE', #7150, .T. ) ;
#4978=CARTESIAN_POINT ( 'NONE',  ( 3.659655290762535262, 1.940877740142120222, 0.7181426529861060226 ) ) ;
#4979=DIRECTION ( 'NONE',  ( 0.000000000000000000, 0.000000000000000000, -1.000000000000000000 ) ) ;
#4982=DIRECTION ( 'NONE',  ( -1.000000000000000000, -0.000000000000000000, -0.000000000000000000 ) ) ;
#4985=ORIENTED_EDGE ( 'NONE', *, *, #8353, .F. ) ;
#4986=AXIS2_PLACEMENT_3D ( 'NONE', #9600, #455, #10811 ) ;
#4991=FACE_OUTER_BOUND ( 'NONE', #6471, .T. ) ;
#4993=AXIS2_PLACEMENT_3D ( 'NONE', #13205, #11998, #1507 ) ;
#4998=DIRECTION ( 'NONE',  ( 0.000000000000000000, 0.000000000000000000, -1.000000000000000000 ) ) ;
#5001=CARTESIAN_POINT ( 'NONE',  ( 2.806999999999999940, -1.679378605318059048, -1.679378605318041950 ) ) ;
#5002=VERTEX_POINT ( 'NONE', #5094 ) ;
#5005=EDGE_LOOP ( 'NONE', ( #8660, #3629, #6515, #3916 ) ) ;
#5011=CARTESIAN_POINT ( 'NONE',  ( 2.774999999999999911, 0.000000000000000000, 0.000000000000000000 ) ) ;
#5015=EDGE_CURVE ( 'NONE', #7227, #7182, #13408, .T. ) ;
#5020=DIRECTION ( 'NONE',  ( -1.000000000000000000, -0.000000000000000000, -0.000000000000000000 ) ) ;
#5024=CARTESIAN_POINT ( 'NONE',  ( 3.875000000000000000, 3.137999999999999901, 0.000000000000000000 ) ) ;
#5028=EDGE_CURVE ( 'NONE', #1342, #5706, #10308, .T. ) ;
#5032=VERTEX_POINT ( 'NONE', #11978 ) ;
#5035=CONICAL_SURFACE ( 'NONE', #597, 0.4070000000000022489, 0.7853981633974547183 ) ;
#5040=CARTESIAN_POINT ( 'NONE',  ( 4.167248288244303822, 0.9139185452513080010, 0.4060177403750064307 ) ) ;
#5042=CARTESIAN_POINT ( 'NONE',  ( 3.426491571325181340, 1.575000000000016387, 2.359999999999999876 ) ) ;
#5045=DIRECTION ( 'NONE',  ( -1.000000000000000000, -0.000000000000000000, -0.000000000000000000 ) ) ;
#5046=AXIS2_PLACEMENT_3D ( 'NONE', #14152, #12996, #9426 ) ;
#5047=DIRECTION ( 'NONE',  ( 0.000000000000000000, 0.000000000000000000, 1.000000000000000000 ) ) ;
#5048=AXIS2_PLACEMENT_3D ( 'NONE', #13058, #12147, #10628 ) ;
#5050=CARTESIAN_POINT ( 'NONE',  ( 3.874999999999999556, 3.137999999999999901, -1.320000000000000062 ) ) ;
#5052=CARTESIAN_POINT ( 'NONE',  ( 3.740430787191658446, 1.905565248334865736, 0.7383113636965974447 ) ) ;
#5057=CARTESIAN_POINT ( 'NONE',  ( 3.426491571325181340, 1.575000000000016609, 1.575000000000000178 ) ) ;
#5060=ADVANCED_FACE ( 'NONE', ( #7605 ), #270, .T. ) ;
#5062=CARTESIAN_POINT ( 'NONE',  ( 0.000000000000000000, 0.000000000000000000, 0.000000000000000000 ) ) ;
#5064=ORIENTED_EDGE ( 'NONE', *, *, #2502, .F. ) ;
#5065=CYLINDRICAL_SURFACE ( 'NONE', #1421, 1.000000000000000000 ) ;
#5069=CARTESIAN_POINT ( 'NONE',  ( 3.426491571325181340, 2.449513323269931135E-16, -2.000179419058113695 ) ) ;
#5072=VECTOR ( 'NONE', #13124, 39.37007874015748143 ) ;
#5076=DIRECTION ( 'NONE',  ( -0.000000000000000000, -1.000000000000000000, -0.000000000000000000 ) ) ;
#5081=EDGE_CURVE ( 'NONE', #7714, #14724, #10798, .T. ) ;
#5083=AXIS2_PLACEMENT_3D ( 'NONE', #9704, #9776, #1795 ) ;
#5086=DIRECTION ( 'NONE',  ( -1.000000000000000000, -0.000000000000000000, -0.000000000000000000 ) ) ;
#5094=CARTESIAN_POINT ( 'NONE',  ( 2.774999999999999911, 1.679378605318042395, -1.973878605318059698 ) ) ;
#5096=CIRCLE ( 'NONE', #11188, 0.4070000000000022489 ) ;
#5097=CARTESIAN_POINT ( 'NONE',  ( 3.426491571325181340, 1.986447008166981387, -0.6339330177794473276 ) ) ;
#5098=CARTESIAN_POINT ( 'NONE',  ( 2.807000000000000384, 1.679378605318059048, 1.941878605318041462 ) ) ;
#5101=( NAMED_UNIT ( * ) SI_UNIT ( $, .STERADIAN. ) SOLID_ANGLE_UNIT ( ) );
#5102=FACE_OUTER_BOUND ( 'NONE', #4830, .T. ) ;
#5108=AXIS2_PLACEMENT_3D ( 'NONE', #11849, #11921, #13130 ) ;
#5114=CARTESIAN_POINT ( 'NONE',  ( 3.875000000000000000, 0.8660254037844384856, 0.5000000000000002220 ) ) ;
#5116=DIRECTION ( 'NONE',  ( -1.000000000000000000, -0.000000000000000000, -0.000000000000000000 ) ) ;
#5117=ORIENTED_EDGE ( 'NONE', *, *, #3639, .F. ) ;
#5123=AXIS2_PLACEMENT_3D ( 'NONE', #14948, #10063, #11347 ) ;
#5125=CARTESIAN_POINT ( 'NONE',  ( 3.875000000000000000, 1.059999999999999165, -0.5000000000000002220 ) ) ;
#5127=CARTESIAN_POINT ( 'NONE',  ( 3.841433886848298673, 1.867524044941962558, 0.7493717214423840645 ) ) ;
#5128=CYLINDRICAL_SURFACE ( 'NONE', #3532, 0.2624999999999997335 ) ;
#5129=ORIENTED_EDGE ( 'NONE', *, *, #14819, .F. ) ;
#5132=EDGE_LOOP ( 'NONE', ( #9411, #6962, #5593, #5426 ) ) ;
#5137=CARTESIAN_POINT ( 'NONE',  ( 2.806999999999999496, -1.679378605318041950, 1.679378605318059048 ) ) ;
#5145=AXIS2_PLACEMENT_3D ( 'NONE', #15143, #755, #11260 ) ;
#5154=CARTESIAN_POINT ( 'NONE',  ( 6.096491571325181269, 0.000000000000000000, 0.000000000000000000 ) ) ;
#5157=CARTESIAN_POINT ( 'NONE',  ( 3.875000000000000000, 0.7099999999999984102, 0.000000000000000000 ) ) ;
#5159=AXIS2_PLACEMENT_3D ( 'NONE', #6023, #10686, #5383 ) ;
#5164=ORIENTED_EDGE ( 'NONE', *, *, #42, .F. ) ;
#5168=CARTESIAN_POINT ( 'NONE',  ( 6.826491571325181695, -1.679378605318048390, 1.679378605318054163 ) ) ;
#5169=CARTESIAN_POINT ( 'NONE',  ( 6.794491571325179891, -1.679378605318048390, 1.679378605318054163 ) ) ;
#5170=CARTESIAN_POINT ( 'NONE',  ( 4.512545870194937692, 1.791067049260529176, -0.3982799620645194882 ) ) ;
#5174=ORIENTED_EDGE ( 'NONE', *, *, #6805, .T. ) ;
#5181=EDGE_LOOP ( 'NONE', ( #7139, #3726, #3643, #7730 ) ) ;
#5182=CARTESIAN_POINT ( 'NONE',  ( 6.794491571325179891, -1.679378605318048390, 1.679378605318054163 ) ) ;
#5188=CARTESIAN_POINT ( 'NONE',  ( 2.774999999999999911, -1.679378605318041950, 1.679378605318059048 ) ) ;
#5190=CARTESIAN_POINT ( 'NONE',  ( 3.495307681290304114, 1.921430432632648122, 0.7213508312486736074 ) ) ;
#5191=CARTESIAN_POINT ( 'NONE',  ( 3.426491571325181340, 1.679378605318042395, -1.679378605318058604 ) ) ;
#5192=EDGE_LOOP ( 'NONE', ( #1141, #8180, #8712, #6731, #6701, #8674, #11970, #13493, #804, #6143, #14292, #6428, #9964, #8846, #14448, #10595, #6375, #7040, #11911, #2882, #8870, #1536, #13419, #12676, #1400, #11115, #2480, #4586, #13483, #8867, #10767, #263, #835, #6978, #45, #13703, #7742 ) ) ;
#5194=CARTESIAN_POINT ( 'NONE',  ( 3.426491571325181340, 1.986429008462982093, 0.6339643213050358828 ) ) ;
#5197=ORIENTED_EDGE ( 'NONE', *, *, #12405, .T. ) ;
#5204=LINE ( 'NONE', #2984, #6455 ) ;
#5209=DIRECTION ( 'NONE',  ( -0.7071067811865429098, 8.659560562354987092E-17, -0.7071067811865521247 ) ) ;
#5217=ADVANCED_FACE ( 'NONE', ( #3229 ), #9817, .F. ) ;
#5221=CIRCLE ( 'NONE', #69, 2.960629921259842146 ) ;
#5225=DIRECTION ( 'NONE',  ( 0.000000000000000000, 1.000000000000000000, -4.591341165821855765E-15 ) ) ;
#5226=FACE_OUTER_BOUND ( 'NONE', #12784, .T. ) ;
#5234=ORIENTED_EDGE ( 'NONE', *, *, #11852, .T. ) ;
#5236=EDGE_CURVE ( 'NONE', #14399, #1593, #7893, .T. ) ;
#5238=DIRECTION ( 'NONE',  ( 0.000000000000000000, 0.000000000000000000, 1.000000000000000000 ) ) ;
#5251=DIRECTION ( 'NONE',  ( 0.000000000000000000, 0.000000000000000000, 1.000000000000000000 ) ) ;
#5260=AXIS2_PLACEMENT_3D ( 'NONE', #12381, #6364, #8648 ) ;
#5263=CARTESIAN_POINT ( 'NONE',  ( 4.426064865072103949, 1.707355206796218328, 0.5795993612514793725 ) ) ;
#5265=ORIENTED_EDGE ( 'NONE', *, *, #11253, .T. ) ;
#5272=AXIS2_PLACEMENT_3D ( 'NONE', #10957, #5076, #6517 ) ;
#5274=ORIENTED_EDGE ( 'NONE', *, *, #2065, .T. ) ;
#5283=DIRECTION ( 'NONE',  ( -1.000000000000000000, -0.000000000000000000, -0.000000000000000000 ) ) ;
#5288=CARTESIAN_POINT ( 'NONE',  ( 4.126800735551335642, 0.9017823133670000990, -0.4322768681130992330 ) ) ;
#5295=AXIS2_PLACEMENT_3D ( 'NONE', #1588, #11007, #353 ) ;
#5296=ADVANCED_FACE ( 'NONE', ( #14894 ), #1506, .F. ) ;
#5297=DIRECTION ( 'NONE',  ( 1.000000000000000000, 0.000000000000000000, 0.000000000000000000 ) ) ;
#5300=CARTESIAN_POINT ( 'NONE',  ( 3.426491571325181340, 0.000000000000000000, 0.0001794190581142465670 ) ) ;
#5303=DIRECTION ( 'NONE',  ( 0.000000000000000000, 1.000000000000000000, -1.836536466328828134E-14 ) ) ;
#5304=LINE ( 'NONE', #6307, #3247 ) ;
#5306=CIRCLE ( 'NONE', #13839, 0.1899999999999996136 ) ;
#5307=FACE_OUTER_BOUND ( 'NONE', #13261, .T. ) ;
#5313=CARTESIAN_POINT ( 'NONE',  ( 3.426491571325181340, 1.679378605318059048, 1.679378605318041506 ) ) ;
#5314=EDGE_CURVE ( 'NONE', #12204, #694, #1234, .T. ) ;
#5318=CARTESIAN_POINT ( 'NONE',  ( 3.426491571325181784, 2.005325245437683090, -0.6184897574297448797 ) ) ;
#5319=CARTESIAN_POINT ( 'NONE',  ( 4.369102373712536291, 1.779600098398884445, -0.5677944546462855291 ) ) ;
#5320=AXIS2_PLACEMENT_3D ( 'NONE', #13539, #14775, #5457 ) ;
#5321=ORIENTED_EDGE ( 'NONE', *, *, #13841, .F. ) ;
#5324=ORIENTED_EDGE ( 'NONE', *, *, #5733, .T. ) ;
#5325=EDGE_LOOP ( 'NONE', ( #4522, #12131, #8476, #1125 ) ) ;
#5326=EDGE_CURVE ( 'NONE', #13304, #1703, #2191, .T. ) ;
#5328=CIRCLE ( 'NONE', #8759, 2.500000000000000000 ) ;
#5330=LINE ( 'NONE', #11990, #5072 ) ;
#5331=CARTESIAN_POINT ( 'NONE',  ( 4.180185220126820589, 0.9181503761820097864, 0.3963891770617307686 ) ) ;
#5338=DIRECTION ( 'NONE',  ( 1.000000000000000000, 0.000000000000000000, 0.000000000000000000 ) ) ;
#5339=CARTESIAN_POINT ( 'NONE',  ( 3.426491571325181340, -1.575000000000027489, -2.359999999999989218 ) ) ;
#5341=VECTOR ( 'NONE', #12463, 39.37007874015748143 ) ;
#5344=VECTOR ( 'NONE', #12361, 39.37007874015748143 ) ;
#5345=DIRECTION ( 'NONE',  ( -1.000000000000000000, -0.000000000000000000, -0.000000000000000000 ) ) ;
#5346=CARTESIAN_POINT ( 'NONE',  ( 4.215778309529500056, 1.784571035030107167, 0.6698587355277484390 ) ) ;
#5347=DIRECTION ( 'NONE',  ( -0.7071067811865429098, 8.659560562354987092E-17, -0.7071067811865521247 ) ) ;
#5348=ORIENTED_EDGE ( 'NONE', *, *, #9449, .F. ) ;
#5356=VECTOR ( 'NONE', #13063, 39.37007874015748854 ) ;
#5359=ORIENTED_EDGE ( 'NONE', *, *, #4492, .T. ) ;
#5361=FACE_OUTER_BOUND ( 'NONE', #11272, .T. ) ;
#5363=AXIS2_PLACEMENT_3D ( 'NONE', #13255, #14648, #11205 ) ;
#5365=CONICAL_SURFACE ( 'NONE', #9021, 1.000000000000000000, 0.7853981633974517207 ) ;
#5366=DIRECTION ( 'NONE',  ( 0.000000000000000000, 1.000000000000000000, -8.723548215061523903E-15 ) ) ;
#5370=AXIS2_PLACEMENT_3D ( 'NONE', #4607, #15001, #3301 ) ;
#5376=CARTESIAN_POINT ( 'NONE',  ( 3.875000000000000000, 0.8660254037844385966, -0.5000000000000002220 ) ) ;
#5382=AXIS2_PLACEMENT_3D ( 'NONE', #2929, #11031, #13236 ) ;
#5383=DIRECTION ( 'NONE',  ( 0.000000000000000000, 0.000000000000000000, 1.000000000000000000 ) ) ;
#5384=DIRECTION ( 'NONE',  ( 0.000000000000000000, 0.000000000000000000, -1.000000000000000000 ) ) ;
#5387=DIRECTION ( 'NONE',  ( -1.000000000000000000, -0.000000000000000000, -0.000000000000000000 ) ) ;
#5388=DIRECTION ( 'NONE',  ( 0.000000000000000000, 0.000000000000000000, 1.000000000000000000 ) ) ;
#5390=CARTESIAN_POINT ( 'NONE',  ( 3.426491571325181340, -1.575000000000027489, -1.574999999999989297 ) ) ;
#5392=ORIENTED_EDGE ( 'NONE', *, *, #4420, .T. ) ;
#5398=CARTESIAN_POINT ( 'NONE',  ( 4.548534283101781206, 1.796214626747565601, 0.3340040616788196304 ) ) ;
#5401=EDGE_CURVE ( 'NONE', #8878, #13854, #10535, .T. ) ;
#5402=EDGE_CURVE ( 'NONE', #1776, #9581, #10457, .T. ) ;
#5403=ORIENTED_EDGE ( 'NONE', *, *, #9625, .T. ) ;
#5404=ORIENTED_EDGE ( 'NONE', *, *, #52, .F. ) ;
#5408=CARTESIAN_POINT ( 'NONE',  ( 3.875000000000000000, 3.137999999999999901, 0.000000000000000000 ) ) ;
#5411=EDGE_CURVE ( 'NONE', #10222, #2606, #12967, .T. ) ;
#5419=AXIS2_PLACEMENT_3D ( 'NONE', #4642, #15038, #9311 ) ;
#5423=CARTESIAN_POINT ( 'NONE',  ( 4.316286828030351685, 1.708216954940201759, 0.6629077590058020109 ) ) ;
#5426=ORIENTED_EDGE ( 'NONE', *, *, #15086, .F. ) ;
#5436=EDGE_CURVE ( 'NONE', #5706, #1342, #12714, .T. ) ;
#5443=CARTESIAN_POINT ( 'NONE',  ( 3.696710981162860676, 0.8840651821477499839, -0.4674177165474920903 ) ) ;
#5444=CARTESIAN_POINT ( 'NONE',  ( 4.449168964073242805, 1.708272156618657833, -0.5570130099483981967 ) ) ;
#5446=DIRECTION ( 'NONE',  ( 0.000000000000000000, -1.000000000000000000, 0.000000000000000000 ) ) ;
#5447=DIRECTION ( 'NONE',  ( 1.000000000000000000, 0.000000000000000000, 0.000000000000000000 ) ) ;
#5449=VERTEX_POINT ( 'NONE', #1188 ) ;
#5451=CARTESIAN_POINT ( 'NONE',  ( 6.826491571325181695, 1.679378605318035733, -1.679378605318065487 ) ) ;
#5455=LINE ( 'NONE', #2209, #4403 ) ;
#5457=DIRECTION ( 'NONE',  ( 0.000000000000000000, 0.000000000000000000, 1.000000000000000000 ) ) ;
#5459=ORIENTED_EDGE ( 'NONE', *, *, #14409, .F. ) ;
#5462=CYLINDRICAL_SURFACE ( 'NONE', #12342, 2.500000000000000444 ) ;
#5466=EDGE_LOOP ( 'NONE', ( #1236, #5989, #8230, #699 ) ) ;
#5468=AXIS2_PLACEMENT_3D ( 'NONE', #14173, #10664, #10 ) ;
#5470=CIRCLE ( 'NONE', #8647, 0.9499999999999992895 ) ;
#5477=ORIENTED_EDGE ( 'NONE', *, *, #3166, .F. ) ;
#5478=ORIENTED_EDGE ( 'NONE', *, *, #9536, .T. ) ;
#5479=VERTEX_POINT ( 'NONE', #4801 ) ;
#5485=VECTOR ( 'NONE', #8498, 39.37007874015748143 ) ;
#5489=DIRECTION ( 'NONE',  ( 1.000000000000000000, 0.000000000000000000, 0.000000000000000000 ) ) ;
#5490=EDGE_CURVE ( 'NONE', #7156, #7967, #6382, .T. ) ;
#5494=AXIS2_PLACEMENT_3D ( 'NONE', #5137, #13290, #12379 ) ;
#5495=CARTESIAN_POINT ( 'NONE',  ( 4.350709184091345882, 1.779665969747238785, 0.5813850623748166857 ) ) ;
#5498=EDGE_LOOP ( 'NONE', ( #3320, #4900, #5477, #10312 ) ) ;
#5499=CIRCLE ( 'NONE', #13546, 0.4849999999999995981 ) ;
#5506=VERTEX_POINT ( 'NONE', #14117 ) ;
#5507=DIRECTION ( 'NONE',  ( 0.7071067811865429098, 8.659560562354987092E-17, 0.7071067811865521247 ) ) ;
#5508=PLANE ( 'NONE',  #11455 ) ;
#5511=CIRCLE ( 'NONE', #11362, 2.500000000000000000 ) ;
#5512=CARTESIAN_POINT ( 'NONE',  ( 2.980731298636167370, 3.137999999999999901, 0.3249191361593797844 ) ) ;
#5514=EDGE_LOOP ( 'NONE', ( #11533, #10066 ) ) ;
#5516=CARTESIAN_POINT ( 'NONE',  ( 3.436969365618575800, 1.985569024027678875, 0.2422625011488116487 ) ) ;
#5519=CIRCLE ( 'NONE', #10158, 1.000000000000000000 ) ;
#5520=DIRECTION ( 'NONE',  ( -1.000000000000000000, -0.000000000000000000, -0.000000000000000000 ) ) ;
#5521=DIRECTION ( 'NONE',  ( 0.000000000000000000, -1.000000000000000000, 1.423315761404775650E-14 ) ) ;
#5522=ORIENTED_EDGE ( 'NONE', *, *, #13879, .T. ) ;
#5525=EDGE_CURVE ( 'NONE', #13304, #4332, #8338, .T. ) ;
#5531=CARTESIAN_POINT ( 'NONE',  ( 3.426491571325181340, 0.9799999999999438050, -2.360000000000016307 ) ) ;
#5542=ADVANCED_FACE ( 'NONE', ( #1334 ), #14672, .F. ) ;
#5543=ADVANCED_FACE ( 'NONE', ( #10123 ), #5900, .F. ) ;
#5545=CARTESIAN_POINT ( 'NONE',  ( 3.426491571325181340, 2.197249752256450025E-20, -0.0001794190581142465670 ) ) ;
#5547=PLANE ( 'NONE',  #826 ) ;
#5551=CARTESIAN_POINT ( 'NONE',  ( 4.066623985734413971, 1.805393779619291594, -0.7271255666244380578 ) ) ;
#5554=ORIENTED_EDGE ( 'NONE', *, *, #14653, .F. ) ;
#5555=ORIENTED_EDGE ( 'NONE', *, *, #680, .T. ) ;
#5556=UNCERTAINTY_MEASURE_WITH_UNIT (LENGTH_MEASURE( 1.000000000000000082E-05 ), #1489, 'distance_accuracy_value', 'NONE');
#5558=VERTEX_POINT ( 'NONE', #4307 ) ;
#5561=DIRECTION ( 'NONE',  ( -0.000000000000000000, -1.000000000000000000, -0.000000000000000000 ) ) ;
#5564=CARTESIAN_POINT ( 'NONE',  ( 3.219323625916810538, 2.473723010511407860, 0.3624492852859261816 ) ) ;
#5565=DIRECTION ( 'NONE',  ( 0.000000000000000000, 0.000000000000000000, -1.000000000000000000 ) ) ;
#5567=AXIS2_PLACEMENT_3D ( 'NONE', #11140, #12065, #3034 ) ;
#5568=CYLINDRICAL_SURFACE ( 'NONE', #7850, 0.4849999999999995981 ) ;
#5570=CARTESIAN_POINT ( 'NONE',  ( 4.048339038639393372, 1.809465041664403362, 0.7309204628693353190 ) ) ;
#5571=ADVANCED_FACE ( 'NONE', ( #8978 ), #254, .T. ) ;
#5572=CARTESIAN_POINT ( 'NONE',  ( 3.651698974834499012, 1.959955860919708748, -0.4475141391230971766 ) ) ;
#5575=ORIENTED_EDGE ( 'NONE', *, *, #11976, .F. ) ;
#5583=ORIENTED_EDGE ( 'NONE', *, *, #14850, .F. ) ;
#5584=MANIFOLD_SOLID_BREP ( 'Fillet3', #2781 ) ;
#5586=CARTESIAN_POINT ( 'NONE',  ( 2.774999999999999911, 0.000000000000000000, 2.500000000000000444 ) ) ;
#5589=AXIS2_PLACEMENT_3D ( 'NONE', #7929, #12576, #3335 ) ;
#5593=ORIENTED_EDGE ( 'NONE', *, *, #6965, .T. ) ;
#5597=ADVANCED_FACE ( 'NONE', ( #13538 ), #4929, .F. ) ;
#5599=CARTESIAN_POINT ( 'NONE',  ( 3.784081183264448978, 1.807375528223629235, -0.7960544091624519591 ) ) ;
#5600=EDGE_CURVE ( 'NONE', #5506, #1362, #13448, .T. ) ;
#5601=CIRCLE ( 'NONE', #9518, 0.2625000000000000111 ) ;
#5604=ORIENTED_EDGE ( 'NONE', *, *, #13901, .F. ) ;
#5606=VECTOR ( 'NONE', #4902, 39.37007874015748143 ) ;
#5607=CARTESIAN_POINT ( 'NONE',  ( 3.426491571325181340, 0.000000000000000000, 2.000179419058113695 ) ) ;
#5609=CARTESIAN_POINT ( 'NONE',  ( 6.794491571325179891, 1.679378605318035733, -1.679378605318065487 ) ) ;
#5611=CARTESIAN_POINT ( 'NONE',  ( 6.826491571325181695, 0.000000000000000000, -1.039370078740158965 ) ) ;
#5617=CIRCLE ( 'NONE', #6346, 0.2624999999999997335 ) ;
#5619=DIRECTION ( 'NONE',  ( 0.000000000000000000, 0.000000000000000000, -1.000000000000000000 ) ) ;
#5626=DIRECTION ( 'NONE',  ( -0.9659258262890699775, 3.169619151431688520E-17, -0.2588190451025145222 ) ) ;
#5629=CIRCLE ( 'NONE', #10505, 0.4070000000000000839 ) ;
#5631=ADVANCED_FACE ( 'NONE', ( #10973 ), #4938, .F. ) ;
#5632=CARTESIAN_POINT ( 'NONE',  ( 6.826491571325181695, -1.679378605318047946, -2.054378605318054163 ) ) ;
#5635=CARTESIAN_POINT ( 'NONE',  ( 3.758446757606395572, 1.898527427273793533, -0.7408372069486923728 ) ) ;
#5638=DIRECTION ( 'NONE',  ( -1.000000000000000000, -0.000000000000000000, -0.000000000000000000 ) ) ;
#5639=ORIENTED_EDGE ( 'NONE', *, *, #12511, .T. ) ;
#5641=CARTESIAN_POINT ( 'NONE',  ( 3.875000000000000000, 3.085321731235734610, 0.4849999999999995981 ) ) ;
#5646=B_SPLINE_CURVE_WITH_KNOTS ( 'NONE', 3,
 ( #13919, #14157, #1293, #5980 ),
 .UNSPECIFIED., .F., .F.,
 ( 4, 4 ),
 ( 2.044667804973039983E-07, 0.001808351910784379481 ),
 .UNSPECIFIED. ) ;
#5651=AXIS2_PLACEMENT_3D ( 'NONE', #2678, #1583, #423 ) ;
#5655=CARTESIAN_POINT ( 'NONE',  ( 3.874999999999999556, 2.750000000000000000, -1.820000000000000284 ) ) ;
#5657=ORIENTED_EDGE ( 'NONE', *, *, #3528, .F. ) ;
#5663=DIRECTION ( 'NONE',  ( 0.9396926207859107594, 0.000000000000000000, -0.3420201433256624401 ) ) ;
#5664=AXIS2_PLACEMENT_3D ( 'NONE', #10513, #9, #12553 ) ;
#5668=DIRECTION ( 'NONE',  ( 0.000000000000000000, 0.000000000000000000, 1.000000000000000000 ) ) ;
#5669=DIRECTION ( 'NONE',  ( 0.000000000000000000, 0.000000000000000000, 1.000000000000000000 ) ) ;
#5670=CARTESIAN_POINT ( 'NONE',  ( 3.407667229351369009, 0.9840573826600637064, -0.1785091600307283921 ) ) ;
#5671=CARTESIAN_POINT ( 'NONE',  ( 3.716778723645624449, 1.830546595533379950, -0.7880236670140078337 ) ) ;
#5673=CARTESIAN_POINT ( 'NONE',  ( 6.176491571325181340, -1.679378605318048390, 2.086378605318056412 ) ) ;
#5674=DIRECTION ( 'NONE',  ( 1.000000000000000000, 0.000000000000000000, 0.000000000000000000 ) ) ;
#5684=DIRECTION ( 'NONE',  ( -1.000000000000000000, -0.000000000000000000, -0.000000000000000000 ) ) ;
#5685=EDGE_CURVE ( 'NONE', #327, #11008, #11764, .T. ) ;
#5689=CARTESIAN_POINT ( 'NONE',  ( 3.716337281397007253, 1.830387028050574738, 0.7888129363977544051 ) ) ;
#5690=VERTEX_POINT ( 'NONE', #11504 ) ;
#5694=CARTESIAN_POINT ( 'NONE',  ( 3.394491571325180423, -1.679378605318059048, -1.941878605318027251 ) ) ;
#5696=DIRECTION ( 'NONE',  ( 0.000000000000000000, 0.000000000000000000, 1.000000000000000000 ) ) ;
#5697=VERTEX_POINT ( 'NONE', #4544 ) ;
#5705=CARTESIAN_POINT ( 'NONE',  ( 3.894800534755237909, 1.849893891846735139, -0.7499754145434819330 ) ) ;
#5706=VERTEX_POINT ( 'NONE', #5694 ) ;
#5707=ORIENTED_EDGE ( 'NONE', *, *, #6878, .T. ) ;
#5712=CARTESIAN_POINT ( 'NONE',  ( 2.527624975756972425, 3.137999999999999901, 0.9199802545633498640 ) ) ;
#5716=ORIENTED_EDGE ( 'NONE', *, *, #14111, .F. ) ;
#5723=CARTESIAN_POINT ( 'NONE',  ( 4.605814143324980847, 1.746023016917476633, 0.1761007706937262884 ) ) ;
#5724=ORIENTED_EDGE ( 'NONE', *, *, #10119, .T. ) ;
#5725=DIRECTION ( 'NONE',  ( -1.000000000000000000, -0.000000000000000000, -0.000000000000000000 ) ) ;
#5727=EDGE_LOOP ( 'NONE', ( #1407, #5274, #11590, #1469 ) ) ;
#5728=AXIS2_PLACEMENT_3D ( 'NONE', #6194, #12073, #4979 ) ;
#5730=VERTEX_POINT ( 'NONE', #8074 ) ;
#5732=LINE ( 'NONE', #10397, #2368 ) ;
#5733=EDGE_CURVE ( 'NONE', #2357, #2874, #9077, .T. ) ;
#5737=CARTESIAN_POINT ( 'NONE',  ( 2.807000000000000828, 1.679378605318042395, -1.679378605318058604 ) ) ;
#5738=CARTESIAN_POINT ( 'NONE',  ( 4.315797241329101475, 3.137999999999999901, -1.570821732971949825 ) ) ;
#5742=CARTESIAN_POINT ( 'NONE',  ( 3.876560711617219379, 2.749999999999999556, 0.000000000000000000 ) ) ;
#5744=CARTESIAN_POINT ( 'NONE',  ( 3.426755384177574193, 0.9750879638133824745, 0.2239670995506589934 ) ) ;
#5745=CARTESIAN_POINT ( 'NONE',  ( 4.204541317192457051, 1.715952400129281630, 0.7235892913703009244 ) ) ;
#5746=DIRECTION ( 'NONE',  ( -1.000000000000000000, -0.000000000000000000, -0.000000000000000000 ) ) ;
#5748=EDGE_LOOP ( 'NONE', ( #15028, #2509, #296, #2532 ) ) ;
#5749=CONICAL_SURFACE ( 'NONE', #7692, 0.2219999999999999751, 0.7853981633974435050 ) ;
#5755=DIRECTION ( 'NONE',  ( -1.000000000000000000, -0.000000000000000000, -0.000000000000000000 ) ) ;
#5770=ADVANCED_FACE ( 'NONE', ( #9133 ), #2241, .F. ) ;
#5775=CIRCLE ( 'NONE', #6750, 1.000000000000000000 ) ;
#5776=EDGE_CURVE ( 'NONE', #2606, #10222, #9321, .T. ) ;
#5783=DIRECTION ( 'NONE',  ( 0.000000000000000000, 0.000000000000000000, -1.000000000000000000 ) ) ;
#5784=ORIENTED_EDGE ( 'NONE', *, *, #3342, .T. ) ;
#5787=LINE ( 'NONE', #2568, #12987 ) ;
#5789=CARTESIAN_POINT ( 'NONE',  ( 3.874999999999999556, 3.137999999999999901, 1.320000000000000062 ) ) ;
#5791=CARTESIAN_POINT ( 'NONE',  ( 3.381088951121218766, 2.435687008709748635, -0.5637784091204912640 ) ) ;
#5795=DIRECTION ( 'NONE',  ( 1.000000000000000000, 0.000000000000000000, 0.000000000000000000 ) ) ;
#5797=CIRCLE ( 'NONE', #11434, 1.039370078740158965 ) ;
#5798=CARTESIAN_POINT ( 'NONE',  ( 2.774999999999999911, 0.6999999999999599876, -2.400000000000011458 ) ) ;
#5799=ADVANCED_FACE ( 'NONE', ( #9525 ), #5568, .F. ) ;
#5800=CARTESIAN_POINT ( 'NONE',  ( 4.623877826222967613, 1.809988068179393395, 0.07275869780465363257 ) ) ;
#5803=ORIENTED_EDGE ( 'NONE', *, *, #12432, .F. ) ;
#5809=FACE_OUTER_BOUND ( 'NONE', #14169, .T. ) ;
#5811=FACE_BOUND ( 'NONE', #12824, .T. ) ;
#5815=CIRCLE ( 'NONE', #4835, 1.932031071636253650 ) ;
#5816=EDGE_CURVE ( 'NONE', #7551, #7156, #1242, .T. ) ;
#5818=CARTESIAN_POINT ( 'NONE',  ( 3.394491571325182644, 1.679378605318042395, -1.416878605318058870 ) ) ;
#5827=CARTESIAN_POINT ( 'NONE',  ( 4.657066280160475635, 1.728587765848446089, 0.2078677355136313021 ) ) ;
#5831=EDGE_LOOP ( 'NONE', ( #14045, #4449, #90, #4008 ) ) ;
#5832=ORIENTED_EDGE ( 'NONE', *, *, #9098, .T. ) ;
#5845=ADVANCED_FACE ( 'NONE', ( #5102 ), #3212, .F. ) ;
#5849=DIRECTION ( 'NONE',  ( 0.000000000000000000, 0.000000000000000000, -1.000000000000000000 ) ) ;
#5852=CARTESIAN_POINT ( 'NONE',  ( 4.344846310392954436, 3.137999999999999901, -1.491010071662831171 ) ) ;
#5853=EDGE_LOOP ( 'NONE', ( #9629, #14220, #1873, #4581 ) ) ;
#5854=DIRECTION ( 'NONE',  ( 0.000000000000000000, 0.000000000000000000, 1.000000000000000000 ) ) ;
#5855=CARTESIAN_POINT ( 'NONE',  ( 6.176491571325181340, 1.679378605318059492, 2.086378605318043533 ) ) ;
#5858=TOROIDAL_SURFACE ( 'NONE', #3659, 0.0001794190581142465670, 1.999999999999999334 ) ;
#5860=CIRCLE ( 'NONE', #2923, 0.3750000000000004996 ) ;
#5861=DIRECTION ( 'NONE',  ( -1.000000000000000000, -0.000000000000000000, -0.000000000000000000 ) ) ;
#5864=CARTESIAN_POINT ( 'NONE',  ( 4.016777269453733368, 1.816382256245877569, -0.7376231757443032500 ) ) ;
#5868=CARTESIAN_POINT ( 'NONE',  ( 3.426491571325181340, 2.062169880637645836, 0.5999481385559802815 ) ) ;
#5879=CONICAL_SURFACE ( 'NONE', #3921, 0.1899999999999996136, 0.7853981633974433940 ) ;
#5881=EDGE_CURVE ( 'NONE', #4965, #3991, #11266, .T. ) ;
#5883=CARTESIAN_POINT ( 'NONE',  ( 4.626593255961919837, 1.749179356862341939, -0.01614418902847078105 ) ) ;
#5885=FACE_OUTER_BOUND ( 'NONE', #3754, .T. ) ;
#5894=DIRECTION ( 'NONE',  ( 0.000000000000000000, 0.000000000000000000, 1.000000000000000000 ) ) ;
#5899=CARTESIAN_POINT ( 'NONE',  ( 3.944129661530210385, 1.867491090171841117, 0.4951980309903491473 ) ) ;
#5900=TOROIDAL_SURFACE ( 'NONE', #11258, 1.580000000000000071, 0.08000000000000000167 ) ;
#5901=DIRECTION ( 'NONE',  ( 8.659560562354890950E-17, -0.7071067811865509034, 0.7071067811865441310 ) ) ;
#5903=CARTESIAN_POINT ( 'NONE',  ( 3.759965575530244131, 0.8734814492854425794, 0.4868720398751328893 ) ) ;
#5904=CARTESIAN_POINT ( 'NONE',  ( 4.661486646721258786, 1.729257228445998384, -0.1974800237815390325 ) ) ;
#5912=ORIENTED_EDGE ( 'NONE', *, *, #13754, .F. ) ;
#5913=DIRECTION ( 'NONE',  ( 1.000000000000000000, 0.000000000000000000, 0.000000000000000000 ) ) ;
#5918=CARTESIAN_POINT ( 'NONE',  ( 3.551656769079091003, 1.993509976604513234, -0.6761768950259927635 ) ) ;
#5922=ORIENTED_EDGE ( 'NONE', *, *, #6913, .F. ) ;
#5928=ADVANCED_FACE ( 'NONE', ( #9000 ), #14688, .F. ) ;
#5934=ORIENTED_EDGE ( 'NONE', *, *, #5015, .T. ) ;
#5935=DIRECTION ( 'NONE',  ( 0.000000000000000000, 0.000000000000000000, -1.000000000000000000 ) ) ;
#5937=AXIS2_PLACEMENT_3D ( 'NONE', #12444, #14817, #1960 ) ;
#5939=DIRECTION ( 'NONE',  ( -0.7071067811865452413, 0.000000000000000000, 0.7071067811865496822 ) ) ;
#5941=ORIENTED_EDGE ( 'NONE', *, *, #2303, .T. ) ;
#5943=CARTESIAN_POINT ( 'NONE',  ( 3.828954533788070602, 1.894954944681144449, -0.4980091310583387720 ) ) ;
#5945=CARTESIAN_POINT ( 'NONE',  ( 2.774999999999999911, 0.000000000000000000, 0.000000000000000000 ) ) ;
#5947=LINE ( 'NONE', #3937, #4721 ) ;
#5948=CARTESIAN_POINT ( 'NONE',  ( 4.674335806064782162, 1.731351353581825681, 0.1332815962874349947 ) ) ;
#5950=DIRECTION ( 'NONE',  ( -0.9659258262890699775, 0.000000000000000000, 0.2588190451025145222 ) ) ;
#5952=ORIENTED_EDGE ( 'NONE', *, *, #14322, .F. ) ;
#5953=DIRECTION ( 'NONE',  ( -0.7071067811865425767, 8.659560562354992023E-17, -0.7071067811865523467 ) ) ;
#5954=ORIENTED_EDGE ( 'NONE', *, *, #15029, .T. ) ;
#5955=EDGE_CURVE ( 'NONE', #8189, #8165, #3946, .T. ) ;
#5961=EDGE_CURVE ( 'NONE', #4007, #906, #7192, .T. ) ;
#5965=DIRECTION ( 'NONE',  ( 0.000000000000000000, 0.000000000000000000, -1.000000000000000000 ) ) ;
#5966=ADVANCED_FACE ( 'NONE', ( #10734 ), #4490, .F. ) ;
#5967=DIRECTION ( 'NONE',  ( 0.000000000000000000, 0.000000000000000000, 1.000000000000000000 ) ) ;
#5969=CIRCLE ( 'NONE', #15003, 0.2944999999999856066 ) ;
#5971=FACE_BOUND ( 'NONE', #13563, .T. ) ;
#5972=CIRCLE ( 'NONE', #4254, 1.932031071636253650 ) ;
#5973=ORIENTED_EDGE ( 'NONE', *, *, #14788, .F. ) ;
#5978=EDGE_CURVE ( 'NONE', #4487, #10219, #11320, .T. ) ;
#5980=CARTESIAN_POINT ( 'NONE',  ( 3.875000000000000000, 1.885381157978845312, 0.5000000000000002220 ) ) ;
#5983=DIRECTION ( 'NONE',  ( -1.000000000000000000, -0.000000000000000000, -0.000000000000000000 ) ) ;
#5985=VECTOR ( 'NONE', #5347, 39.37007874015748143 ) ;
#5987=CARTESIAN_POINT ( 'NONE',  ( 3.426491571325181340, 2.360000000000015863, 1.574999999999999956 ) ) ;
#5989=ORIENTED_EDGE ( 'NONE', *, *, #10067, .F. ) ;
#5990=CARTESIAN_POINT ( 'NONE',  ( 3.447264066911562619, 1.944154718373165780, -0.6966300195041605914 ) ) ;
#5992=DIRECTION ( 'NONE',  ( -1.000000000000000000, -0.000000000000000000, -0.000000000000000000 ) ) ;
#5996=AXIS2_PLACEMENT_3D ( 'NONE', #7758, #768, #7907 ) ;
#6000=DIRECTION ( 'NONE',  ( -1.000000000000000000, -0.000000000000000000, -0.000000000000000000 ) ) ;
#6001=VERTEX_POINT ( 'NONE', #3064 ) ;
#6004=CIRCLE ( 'NONE', #4036, 3.000000000000000444 ) ;
#6017=TOROIDAL_SURFACE ( 'NONE', #13313, 0.0001794190581142465670, 1.999999999999999334 ) ;
#6018=DIRECTION ( 'NONE',  ( 0.000000000000000000, 0.000000000000000000, 1.000000000000000000 ) ) ;
#6020=VERTEX_POINT ( 'NONE', #2210 ) ;
#6021=CARTESIAN_POINT ( 'NONE',  ( 3.663085273664862029, 1.933817475710640998, -0.4530194878470137354 ) ) ;
#6023=CARTESIAN_POINT ( 'NONE',  ( 2.774999999999999911, -1.679378605318059048, -1.679378605318041950 ) ) ;
#6025=AXIS2_PLACEMENT_3D ( 'NONE', #7354, #12154, #7566 ) ;
#6030=ORIENTED_EDGE ( 'NONE', *, *, #2904, .T. ) ;
#6033=VERTEX_POINT ( 'NONE', #5818 ) ;
#6047=VECTOR ( 'NONE', #8922, 39.37007874015748143 ) ;
#6049=CARTESIAN_POINT ( 'NONE',  ( 4.040612674447555897, 1.739716132213777522, 0.7790939297231012084 ) ) ;
#6060=CIRCLE ( 'NONE', #12670, 2.500000000000000000 ) ;
#6066=ORIENTED_EDGE ( 'NONE', *, *, #13005, .F. ) ;
#6067=CARTESIAN_POINT ( 'NONE',  ( 3.426491571325181340, 1.679378605318059048, 1.679378605318041506 ) ) ;
#6068=EDGE_CURVE ( 'NONE', #5706, #12243, #11547, .T. ) ;
#6070=CARTESIAN_POINT ( 'NONE',  ( 3.874999999999999556, 3.105999999999998984, 1.130000000000000560 ) ) ;
#6071=DIRECTION ( 'NONE',  ( -1.000000000000000000, -0.000000000000000000, -0.000000000000000000 ) ) ;
#6073=AXIS2_PLACEMENT_3D ( 'NONE', #5789, #3651, #11599 ) ;
#6074=CARTESIAN_POINT ( 'NONE',  ( 3.426491571325181340, -0.6999999999999989564, -2.399999999999999911 ) ) ;
#6077=DIRECTION ( 'NONE',  ( 0.000000000000000000, 0.000000000000000000, -1.000000000000000000 ) ) ;
#6079=EDGE_LOOP ( 'NONE', ( #10369, #3375 ) ) ;
#6081=CARTESIAN_POINT ( 'NONE',  ( 6.826491571325181695, 1.679378605318035733, -2.054378605318066153 ) ) ;
#6085=VECTOR ( 'NONE', #8549, 39.37007874015748143 ) ;
#6086=CARTESIAN_POINT ( 'NONE',  ( 2.774999999999999911, 0.9799999999999438050, -2.360000000000016307 ) ) ;
#6090=VERTEX_POINT ( 'NONE', #1209 ) ;
#6091=VERTEX_POINT ( 'NONE', #4742 ) ;
#6096=AXIS2_PLACEMENT_3D ( 'NONE', #5001, #11095, #2701 ) ;
#6100=AXIS2_PLACEMENT_3D ( 'NONE', #3119, #8854, #13345 ) ;
#6101=CARTESIAN_POINT ( 'NONE',  ( 3.394491571325183088, -1.679378605318041950, 1.416878605318058870 ) ) ;
#6102=ORIENTED_EDGE ( 'NONE', *, *, #5881, .T. ) ;
#6103=VECTOR ( 'NONE', #14420, 39.37007874015748143 ) ;
#6104=DIRECTION ( 'NONE',  ( 0.000000000000000000, 0.000000000000000000, -1.000000000000000000 ) ) ;
#6109=AXIS2_PLACEMENT_3D ( 'NONE', #2725, #14563, #8838 ) ;
#6110=CARTESIAN_POINT ( 'NONE',  ( 4.263277331923934099, 1.731577658895514071, -0.6428753901762764844 ) ) ;
#6115=CARTESIAN_POINT ( 'NONE',  ( 3.874999999999999556, 3.137999999999999901, -1.542000000000000037 ) ) ;
#6124=EDGE_CURVE ( 'NONE', #626, #6575, #14668, .T. ) ;
#6126=CARTESIAN_POINT ( 'NONE',  ( 3.874999999999999556, 3.137999999999999901, 1.320000000000000062 ) ) ;
#6129=CARTESIAN_POINT ( 'NONE',  ( 3.643781337222963046, 1.948212547232942127, 0.7131559760554623262 ) ) ;
#6131=VERTEX_POINT ( 'NONE', #2369 ) ;
#6135=EDGE_LOOP ( 'NONE', ( #14555, #2685 ) ) ;
#6136=CARTESIAN_POINT ( 'NONE',  ( 3.426491571325181340, 1.679378605318059048, 1.384878605318043521 ) ) ;
#6143=ORIENTED_EDGE ( 'NONE', *, *, #9449, .T. ) ;
#6149=DIRECTION ( 'NONE',  ( 0.000000000000000000, 0.000000000000000000, -1.000000000000000000 ) ) ;
#6154=EDGE_CURVE ( 'NONE', #2972, #11468, #3822, .T. ) ;
#6156=CARTESIAN_POINT ( 'NONE',  ( 3.875000000000000000, 0.7099999999999984102, -0.4849999999999995981 ) ) ;
#6161=CARTESIAN_POINT ( 'NONE',  ( 3.426491571325181340, 0.000000000000000000, 2.500000000000000444 ) ) ;
#6170=CYLINDRICAL_SURFACE ( 'NONE', #1687, 0.5000000000000002220 ) ;
#6172=DIRECTION ( 'NONE',  ( 1.000000000000000000, 0.000000000000000000, 0.000000000000000000 ) ) ;
#6173=AXIS2_PLACEMENT_3D ( 'NONE', #7899, #12549, #13848 ) ;
#6175=EDGE_CURVE ( 'NONE', #159, #3499, #11851, .T. ) ;
#6177=CONICAL_SURFACE ( 'NONE', #5937, 0.2625000000000000111, 0.7853981633974503884 ) ;
#6179=VERTEX_POINT ( 'NONE', #11781 ) ;
#6181=EDGE_LOOP ( 'NONE', ( #15013, #3814 ) ) ;
#6183=CIRCLE ( 'NONE', #527, 0.1000000000000000194 ) ;
#6190=CARTESIAN_POINT ( 'NONE',  ( 3.874999999999999556, 3.105999999999998984, -1.509999999999999787 ) ) ;
#6194=CARTESIAN_POINT ( 'NONE',  ( 6.176491571325181340, 0.000000000000000000, 0.000000000000000000 ) ) ;
#6196=EDGE_CURVE ( 'NONE', #3491, #12114, #3022, .T. ) ;
#6198=ORIENTED_EDGE ( 'NONE', *, *, #12596, .F. ) ;
#6199=AXIS2_PLACEMENT_3D ( 'NONE', #1115, #12672, #8342 ) ;
#6200=DIRECTION ( 'NONE',  ( 0.7071067811865519026, 8.659560562354877391E-17, 0.7071067811865430208 ) ) ;
#6201=FACE_OUTER_BOUND ( 'NONE', #7797, .T. ) ;
#6202=ORIENTED_EDGE ( 'NONE', *, *, #8982, .T. ) ;
#6208=ORIENTED_EDGE ( 'NONE', *, *, #12366, .F. ) ;
#6210=DIRECTION ( 'NONE',  ( 0.000000000000000000, 0.000000000000000000, -1.000000000000000000 ) ) ;
#6212=AXIS2_PLACEMENT_3D ( 'NONE', #6067, #4408, #6859 ) ;
#6218=EDGE_LOOP ( 'NONE', ( #14232, #13319, #8315, #11539 ) ) ;
#6219=DIRECTION ( 'NONE',  ( 0.000000000000000000, 0.000000000000000000, 1.000000000000000000 ) ) ;
#6225=DIRECTION ( 'NONE',  ( -0.000000000000000000, -1.000000000000000000, -0.000000000000000000 ) ) ;
#6228=CIRCLE ( 'NONE', #5996, 1.932031071636253650 ) ;
#6231=VECTOR ( 'NONE', #12109, 39.37007874015748143 ) ;
#6233=EDGE_CURVE ( 'NONE', #12635, #13163, #5221, .T. ) ;
#6234=ORIENTED_EDGE ( 'NONE', *, *, #14133, .T. ) ;
#6235=VERTEX_POINT ( 'NONE', #5611 ) ;
#6239=CARTESIAN_POINT ( 'NONE',  ( 4.769268701363833074, 3.137999999999999901, -0.3249191361593796734 ) ) ;
#6240=EDGE_CURVE ( 'NONE', #331, #14332, #10272, .T. ) ;
#6244=VECTOR ( 'NONE', #5507, 39.37007874015748143 ) ;
#6245=AXIS2_PLACEMENT_3D ( 'NONE', #2377, #11721, #13755 ) ;
#6246=CARTESIAN_POINT ( 'NONE',  ( 4.621667715411809318, 1.809504207475592485, 0.09880105512956799396 ) ) ;
#6247=DIRECTION ( 'NONE',  ( 0.000000000000000000, 0.000000000000000000, 1.000000000000000000 ) ) ;
#6248=EDGE_CURVE ( 'NONE', #7097, #14200, #3304, .T. ) ;
#6254=AXIS2_PLACEMENT_3D ( 'NONE', #15032, #5638, #10221 ) ;
#6255=VERTEX_POINT ( 'NONE', #10785 ) ;
#6258=DIRECTION ( 'NONE',  ( -1.000000000000000000, -0.000000000000000000, -0.000000000000000000 ) ) ;
#6263=CARTESIAN_POINT ( 'NONE',  ( 6.794491571325181667, 1.679378605318059492, 1.304378605318041062 ) ) ;
#6265=ADVANCED_FACE ( 'NONE', ( #13277 ), #6447, .T. ) ;
#6266=CIRCLE ( 'NONE', #6500, 0.4849999999999995981 ) ;
#6267=CARTESIAN_POINT ( 'NONE',  ( 3.458515826269089377, 2.043633784419520705, 0.6239720965697329591 ) ) ;
#6269=VECTOR ( 'NONE', #1999, 39.37007874015748143 ) ;
#6273=CARTESIAN_POINT ( 'NONE',  ( 3.807348201284447953, 1.879736805572670422, 0.7469949793200116872 ) ) ;
#6274=CARTESIAN_POINT ( 'NONE',  ( 3.874999999999999556, 3.105999999999998984, -1.509999999999999787 ) ) ;
#6275=AXIS2_PLACEMENT_3D ( 'NONE', #14677, #13669, #10094 ) ;
#6278=FACE_OUTER_BOUND ( 'NONE', #5192, .T. ) ;
#6279=ORIENTED_EDGE ( 'NONE', *, *, #6154, .T. ) ;
#6283=( LENGTH_UNIT ( ) NAMED_UNIT ( * ) SI_UNIT ( $, .METRE. ) );
#6298=ORIENTED_EDGE ( 'NONE', *, *, #9053, .F. ) ;
#6301=CARTESIAN_POINT ( 'NONE',  ( 3.426491571325181340, -1.574999999999984190, 1.575000000000033040 ) ) ;
#6304=DIRECTION ( 'NONE',  ( 1.000000000000000000, 0.000000000000000000, 0.000000000000000000 ) ) ;
#6306=CARTESIAN_POINT ( 'NONE',  ( 6.176491571325181340, 1.679378605318035733, -2.086378605318067958 ) ) ;
#6307=CARTESIAN_POINT ( 'NONE',  ( 6.176491571325181340, 1.679378605318059492, 2.086378605318043533 ) ) ;
#6309=ORIENTED_EDGE ( 'NONE', *, *, #2588, .T. ) ;
#6310=ORIENTED_EDGE ( 'NONE', *, *, #13754, .T. ) ;
#6314=DIRECTION ( 'NONE',  ( 1.000000000000000000, 0.000000000000000000, 0.000000000000000000 ) ) ;
#6317=FACE_OUTER_BOUND ( 'NONE', #5005, .T. ) ;
#6318=AXIS2_PLACEMENT_3D ( 'NONE', #8333, #2569, #12965 ) ;
#6319=CARTESIAN_POINT ( 'NONE',  ( 3.426491571325181784, 2.056034060376116024, -0.5999481385559809477 ) ) ;
#6320=AXIS2_PLACEMENT_3D ( 'NONE', #8511, #1296, #13220 ) ;
#6321=CARTESIAN_POINT ( 'NONE',  ( 4.607097790994713726, 1.806582460388006073, 0.1715432876979409993 ) ) ;
#6327=AXIS2_PLACEMENT_3D ( 'NONE', #10509, #9595, #2547 ) ;
#6328=CARTESIAN_POINT ( 'NONE',  ( 4.264972657050305038, 1.781419589088464317, -0.6418377093470817307 ) ) ;
#6333=ORIENTED_EDGE ( 'NONE', *, *, #4896, .F. ) ;
#6334=CARTESIAN_POINT ( 'NONE',  ( 3.394491571325183088, -1.679378605318041950, 1.679378605318059048 ) ) ;
#6338=ORIENTED_EDGE ( 'NONE', *, *, #10260, .F. ) ;
#6341=ADVANCED_FACE ( 'NONE', ( #2128 ), #7430, .F. ) ;
#6344=EDGE_CURVE ( 'NONE', #4913, #2874, #4363, .T. ) ;
#6345=STYLED_ITEM('',(#15171),#10609);
#6346=AXIS2_PLACEMENT_3D ( 'NONE', #10605, #14191, #6104 ) ;
#6350=ADVANCED_FACE ( 'NONE', ( #13678 ), #13036, .F. ) ;
#6351=LINE ( 'NONE', #11002, #5356 ) ;
#6352=FACE_OUTER_BOUND ( 'NONE', #6648, .T. ) ;
#6356=FACE_BOUND ( 'NONE', #4811, .T. ) ;
#6357=ORIENTED_EDGE ( 'NONE', *, *, #4972, .T. ) ;
#6359=CIRCLE ( 'NONE', #14404, 2.070731779878276502 ) ;
#6362=DIRECTION ( 'NONE',  ( 0.000000000000000000, 0.000000000000000000, -1.000000000000000000 ) ) ;
#6364=DIRECTION ( 'NONE',  ( 1.000000000000000000, 0.000000000000000000, 0.000000000000000000 ) ) ;
#6367=LINE ( 'NONE', #14308, #9260 ) ;
#6374=CARTESIAN_POINT ( 'NONE',  ( 3.426491571325181340, 1.987932976489903636, -0.2209981660730357955 ) ) ;
#6375=ORIENTED_EDGE ( 'NONE', *, *, #9707, .T. ) ;
#6382=CIRCLE ( 'NONE', #10531, 1.500000000000000222 ) ;
#6385=ORIENTED_EDGE ( 'NONE', *, *, #14185, .F. ) ;
#6390=ORIENTED_EDGE ( 'NONE', *, *, #4955, .F. ) ;
#6393=AXIS2_PLACEMENT_3D ( 'NONE', #9621, #4959, #323 ) ;
#6395=CARTESIAN_POINT ( 'NONE',  ( 3.923955648118384598, 1.840411246837426962, 0.7499999999999997780 ) ) ;
#6402=EDGE_CURVE ( 'NONE', #2606, #3991, #5204, .T. ) ;
#6404=CARTESIAN_POINT ( 'NONE',  ( 4.374208753957563367, 0.9996035968963620233, -0.03268784858779524849 ) ) ;
#6409=LINE ( 'NONE', #13273, #14632 ) ;
#6413=CARTESIAN_POINT ( 'NONE',  ( 4.497905261668263321, 1.733752379391429566, 0.4204404687884559788 ) ) ;
#6414=EDGE_CURVE ( 'NONE', #114, #14916, #14496, .T. ) ;
#6415=DIRECTION ( 'NONE',  ( 0.000000000000000000, 0.000000000000000000, 1.000000000000000000 ) ) ;
#6416=VERTEX_POINT ( 'NONE', #1742 ) ;
#6417=CIRCLE ( 'NONE', #10817, 1.500000000000000222 ) ;
#6422=FACE_OUTER_BOUND ( 'NONE', #5727, .T. ) ;
#6428=ORIENTED_EDGE ( 'NONE', *, *, #3071, .T. ) ;
#6431=EDGE_CURVE ( 'NONE', #6255, #6090, #7914, .T. ) ;
#6438=DIRECTION ( 'NONE',  ( 0.000000000000000000, 0.000000000000000000, 1.000000000000000000 ) ) ;
#6439=EDGE_CURVE ( 'NONE', #14916, #114, #5969, .T. ) ;
#6440=ORIENTED_EDGE ( 'NONE', *, *, #11951, .F. ) ;
#6443=VERTEX_POINT ( 'NONE', #5098 ) ;
#6444=CARTESIAN_POINT ( 'NONE',  ( 2.774999999999999911, 0.9800000000000039790, 3.360000000000000320 ) ) ;
#6447=CONICAL_SURFACE ( 'NONE', #8173, 2.960629921259841257, 0.7853981633974552734 ) ;
#6453=DIRECTION ( 'NONE',  ( 0.000000000000000000, 0.000000000000000000, -1.000000000000000000 ) ) ;
#6455=VECTOR ( 'NONE', #9869, 39.37007874015748143 ) ;
#6456=CYLINDRICAL_SURFACE ( 'NONE', #3755, 0.7849999999999969225 ) ;
#6457=ORIENTED_EDGE ( 'NONE', *, *, #9342, .T. ) ;
#6458=ORIENTED_EDGE ( 'NONE', *, *, #896, .T. ) ;
#6459=VERTEX_POINT ( 'NONE', #12696 ) ;
#6465=DIRECTION ( 'NONE',  ( 0.000000000000000000, 1.000000000000000000, -1.423315761404775650E-14 ) ) ;
#6466=AXIS2_PLACEMENT_3D ( 'NONE', #11275, #10135, #14645 ) ;
#6467=CARTESIAN_POINT ( 'NONE',  ( 4.439088310279003302, 1.783130252920299696, 0.4984960193556706720 ) ) ;
#6471=EDGE_LOOP ( 'NONE', ( #13179, #9468, #3005, #4300, #5954, #5639, #1988, #11130 ) ) ;
#6474=VERTEX_POINT ( 'NONE', #10189 ) ;
#6475=DIRECTION ( 'NONE',  ( 0.000000000000000000, 0.000000000000000000, -1.000000000000000000 ) ) ;
#6476=CONICAL_SURFACE ( 'NONE', #2805, 0.4070000000000022489, 0.7853981633974547183 ) ;
#6478=CARTESIAN_POINT ( 'NONE',  ( 4.344846310392954436, 2.750000000000000000, 1.491010071662831171 ) ) ;
#6479=CARTESIAN_POINT ( 'NONE',  ( 3.941521638426727758, 0.8684168616498817439, 0.4958385474027912632 ) ) ;
#6480=DIRECTION ( 'NONE',  ( 1.000000000000000000, 0.000000000000000000, 0.000000000000000000 ) ) ;
#6484=DIRECTION ( 'NONE',  ( 0.000000000000000000, 0.000000000000000000, 1.000000000000000000 ) ) ;
#6490=AXIS2_PLACEMENT_3D ( 'NONE', #9719, #4982, #9578 ) ;
#6492=CARTESIAN_POINT ( 'NONE',  ( 4.593106923254413942, 1.719712382094653824, 0.3671620375188934804 ) ) ;
#6497=ORIENTED_EDGE ( 'NONE', *, *, #11689, .F. ) ;
#6498=ORIENTED_EDGE ( 'NONE', *, *, #14133, .F. ) ;
#6500=AXIS2_PLACEMENT_3D ( 'NONE', #14368, #652, #14595 ) ;
#6502=ORIENTED_EDGE ( 'NONE', *, *, #1157, .F. ) ;
#6505=AXIS2_PLACEMENT_3D ( 'NONE', #14503, #15027, #13579 ) ;
#6508=EDGE_CURVE ( 'NONE', #6847, #4204, #14551, .T. ) ;
#6512=AXIS2_PLACEMENT_3D ( 'NONE', #9790, #7635, #2899 ) ;
#6515=ORIENTED_EDGE ( 'NONE', *, *, #7688, .T. ) ;
#6517=DIRECTION ( 'NONE',  ( 0.000000000000000000, 0.000000000000000000, 1.000000000000000000 ) ) ;
#6519=CARTESIAN_POINT ( 'NONE',  ( 6.826491571325181695, 1.679378605318059492, 2.086378605318041757 ) ) ;
#6520=ORIENTED_EDGE ( 'NONE', *, *, #8940, .F. ) ;
#6523=DIRECTION ( 'NONE',  ( -0.000000000000000000, 1.000000000000000000, -0.000000000000000000 ) ) ;
#6532=CARTESIAN_POINT ( 'NONE',  ( 3.504516174824143793, 1.917097053177361010, 0.7259348004102793572 ) ) ;
#6534=CIRCLE ( 'NONE', #11348, 0.2945000000000009277 ) ;
#6537=ORIENTED_EDGE ( 'NONE', *, *, #8940, .T. ) ;
#6538=EDGE_CURVE ( 'NONE', #4204, #1773, #7614, .T. ) ;
#6545=CARTESIAN_POINT ( 'NONE',  ( 3.426491571325181340, 2.062169880637645836, -0.5999481385559802815 ) ) ;
#6546=CARTESIAN_POINT ( 'NONE',  ( 4.100009802906539491, 1.799994069799653484, 0.7160437602263716173 ) ) ;
#6552=ORIENTED_EDGE ( 'NONE', *, *, #6862, .F. ) ;
#6562=ORIENTED_EDGE ( 'NONE', *, *, #9096, .F. ) ;
#6567=VECTOR ( 'NONE', #13766, 39.37007874015748143 ) ;
#6571=AXIS2_PLACEMENT_3D ( 'NONE', #14138, #7125, #2518 ) ;
#6573=CARTESIAN_POINT ( 'NONE',  ( 3.858712094495529321, 1.861610320989349754, 0.7499885605692133694 ) ) ;
#6574=CARTESIAN_POINT ( 'NONE',  ( 3.875000000000000000, 1.885381157978844868, -0.5000000000000002220 ) ) ;
#6575=VERTEX_POINT ( 'NONE', #10710 ) ;
#6579=AXIS2_PLACEMENT_3D ( 'NONE', #1900, #586, #816 ) ;
#6582=ADVANCED_FACE ( 'NONE', ( #4829 ), #14063, .F. ) ;
#6589=DIRECTION ( 'NONE',  ( 0.000000000000000000, 0.000000000000000000, -1.000000000000000000 ) ) ;
#6593=CARTESIAN_POINT ( 'NONE',  ( 3.388178971404831596, 0.9934719948626907771, 0.1152309124458658768 ) ) ;
#6594=CARTESIAN_POINT ( 'NONE',  ( 4.430922016235464334, 1.707647511453724842, -0.5743937140048646084 ) ) ;
#6597=CARTESIAN_POINT ( 'NONE',  ( 4.180700663235655590, 0.9180451591693143953, -0.3969666424556979045 ) ) ;
#6598=DIRECTION ( 'NONE',  ( 0.000000000000000000, -1.000000000000000000, 0.000000000000000000 ) ) ;
#6600=DIRECTION ( 'NONE',  ( 0.000000000000000000, 0.000000000000000000, -1.000000000000000000 ) ) ;
#6601=VERTEX_POINT ( 'NONE', #3604 ) ;
#6602=ADVANCED_FACE ( 'NONE', ( #2454, #7134, #13064, #5971, #14148, #11003 ), #8636, .F. ) ;
#6604=CARTESIAN_POINT ( 'NONE',  ( 3.458450979136563852, 2.043671318866147946, -0.6239234495429138994 ) ) ;
#6608=DIRECTION ( 'NONE',  ( -1.000000000000000000, -0.000000000000000000, -0.000000000000000000 ) ) ;
#6610=EDGE_LOOP ( 'NONE', ( #12997, #2464, #8904, #6921 ) ) ;
#6611=DIRECTION ( 'NONE',  ( 0.000000000000000000, 0.000000000000000000, -1.000000000000000000 ) ) ;
#6615=VERTEX_POINT ( 'NONE', #13139 ) ;
#6617=EDGE_CURVE ( 'NONE', #7135, #6235, #3274, .T. ) ;
#6618=LINE ( 'NONE', #7904, #6269 ) ;
#6620=EDGE_CURVE ( 'NONE', #327, #2972, #7562, .T. ) ;
#6629=VERTEX_POINT ( 'NONE', #14440 ) ;
#6631=ORIENTED_EDGE ( 'NONE', *, *, #6804, .T. ) ;
#6632=AXIS2_PLACEMENT_3D ( 'NONE', #2318, #7000, #5854 ) ;
#6636=CARTESIAN_POINT ( 'NONE',  ( 3.874999999999999556, 2.782000000000002693, 1.130000000000000560 ) ) ;
#6637=EDGE_LOOP ( 'NONE', ( #10117, #1755, #5164, #6631 ) ) ;
#6641=EDGE_CURVE ( 'NONE', #12484, #8434, #13353, .T. ) ;
#6645=CARTESIAN_POINT ( 'NONE',  ( 4.525494676330790611, 1.792733192933819053, 0.3777435136916634795 ) ) ;
#6646=CARTESIAN_POINT ( 'NONE',  ( 3.693802410306114226, 1.943924811042458733, -0.4665840092633480318 ) ) ;
#6647=ORIENTED_EDGE ( 'NONE', *, *, #4667, .T. ) ;
#6648=EDGE_LOOP ( 'NONE', ( #12960, #614, #5197, #10864 ) ) ;
#6649=DIRECTION ( 'NONE',  ( 0.000000000000000000, 0.000000000000000000, -1.000000000000000000 ) ) ;
#6652=DIRECTION ( 'NONE',  ( -0.7071067811865421326, 8.659560562354996953E-17, -0.7071067811865527908 ) ) ;
#6663=ADVANCED_FACE ( 'NONE', ( #6352 ), #5128, .F. ) ;
#6665=CARTESIAN_POINT ( 'NONE',  ( 3.441951518218600015, 0.9681238899719051272, -0.2520395006946318239 ) ) ;
#6672=EDGE_LOOP ( 'NONE', ( #11207, #2640, #7941, #9193 ) ) ;
#6681=CARTESIAN_POINT ( 'NONE',  ( 3.426491571325181340, -0.9799999999999436939, 3.360000000000016751 ) ) ;
#6682=CARTESIAN_POINT ( 'NONE',  ( 3.828636530710406216, 1.793264967391777542, 0.7984341528290008760 ) ) ;
#6685=ORIENTED_EDGE ( 'NONE', *, *, #2219, .T. ) ;
#6686=DIRECTION ( 'NONE',  ( -1.000000000000000000, -0.000000000000000000, -0.000000000000000000 ) ) ;
#6688=VECTOR ( 'NONE', #6735, 39.37007874015748143 ) ;
#6692=CARTESIAN_POINT ( 'NONE',  ( 3.537411752015444222, 2.007197475989087820, 0.3717360073472075199 ) ) ;
#6693=EDGE_CURVE ( 'NONE', #14527, #8165, #4042, .T. ) ;
#6698=ORIENTED_EDGE ( 'NONE', *, *, #6196, .T. ) ;
#6699=EDGE_CURVE ( 'NONE', #1776, #5690, #11070, .T. ) ;
#6701=ORIENTED_EDGE ( 'NONE', *, *, #9911, .T. ) ;
#6702=DIRECTION ( 'NONE',  ( 0.000000000000000000, -1.000000000000000000, 0.000000000000000000 ) ) ;
#6707=VECTOR ( 'NONE', #4348, 39.37007874015748143 ) ;
#6708=CARTESIAN_POINT ( 'NONE',  ( 3.133380147778130453, 2.497928943106615396, 0.1166857200839504505 ) ) ;
#6710=CARTESIAN_POINT ( 'NONE',  ( 2.774999999999999911, -0.9799999999999989830, -2.359999999999999876 ) ) ;
#6713=EDGE_CURVE ( 'NONE', #3499, #14976, #9405, .T. ) ;
#6716=CARTESIAN_POINT ( 'NONE',  ( 4.391810419801174703, 1.780532734934683337, 0.5461860461645056120 ) ) ;
#6717=CIRCLE ( 'NONE', #14523, 0.4070000000000025264 ) ;
#6718=CARTESIAN_POINT ( 'NONE',  ( 3.426491571325181340, 1.954234464180151676, -0.6847610993685215863 ) ) ;
#6722=EDGE_CURVE ( 'NONE', #10316, #13316, #2047, .T. ) ;
#6728=LINE ( 'NONE', #3356, #2885 ) ;
#6731=ORIENTED_EDGE ( 'NONE', *, *, #12482, .T. ) ;
#6732=DIRECTION ( 'NONE',  ( 0.7071067811865421326, 8.659560562354996953E-17, 0.7071067811865527908 ) ) ;
#6735=DIRECTION ( 'NONE',  ( -1.000000000000000000, -0.000000000000000000, -0.000000000000000000 ) ) ;
#6736=CIRCLE ( 'NONE', #11361, 0.4070000000000025264 ) ;
#6739=ORIENTED_EDGE ( 'NONE', *, *, #14059, .F. ) ;
#6740=CARTESIAN_POINT ( 'NONE',  ( 3.873439288382781065, 3.137999999999999901, 6.065921084684207584E-32 ) ) ;
#6741=CARTESIAN_POINT ( 'NONE',  ( 3.652468232434641138, 1.936298606780756382, 0.4501807712518157145 ) ) ;
#6743=EDGE_CURVE ( 'NONE', #13527, #4018, #8790, .T. ) ;
#6746=DIRECTION ( 'NONE',  ( -0.000000000000000000, -1.000000000000000000, -0.000000000000000000 ) ) ;
#6750=AXIS2_PLACEMENT_3D ( 'NONE', #11974, #10977, #3942 ) ;
#6756=AXIS2_PLACEMENT_3D ( 'NONE', #14921, #5447, #10114 ) ;
#6760=VECTOR ( 'NONE', #10514, 39.37007874015748143 ) ;
#6771=EDGE_CURVE ( 'NONE', #10875, #1362, #3903, .T. ) ;
#6775=CARTESIAN_POINT ( 'NONE',  ( 3.437087787517782100, 2.053741209332538453, 0.2425028344550888282 ) ) ;
#6777=EDGE_LOOP ( 'NONE', ( #8942, #14675, #1732, #14223 ) ) ;
#6779=EDGE_LOOP ( 'NONE', ( #4427, #107, #13916, #6739 ) ) ;
#6781=EDGE_LOOP ( 'NONE', ( #8365, #2439, #2351, #13438 ) ) ;
#6783=ORIENTED_EDGE ( 'NONE', *, *, #5978, .T. ) ;
#6784=DIRECTION ( 'NONE',  ( 0.000000000000000000, 1.000000000000000000, 0.000000000000000000 ) ) ;
#6786=CARTESIAN_POINT ( 'NONE',  ( 2.980731298636167370, 3.137999999999999901, 0.3249191361593797844 ) ) ;
#6790=CARTESIAN_POINT ( 'NONE',  ( 3.232037046709189898, 2.470280355568556185, -0.3878822227790326704 ) ) ;
#6791=VECTOR ( 'NONE', #9085, 39.37007874015748143 ) ;
#6793=CARTESIAN_POINT ( 'NONE',  ( 3.874999999999999556, 3.105999999999998984, 1.320000000000000062 ) ) ;
#6795=DIRECTION ( 'NONE',  ( 0.000000000000000000, 0.000000000000000000, 1.000000000000000000 ) ) ;
#6796=CARTESIAN_POINT ( 'NONE',  ( 4.586165101391412868, 1.802583718471729268, -0.2454321292609802641 ) ) ;
#6797=DIRECTION ( 'NONE',  ( -1.000000000000000000, -0.000000000000000000, -0.000000000000000000 ) ) ;
#6801=DIRECTION ( 'NONE',  ( -1.000000000000000000, -0.000000000000000000, -0.000000000000000000 ) ) ;
#6804=EDGE_CURVE ( 'NONE', #4100, #803, #7793, .T. ) ;
#6805=EDGE_CURVE ( 'NONE', #9590, #7408, #960, .T. ) ;
#6810=EDGE_LOOP ( 'NONE', ( #13933, #13838, #11305, #3398, #759, #3911, #3388, #230, #13937, #2668, #14717, #14945 ) ) ;
#6811=ADVANCED_FACE ( 'NONE', ( #8864 ), #9023, .T. ) ;
#6818=EDGE_CURVE ( 'NONE', #12391, #14596, #8661, .T. ) ;
#6825=CONICAL_SURFACE ( 'NONE', #14611, 1.932031071636253650, 0.2617993877991429685 ) ;
#6826=CARTESIAN_POINT ( 'NONE',  ( 3.402054984780856550, 0.9867414601700450483, -0.1630887597480132623 ) ) ;
#6828=CARTESIAN_POINT ( 'NONE',  ( 4.111306219097818904, 1.727883204818585483, -0.7590129541647976374 ) ) ;
#6830=FACE_OUTER_BOUND ( 'NONE', #12043, .T. ) ;
#6836=AXIS2_PLACEMENT_3D ( 'NONE', #10685, #10534, #9619 ) ;
#6847=VERTEX_POINT ( 'NONE', #6718 ) ;
#6849=CARTESIAN_POINT ( 'NONE',  ( 4.769268701363833074, 2.750000000000000000, -0.3249191361593796734 ) ) ;
#6855=VECTOR ( 'NONE', #458, 39.37007874015748143 ) ;
#6857=CARTESIAN_POINT ( 'NONE',  ( 3.490426473332387758, 2.028536269912275536, 0.3203772365046669846 ) ) ;
#6858=APPLICATION_CONTEXT ( 'automotive_design' ) ;
#6859=DIRECTION ( 'NONE',  ( 0.000000000000000000, 0.000000000000000000, -1.000000000000000000 ) ) ;
#6862=EDGE_CURVE ( 'NONE', #3928, #11740, #15099, .T. ) ;
#6863=ORIENTED_EDGE ( 'NONE', *, *, #14059, .T. ) ;
#6864=VERTEX_POINT ( 'NONE', #728 ) ;
#6868=FACE_OUTER_BOUND ( 'NONE', #1809, .T. ) ;
#6870=FACE_OUTER_BOUND ( 'NONE', #2023, .T. ) ;
#6876=CARTESIAN_POINT ( 'NONE',  ( 3.874999999999999556, 3.137999999999999901, -1.320000000000000062 ) ) ;
#6878=EDGE_CURVE ( 'NONE', #14332, #3499, #540, .T. ) ;
#6879=CARTESIAN_POINT ( 'NONE',  ( 4.606274573907592540, 1.806393012917786534, -0.1768982737102013092 ) ) ;
#6881=CARTESIAN_POINT ( 'NONE',  ( 3.426491571325181340, 3.360000000000016751, 0.9799999999999461364 ) ) ;
#6892=CARTESIAN_POINT ( 'NONE',  ( 2.806999999999999496, -1.679378605318041950, 1.941878605318059003 ) ) ;
#6902=CIRCLE ( 'NONE', #8842, 0.2220000000000021678 ) ;
#6903=CARTESIAN_POINT ( 'NONE',  ( 3.394491571325183088, 1.679378605318059048, 1.679378605318041506 ) ) ;
#6910=DIRECTION ( 'NONE',  ( -1.000000000000000000, -0.000000000000000000, -0.000000000000000000 ) ) ;
#6911=CARTESIAN_POINT ( 'NONE',  ( 6.176491571325181340, 0.000000000000000000, 0.000000000000000000 ) ) ;
#6913=EDGE_CURVE ( 'NONE', #11132, #8878, #8631, .T. ) ;
#6914=DIRECTION ( 'NONE',  ( 1.000000000000000000, 0.000000000000000000, 0.000000000000000000 ) ) ;
#6918=CARTESIAN_POINT ( 'NONE',  ( 3.426491571325181340, -2.359999999999979892, 1.575000000000016387 ) ) ;
#6921=ORIENTED_EDGE ( 'NONE', *, *, #1765, .T. ) ;
#6925=EDGE_CURVE ( 'NONE', #8503, #13119, #4477, .T. ) ;
#6929=DIRECTION ( 'NONE',  ( 0.7071067811865421326, 0.000000000000000000, -0.7071067811865527908 ) ) ;
#6930=DIRECTION ( 'NONE',  ( 0.000000000000000000, 1.000000000000000000, 0.000000000000000000 ) ) ;
#6931=VECTOR ( 'NONE', #5950, 39.37007874015748143 ) ;
#6932=CARTESIAN_POINT ( 'NONE',  ( 3.741597707132858108, 1.905344493321387889, -0.7379504897677242603 ) ) ;
#6935=ADVANCED_FACE ( 'NONE', ( #10692 ), #14043, .F. ) ;
#6945=ADVANCED_FACE ( 'NONE', ( #5885 ), #2528, .F. ) ;
#6951=CARTESIAN_POINT ( 'NONE',  ( 4.685776054466175289, 1.733272791389190548, 0.03942178684877539058 ) ) ;
#6953=VERTEX_POINT ( 'NONE', #8263 ) ;
#6956=CARTESIAN_POINT ( 'NONE',  ( 2.774999999999999911, 0.000000000000000000, 1.039370078740158965 ) ) ;
#6962=ORIENTED_EDGE ( 'NONE', *, *, #78, .T. ) ;
#6965=EDGE_CURVE ( 'NONE', #8303, #11264, #10388, .T. ) ;
#6966=DIRECTION ( 'NONE',  ( 0.000000000000000000, 0.000000000000000000, -1.000000000000000000 ) ) ;
#6973=CARTESIAN_POINT ( 'NONE',  ( 3.510666870471307988, 0.9394827552388973491, 0.3428102772992727143 ) ) ;
#6976=DIRECTION ( 'NONE',  ( -0.000000000000000000, -1.000000000000000000, -0.000000000000000000 ) ) ;
#6977=DIRECTION ( 'NONE',  ( -0.7071067811865429098, 8.659560562354987092E-17, -0.7071067811865521247 ) ) ;
#6978=ORIENTED_EDGE ( 'NONE', *, *, #13518, .F. ) ;
#6980=AXIS2_PLACEMENT_3D ( 'NONE', #11307, #2121, #887 ) ;
#6984=VECTOR ( 'NONE', #14248, 39.37007874015748143 ) ;
#6986=B_SPLINE_CURVE_WITH_KNOTS ( 'NONE', 3,
 ( #2497, #9393, #4954, #7109, #9618, #11830, #11756, #8470, #1256, #178, #6021, #10684, #4882, #14259, #3795, #13112, #5943, #2648, #7327, #11980 ),
 .UNSPECIFIED., .F., .F.,
 ( 4, 2, 2, 2, 2, 2, 2, 2, 2, 4 ),
 ( 4.481635188367946092E-07, 0.003578814135748883529, 0.005367997121863906339, 0.007157180107978928715, 0.008051771601036455950, 0.008946363094093984919, 0.01073554608020907929, 0.01252472906632417539, 0.01341932055938169915, 0.01431391205243922465 ),
 .UNSPECIFIED. ) ;
#6995=CARTESIAN_POINT ( 'NONE',  ( 3.426491571325181340, 1.575000000000000178, -2.360000000000018971 ) ) ;
#6996=VECTOR ( 'NONE', #5520, 39.37007874015748143 ) ;
#7000=DIRECTION ( 'NONE',  ( -1.000000000000000000, -0.000000000000000000, -0.000000000000000000 ) ) ;
#7004=DIRECTION ( 'NONE',  ( 0.000000000000000000, 1.224646799147354933E-16, 1.000000000000000000 ) ) ;
#7007=ADVANCED_FACE ( 'NONE', ( #5307 ), #2659, .F. ) ;
#7012=CARTESIAN_POINT ( 'NONE',  ( 3.426491571325181340, 1.679378605318042395, -1.941878605318058337 ) ) ;
#7014=CARTESIAN_POINT ( 'NONE',  ( 3.612497800988201835, 1.962888430913071414, -0.7027605075283567260 ) ) ;
#7016=ORIENTED_EDGE ( 'NONE', *, *, #12221, .F. ) ;
#7020=CIRCLE ( 'NONE', #10914, 0.4849999999999995981 ) ;
#7027=DIRECTION ( 'NONE',  ( -1.000000000000000000, -0.000000000000000000, -0.000000000000000000 ) ) ;
#7032=CARTESIAN_POINT ( 'NONE',  ( 4.487607086153403202, 1.787994762819255623, -0.4363467488208105372 ) ) ;
#7033=VERTEX_POINT ( 'NONE', #14554 ) ;
#7035=ORIENTED_EDGE ( 'NONE', *, *, #2588, .F. ) ;
#7036=EDGE_CURVE ( 'NONE', #6615, #2564, #3734, .T. ) ;
#7038=ORIENTED_EDGE ( 'NONE', *, *, #11494, .T. ) ;
#7040=ORIENTED_EDGE ( 'NONE', *, *, #3166, .T. ) ;
#7041=ORIENTED_EDGE ( 'NONE', *, *, #1714, .T. ) ;
#7045=DIRECTION ( 'NONE',  ( -0.000000000000000000, -1.000000000000000000, -0.000000000000000000 ) ) ;
#7048=CARTESIAN_POINT ( 'NONE',  ( 3.874999999999999556, 2.782000000000002693, 1.509999999999999787 ) ) ;
#7049=CONICAL_SURFACE ( 'NONE', #4856, 1.039370078740158965, 0.7853981633974517207 ) ;
#7051=CYLINDRICAL_SURFACE ( 'NONE', #2149, 1.000000000000000222 ) ;
#7053=VECTOR ( 'NONE', #4506, 39.37007874015748143 ) ;
#7054=CARTESIAN_POINT ( 'NONE',  ( 3.944129661530210385, 1.761538328845252188, 0.7935532608319412207 ) ) ;
#7055=EDGE_CURVE ( 'NONE', #12114, #3491, #13251, .T. ) ;
#7056=ORIENTED_EDGE ( 'NONE', *, *, #5436, .F. ) ;
#7075=CARTESIAN_POINT ( 'NONE',  ( 6.787121492585022509, 0.000000000000000000, 0.000000000000000000 ) ) ;
#7077=ORIENTED_EDGE ( 'NONE', *, *, #12405, .F. ) ;
#7078=VECTOR ( 'NONE', #8930, 39.37007874015748143 ) ;
#7080=VECTOR ( 'NONE', #13346, 39.37007874015748143 ) ;
#7081=DIRECTION ( 'NONE',  ( -1.000000000000000000, -0.000000000000000000, -0.000000000000000000 ) ) ;
#7086=CONICAL_SURFACE ( 'NONE', #13881, 0.3750000000000004996, 0.7853981633974376209 ) ;
#7088=VECTOR ( 'NONE', #5939, 39.37007874015748854 ) ;
#7094=ADVANCED_FACE ( 'NONE', ( #11270 ), #6456, .T. ) ;
#7096=CARTESIAN_POINT ( 'NONE',  ( 3.651772946692535271, 1.855017273657071586, -0.7749448188891172595 ) ) ;
#7097=VERTEX_POINT ( 'NONE', #13118 ) ;
#7104=DIRECTION ( 'NONE',  ( 0.000000000000000000, 1.000000000000000000, -0.000000000000000000 ) ) ;
#7106=EDGE_CURVE ( 'NONE', #788, #331, #8477, .T. ) ;
#7109=CARTESIAN_POINT ( 'NONE',  ( 3.520930857593272290, 1.966513645793204201, -0.3538087319994585034 ) ) ;
#7111=DIRECTION ( 'NONE',  ( 1.000000000000000000, 0.000000000000000000, 0.000000000000000000 ) ) ;
#7112=AXIS2_PLACEMENT_3D ( 'NONE', #2673, #7345, #11923 ) ;
#7115=CARTESIAN_POINT ( 'NONE',  ( 4.626010065331895404, 1.749087012044151512, -0.03377502978455236560 ) ) ;
#7116=ORIENTED_EDGE ( 'NONE', *, *, #8856, .T. ) ;
#7125=DIRECTION ( 'NONE',  ( 1.000000000000000000, 0.000000000000000000, 0.000000000000000000 ) ) ;
#7126=ADVANCED_FACE ( 'NONE', ( #13548 ), #10768, .T. ) ;
#7128=DIRECTION ( 'NONE',  ( -1.000000000000000000, -0.000000000000000000, -0.000000000000000000 ) ) ;
#7134=FACE_OUTER_BOUND ( 'NONE', #2199, .T. ) ;
#7135=VERTEX_POINT ( 'NONE', #11910 ) ;
#7136=DIRECTION ( 'NONE',  ( -1.000000000000000000, -0.000000000000000000, -0.000000000000000000 ) ) ;
#7138=ORIENTED_EDGE ( 'NONE', *, *, #12678, .T. ) ;
#7139=ORIENTED_EDGE ( 'NONE', *, *, #977, .T. ) ;
#7143=EDGE_LOOP ( 'NONE', ( #7138, #4659 ) ) ;
#7148=CARTESIAN_POINT ( 'NONE',  ( 6.826491571325181695, 3.673940397442060361E-16, -3.000000000000000444 ) ) ;
#7150=EDGE_LOOP ( 'NONE', ( #8071, #1854, #12374, #13734 ) ) ;
#7151=DIRECTION ( 'NONE',  ( 0.000000000000000000, 1.000000000000000000, -0.000000000000000000 ) ) ;
#7152=CARTESIAN_POINT ( 'NONE',  ( 3.400026199384122538, 1.967065180803424740, -0.6696926287964158897 ) ) ;
#7153=AXIS2_PLACEMENT_3D ( 'NONE', #12198, #542, #14417 ) ;
#7154=LINE ( 'NONE', #150, #12270 ) ;
#7155=DIRECTION ( 'NONE',  ( -1.000000000000000000, -0.000000000000000000, -0.000000000000000000 ) ) ;
#7156=VERTEX_POINT ( 'NONE', #1002 ) ;
#7157=DIRECTION ( 'NONE',  ( 0.000000000000000000, 0.000000000000000000, -1.000000000000000000 ) ) ;
#7162=LINE ( 'NONE', #3553, #3677 ) ;
#7170=CARTESIAN_POINT ( 'NONE',  ( 3.426491571325181340, 2.005438169188070052, 0.6189082257615707849 ) ) ;
#7178=LINE ( 'NONE', #8398, #13395 ) ;
#7181=AXIS2_PLACEMENT_3D ( 'NONE', #2505, #5725, #9324 ) ;
#7182=VERTEX_POINT ( 'NONE', #6849 ) ;
#7185=ORIENTED_EDGE ( 'NONE', *, *, #4221, .F. ) ;
#7187=ORIENTED_EDGE ( 'NONE', *, *, #12485, .F. ) ;
#7188=FACE_OUTER_BOUND ( 'NONE', #7421, .T. ) ;
#7190=FACE_BOUND ( 'NONE', #8626, .T. ) ;
#7191=EDGE_LOOP ( 'NONE', ( #13644, #9560 ) ) ;
#7192=CIRCLE ( 'NONE', #6212, 0.2944999999999979301 ) ;
#7194=FACE_OUTER_BOUND ( 'NONE', #8607, .T. ) ;
#7195=EDGE_CURVE ( 'NONE', #5706, #14916, #4541, .T. ) ;
#7196=AXIS2_PLACEMENT_3D ( 'NONE', #5451, #7741, #4226 ) ;
#7197=DIRECTION ( 'NONE',  ( 0.000000000000000000, 0.000000000000000000, -1.000000000000000000 ) ) ;
#7204=CARTESIAN_POINT ( 'NONE',  ( 4.500347009044375568, 1.711009772181913968, 0.5018703121815807355 ) ) ;
#7205=EDGE_CURVE ( 'NONE', #1593, #788, #10108, .T. ) ;
#7212=CARTESIAN_POINT ( 'NONE',  ( 3.875000000000000000, 0.7099999999999984102, 0.4849999999999995981 ) ) ;
#7216=CIRCLE ( 'NONE', #13531, 0.9999999999999996669 ) ;
#7217=CARTESIAN_POINT ( 'NONE',  ( 3.426491571325181340, -2.359999999999984333, 1.575000000000016387 ) ) ;
#7220=ORIENTED_EDGE ( 'NONE', *, *, #6240, .T. ) ;
#7227=VERTEX_POINT ( 'NONE', #13773 ) ;
#7228=AXIS2_PLACEMENT_3D ( 'NONE', #6681, #5387, #5619 ) ;
#7229=VECTOR ( 'NONE', #13079, 39.37007874015748143 ) ;
#7240=ORIENTED_EDGE ( 'NONE', *, *, #7055, .T. ) ;
#7242=ORIENTED_EDGE ( 'NONE', *, *, #6414, .F. ) ;
#7243=ADVANCED_FACE ( 'NONE', ( #3316 ), #3564, .F. ) ;
#7244=VECTOR ( 'NONE', #5521, 39.37007874015748143 ) ;
#7247=AXIS2_PLACEMENT_3D ( 'NONE', #3786, #6930, #11586 ) ;
#7255=AXIS2_PLACEMENT_3D ( 'NONE', #2116, #6801, #3048 ) ;
#7256=CARTESIAN_POINT ( 'NONE',  ( 4.310174322509690015, 1.779561302064900596, -0.6129903542706727215 ) ) ;
#7257=ORIENTED_EDGE ( 'NONE', *, *, #1393, .T. ) ;
#7259=ORIENTED_EDGE ( 'NONE', *, *, #3844, .T. ) ;
#7267=VERTEX_POINT ( 'NONE', #2157 ) ;
#7269=FACE_OUTER_BOUND ( 'NONE', #2364, .T. ) ;
#7276=CARTESIAN_POINT ( 'NONE',  ( 3.574207760192867678, 1.912292896761111471, 0.6869911351339433869 ) ) ;
#7279=ADVANCED_FACE ( 'NONE', ( #9211 ), #5462, .T. ) ;
#7282=LINE ( 'NONE', #10935, #14305 ) ;
#7290=EDGE_LOOP ( 'NONE', ( #12519, #1911, #7574, #2620 ) ) ;
#7294=FACE_OUTER_BOUND ( 'NONE', #6610, .T. ) ;
#7295=DIRECTION ( 'NONE',  ( 0.000000000000000000, 0.000000000000000000, -1.000000000000000000 ) ) ;
#7298=DIRECTION ( 'NONE',  ( -0.7071067811865459074, 0.000000000000000000, 0.7071067811865490160 ) ) ;
#7299=CARTESIAN_POINT ( 'NONE',  ( 3.426491571325181340, 1.679378605318059048, 1.973878605318039492 ) ) ;
#7301=VERTEX_POINT ( 'NONE', #5852 ) ;
#7305=VECTOR ( 'NONE', #1371, 39.37007874015748143 ) ;
#7307=ORIENTED_EDGE ( 'NONE', *, *, #1582, .T. ) ;
#7311=DIRECTION ( 'NONE',  ( 0.000000000000000000, 0.000000000000000000, -1.000000000000000000 ) ) ;
#7313=CARTESIAN_POINT ( 'NONE',  ( 3.426491571325181340, -0.9799999999999989830, -2.359999999999999876 ) ) ;
#7314=AXIS2_PLACEMENT_3D ( 'NONE', #14498, #7624, #10080 ) ;
#7315=EDGE_CURVE ( 'NONE', #6090, #6255, #14793, .T. ) ;
#7316=DIRECTION ( 'NONE',  ( 1.000000000000000000, 0.000000000000000000, 0.000000000000000000 ) ) ;
#7318=ORIENTED_EDGE ( 'NONE', *, *, #8982, .F. ) ;
#7320=VECTOR ( 'NONE', #3603, 39.37007874015748143 ) ;
#7323=CARTESIAN_POINT ( 'NONE',  ( 3.426491571325181340, 0.9799999999999436939, -3.360000000000016751 ) ) ;
#7326=VECTOR ( 'NONE', #13857, 39.37007874015748143 ) ;
#7327=CARTESIAN_POINT ( 'NONE',  ( 3.863498198434387909, 1.886760551146561271, -0.5000000000000004441 ) ) ;
#7332=AXIS2_PLACEMENT_3D ( 'NONE', #13996, #2385, #9356 ) ;
#7341=EDGE_LOOP ( 'NONE', ( #7388, #58, #11635, #14345 ) ) ;
#7344=VECTOR ( 'NONE', #7839, 39.37007874015748854 ) ;
#7345=DIRECTION ( 'NONE',  ( -1.000000000000000000, -0.000000000000000000, -0.000000000000000000 ) ) ;
#7346=CARTESIAN_POINT ( 'NONE',  ( 3.426491571325181340, -2.399999999999999911, 0.7000000000000007327 ) ) ;
#7347=FACE_BOUND ( 'NONE', #13995, .T. ) ;
#7350=CARTESIAN_POINT ( 'NONE',  ( 3.596711980515629570, 1.970780182464999530, 0.6960332242240829803 ) ) ;
#7351=DIRECTION ( 'NONE',  ( 0.000000000000000000, 0.000000000000000000, -1.000000000000000000 ) ) ;
#7352=ORIENTED_EDGE ( 'NONE', *, *, #1667, .T. ) ;
#7354=CARTESIAN_POINT ( 'NONE',  ( 6.826491571325181695, 1.679378605318035733, -1.679378605318065487 ) ) ;
#7358=DIRECTION ( 'NONE',  ( 0.000000000000000000, 0.000000000000000000, 1.000000000000000000 ) ) ;
#7360=ORIENTED_EDGE ( 'NONE', *, *, #12956, .T. ) ;
#7363=EDGE_CURVE ( 'NONE', #3991, #14644, #592, .T. ) ;
#7365=EDGE_CURVE ( 'NONE', #331, #159, #5519, .T. ) ;
#7368=VERTEX_POINT ( 'NONE', #6074 ) ;
#7379=FACE_OUTER_BOUND ( 'NONE', #13045, .T. ) ;
#7380=EDGE_CURVE ( 'NONE', #7890, #2690, #4535, .T. ) ;
#7384=CYLINDRICAL_SURFACE ( 'NONE', #1415, 0.4849999999999995981 ) ;
#7386=EDGE_LOOP ( 'NONE', ( #11174, #9446, #7529, #13104 ) ) ;
#7388=ORIENTED_EDGE ( 'NONE', *, *, #7727, .T. ) ;
#7389=EDGE_CURVE ( 'NONE', #13163, #12635, #11121, .T. ) ;
#7396=CARTESIAN_POINT ( 'NONE',  ( 3.426491571325181784, 1.978195973981552003, -0.6427388825267555950 ) ) ;
#7406=CARTESIAN_POINT ( 'NONE',  ( 4.322740670651102235, 0.9748968923800885866, -0.2231469905907089712 ) ) ;
#7408=VERTEX_POINT ( 'NONE', #1235 ) ;
#7410=CARTESIAN_POINT ( 'NONE',  ( 6.794491571325179891, -1.679378605318048390, 2.054378605318054607 ) ) ;
#7411=DIRECTION ( 'NONE',  ( 0.000000000000000000, 0.000000000000000000, 1.000000000000000000 ) ) ;
#7412=AXIS2_PLACEMENT_3D ( 'NONE', #11534, #11767, #1035 ) ;
#7415=DIRECTION ( 'NONE',  ( 0.000000000000000000, 1.000000000000000000, -0.000000000000000000 ) ) ;
#7418=AXIS2_PLACEMENT_3D ( 'NONE', #7598, #258, #9897 ) ;
#7421=EDGE_LOOP ( 'NONE', ( #9738, #591, #516, #8698, #12661, #1956 ) ) ;
#7428=CARTESIAN_POINT ( 'NONE',  ( 3.426491571325181340, 0.000000000000000000, 0.000000000000000000 ) ) ;
#7430=CONICAL_SURFACE ( 'NONE', #83, 0.2219999999999999751, 0.7853981633974349563 ) ;
#7434=CARTESIAN_POINT ( 'NONE',  ( 2.774999999999999911, 1.679378605318042395, -1.384878605318057732 ) ) ;
#7435=LINE ( 'NONE', #12092, #1998 ) ;
#7442=FACE_OUTER_BOUND ( 'NONE', #9072, .T. ) ;
#7446=DIRECTION ( 'NONE',  ( -1.000000000000000000, -0.000000000000000000, -0.000000000000000000 ) ) ;
#7449=DIRECTION ( 'NONE',  ( 0.000000000000000000, 0.000000000000000000, -1.000000000000000000 ) ) ;
#7451=CONICAL_SURFACE ( 'NONE', #11351, 0.4070000000000025264, 0.7853981633974557175 ) ;
#7463=CARTESIAN_POINT ( 'NONE',  ( 3.426491571325181784, 2.032414231895940393, -0.6051366186278370751 ) ) ;
#7465=AXIS2_PLACEMENT_3D ( 'NONE', #3450, #13914, #12698 ) ;
#7467=CARTESIAN_POINT ( 'NONE',  ( 4.422240817987284522, 1.782290669966776209, -0.5151263722802654765 ) ) ;
#7471=ORIENTED_EDGE ( 'NONE', *, *, #5411, .F. ) ;
#7472=VECTOR ( 'NONE', #7921, 39.37007874015748143 ) ;
#7473=ORIENTED_EDGE ( 'NONE', *, *, #7195, .T. ) ;
#7475=CARTESIAN_POINT ( 'NONE',  ( 4.769268701363833074, 2.750000000000000000, 0.3249191361593796734 ) ) ;
#7478=FACE_OUTER_BOUND ( 'NONE', #7341, .T. ) ;
#7487=CARTESIAN_POINT ( 'NONE',  ( 3.875000000000000000, 3.137999999999999901, 0.5000000000000002220 ) ) ;
#7488=EDGE_CURVE ( 'NONE', #10132, #1776, #1829, .T. ) ;
#7490=CARTESIAN_POINT ( 'NONE',  ( 3.497790632039259329, 1.947309111526952963, 0.6487173296532952049 ) ) ;
#7496=ORIENTED_EDGE ( 'NONE', *, *, #12925, .F. ) ;
#7507=DIRECTION ( 'NONE',  ( 0.000000000000000000, 0.000000000000000000, -1.000000000000000000 ) ) ;
#7511=FACE_OUTER_BOUND ( 'NONE', #5831, .T. ) ;
#7512=VERTEX_POINT ( 'NONE', #6374 ) ;
#7513=CARTESIAN_POINT ( 'NONE',  ( 6.215861650065340527, 0.000000000000000000, 0.000000000000000000 ) ) ;
#7519=CARTESIAN_POINT ( 'NONE',  ( 6.208491571325183145, 1.679378605318035733, -1.304378605318064821 ) ) ;
#7521=ADVANCED_FACE ( 'NONE', ( #9737 ), #2083, .F. ) ;
#7524=CARTESIAN_POINT ( 'NONE',  ( 6.794491571325179891, -1.679378605318047946, -1.679378605318053497 ) ) ;
#7525=ORIENTED_EDGE ( 'NONE', *, *, #7205, .F. ) ;
#7529=ORIENTED_EDGE ( 'NONE', *, *, #2265, .F. ) ;
#7530=CARTESIAN_POINT ( 'NONE',  ( 2.814370078740158210, 1.224646799147353207E-16, -1.000000000000000000 ) ) ;
#7531=DIRECTION ( 'NONE',  ( 0.000000000000000000, 0.000000000000000000, 1.000000000000000000 ) ) ;
#7535=CARTESIAN_POINT ( 'NONE',  ( 4.620520747435304720, 1.809297920034194984, -0.09820618556490041950 ) ) ;
#7541=AXIS2_PLACEMENT_3D ( 'NONE', #7581, #12240, #7507 ) ;
#7542=CIRCLE ( 'NONE', #10235, 0.7500000000000001110 ) ;
#7543=ORIENTED_EDGE ( 'NONE', *, *, #546, .T. ) ;
#7544=VERTEX_POINT ( 'NONE', #11173 ) ;
#7549=CARTESIAN_POINT ( 'NONE',  ( 4.271631709730848492, 0.9523919498644370929, 0.3061575615593492561 ) ) ;
#7551=VERTEX_POINT ( 'NONE', #13381 ) ;
#7553=FACE_OUTER_BOUND ( 'NONE', #11294, .T. ) ;
#7561=CARTESIAN_POINT ( 'NONE',  ( 3.874999999999999556, 2.750000000000000000, -1.320000000000000062 ) ) ;
#7562=LINE ( 'NONE', #1585, #7675 ) ;
#7566=DIRECTION ( 'NONE',  ( 0.000000000000000000, 0.000000000000000000, 1.000000000000000000 ) ) ;
#7573=CARTESIAN_POINT ( 'NONE',  ( 3.426491571325181340, 1.679378605318042395, -1.973878605318056367 ) ) ;
#7574=ORIENTED_EDGE ( 'NONE', *, *, #9048, .T. ) ;
#7577=ADVANCED_FACE ( 'NONE', ( #7511 ), #1688, .F. ) ;
#7581=CARTESIAN_POINT ( 'NONE',  ( 6.176491571325181340, -1.679378605318047946, -1.679378605318053497 ) ) ;
#7585=CARTESIAN_POINT ( 'NONE',  ( 4.007132756949598473, 0.8754566745458228771, -0.4833557680116081778 ) ) ;
#7590=CARTESIAN_POINT ( 'NONE',  ( 3.874999999999999556, 3.137999999999999901, 1.320000000000000062 ) ) ;
#7592=EDGE_CURVE ( 'NONE', #8434, #4931, #14064, .T. ) ;
#7598=CARTESIAN_POINT ( 'NONE',  ( 3.426491571325181340, -1.679378605318041950, 1.679378605318059048 ) ) ;
#7603=EDGE_LOOP ( 'NONE', ( #1495, #9173, #14621, #2627 ) ) ;
#7605=FACE_OUTER_BOUND ( 'NONE', #15095, .T. ) ;
#7606=EDGE_CURVE ( 'NONE', #3928, #7512, #3073, .T. ) ;
#7609=CARTESIAN_POINT ( 'NONE',  ( 4.626583745745669773, 1.810565237260122418, -0.02390113810800691824 ) ) ;
#7613=ORIENTED_EDGE ( 'NONE', *, *, #6068, .F. ) ;
#7614=B_SPLINE_CURVE_WITH_KNOTS ( 'NONE', 3,
 ( #4220, #2135, #11400, #13526, #9189, #6828, #10330, #14992, #8882, #3068, #7735, #12390, #1906, #6594, #5444, #10110, #14763, #2604, #11785, #12924, #4908, #9574, #5904, #9347, #14218, #13985, #2292, #8202, #8360, #1285, #11858, #10634, #1214, #1135, #5827, #12842, #8283, #1359, #12764, #206, #3448, #7204, #10560, #4676, #2375, #10489, #3521, #11555, #1057, #5745, #10411, #15073, #3682, #6049, #12993, #7054 ),
 .UNSPECIFIED., .F., .F.,
 ( 4, 2, 2, 2, 2, 2, 2, 2, 2, 2, 2, 2, 2, 2, 2, 2, 2, 2, 2, 2, 2, 2, 2, 2, 2, 2, 2, 4 ),
 ( 0.000000000000000000, 0.001913177148301513928, 0.003826354296603027855, 0.005739531444904541133, 0.007652708593206055711, 0.01147906288980911349, 0.01339224003811062894, 0.01530541718641214612, 0.01913177148301517527, 0.02104494863131669072, 0.02295812577961820616, 0.02678448007622125787, 0.02774106865037202080, 0.02869765722452279066, 0.03061083437282431305, 0.03443718866942736129, 0.03539377724357812421, 0.03635036581772889408, 0.03826354296603043381, 0.04208989726263349940, 0.04400307441093503219, 0.04591625155923656498, 0.04782942870753809778, 0.04974260585583962363, 0.05356896015244266840, 0.05548213730074420813, 0.05739531444904575480, 0.06122166874564884120 ),
 .UNSPECIFIED. ) ;
#7616=ADVANCED_FACE ( 'NONE', ( #9192 ), #13805, .F. ) ;
#7618=CARTESIAN_POINT ( 'NONE',  ( 3.958015244391202447, 0.8698464393224263347, 0.4933369105775312069 ) ) ;
#7624=DIRECTION ( 'NONE',  ( -0.9396926207859107594, 0.000000000000000000, 0.3420201433256624401 ) ) ;
#7629=CARTESIAN_POINT ( 'NONE',  ( 3.893742162958262032, 1.774205514365693181, 0.7983174907408143728 ) ) ;
#7635=DIRECTION ( 'NONE',  ( -1.000000000000000000, -0.000000000000000000, -0.000000000000000000 ) ) ;
#7639=EDGE_CURVE ( 'NONE', #13316, #6459, #3373, .T. ) ;
#7643=VERTEX_POINT ( 'NONE', #10332 ) ;
#7652=CARTESIAN_POINT ( 'NONE',  ( 3.426491571325181340, 1.679378605318042395, -1.384878605318061062 ) ) ;
#7654=CARTESIAN_POINT ( 'NONE',  ( 2.527624975756972425, 2.750000000000000000, 0.9199802545633498640 ) ) ;
#7658=CARTESIAN_POINT ( 'NONE',  ( 4.205440198960407550, 0.9266839483850188852, -0.3766322587779434850 ) ) ;
#7659=DIRECTION ( 'NONE',  ( 0.000000000000000000, 0.000000000000000000, -1.000000000000000000 ) ) ;
#7662=FACE_OUTER_BOUND ( 'NONE', #12191, .T. ) ;
#7664=EDGE_CURVE ( 'NONE', #12484, #7097, #982, .T. ) ;
#7671=LINE ( 'NONE', #3170, #10387 ) ;
#7675=VECTOR ( 'NONE', #2821, 39.37007874015748854 ) ;
#7676=DIRECTION ( 'NONE',  ( -1.000000000000000000, -0.000000000000000000, -0.000000000000000000 ) ) ;
#7680=CARTESIAN_POINT ( 'NONE',  ( 3.426491571325181340, -3.000039370078740220, -0.5999481385559802815 ) ) ;
#7682=DIRECTION ( 'NONE',  ( 0.000000000000000000, 0.000000000000000000, -1.000000000000000000 ) ) ;
#7684=CARTESIAN_POINT ( 'NONE',  ( 3.426491571325181340, 2.015586091437299388, -0.6121388925861622754 ) ) ;
#7687=EDGE_LOOP ( 'NONE', ( #943, #13542, #11868, #12786 ) ) ;
#7688=EDGE_CURVE ( 'NONE', #6864, #4931, #11255, .T. ) ;
#7689=CARTESIAN_POINT ( 'NONE',  ( 4.198116201031909078, 1.736978055819331512, -0.6778351007205051237 ) ) ;
#7692=AXIS2_PLACEMENT_3D ( 'NONE', #9774, #9925, #13342 ) ;
#7695=CIRCLE ( 'NONE', #583, 0.4070000000000025264 ) ;
#7698=CARTESIAN_POINT ( 'NONE',  ( 4.375014056583601096, 1.000007028289835675, -0.01611911748198105107 ) ) ;
#7703=LINE ( 'NONE', #4109, #5344 ) ;
#7704=CARTESIAN_POINT ( 'NONE',  ( 3.876560711617219379, 1.855806856933289950, 0.7500000000000001110 ) ) ;
#7707=VECTOR ( 'NONE', #7803, 39.37007874015748143 ) ;
#7708=CIRCLE ( 'NONE', #14782, 0.07999999999999996003 ) ;
#7711=CARTESIAN_POINT ( 'NONE',  ( 3.836102718394629019, 1.791032951870848544, 0.7985211043516597940 ) ) ;
#7712=CARTESIAN_POINT ( 'NONE',  ( 3.631360142079332665, 1.967959863695790457, -0.4367743950684919718 ) ) ;
#7714=VERTEX_POINT ( 'NONE', #13756 ) ;
#7716=EDGE_LOOP ( 'NONE', ( #6440, #7943, #11, #4189 ) ) ;
#7717=ORIENTED_EDGE ( 'NONE', *, *, #14185, .T. ) ;
#7727=EDGE_CURVE ( 'NONE', #1043, #9581, #1109, .T. ) ;
#7730=ORIENTED_EDGE ( 'NONE', *, *, #6693, .T. ) ;
#7732=ADVANCED_FACE ( 'NONE', ( #7816 ), #7977, .F. ) ;
#7735=CARTESIAN_POINT ( 'NONE',  ( 4.313738930246985070, 1.707933241827553683, -0.6660024015622548754 ) ) ;
#7741=DIRECTION ( 'NONE',  ( -1.000000000000000000, -0.000000000000000000, -0.000000000000000000 ) ) ;
#7742=ORIENTED_EDGE ( 'NONE', *, *, #12642, .T. ) ;
#7743=AXIS2_PLACEMENT_3D ( 'NONE', #11444, #6702, #6475 ) ;
#7745=LENGTH_MEASURE_WITH_UNIT ( LENGTH_MEASURE( 0.02539999999999999897 ), #1922 );
#7753=CARTESIAN_POINT ( 'NONE',  ( 3.876560711617219379, -3.000039370078740220, 0.000000000000000000 ) ) ;
#7758=CARTESIAN_POINT ( 'NONE',  ( 3.944129661530210385, 0.000000000000000000, 0.000000000000000000 ) ) ;
#7763=EDGE_CURVE ( 'NONE', #6255, #4759, #9648, .T. ) ;
#7769=CARTESIAN_POINT ( 'NONE',  ( 4.233629482522627718, 1.713288744528204788, -0.7097370609146418374 ) ) ;
#7770=ORIENTED_EDGE ( 'NONE', *, *, #5314, .T. ) ;
#7772=ORIENTED_EDGE ( 'NONE', *, *, #4030, .F. ) ;
#7773=AXIS2_PLACEMENT_3D ( 'NONE', #5042, #12140, #14494 ) ;
#7774=DIRECTION ( 'NONE',  ( 0.000000000000000000, 1.000000000000000000, -0.000000000000000000 ) ) ;
#7783=ADVANCED_FACE ( 'NONE', ( #1289 ), #10713, .F. ) ;
#7791=AXIS2_PLACEMENT_3D ( 'NONE', #8784, #5338, #8857 ) ;
#7792=CARTESIAN_POINT ( 'NONE',  ( 4.159006841833645218, 1.720943226083167188, 0.7430362912831911526 ) ) ;
#7793=LINE ( 'NONE', #14820, #13280 ) ;
#7796=CARTESIAN_POINT ( 'NONE',  ( 3.875000000000000000, 1.112678268764263789, 0.000000000000000000 ) ) ;
#7797=EDGE_LOOP ( 'NONE', ( #8478, #14891, #10674, #1621 ) ) ;
#7801=CARTESIAN_POINT ( 'NONE',  ( 3.426491571325181340, 0.000000000000000000, 0.000000000000000000 ) ) ;
#7803=DIRECTION ( 'NONE',  ( -0.000000000000000000, -1.000000000000000000, -0.000000000000000000 ) ) ;
#7806=CARTESIAN_POINT ( 'NONE',  ( 3.426491571325181340, -1.679378605318059048, -1.679378605318041950 ) ) ;
#7809=ORIENTED_EDGE ( 'NONE', *, *, #1714, .F. ) ;
#7812=CARTESIAN_POINT ( 'NONE',  ( 3.623103638349538524, 0.9015510240917827822, -0.4331298522267356677 ) ) ;
#7814=CONICAL_SURFACE ( 'NONE', #4903, 0.3750000000000004996, 0.7853981633974547183 ) ;
#7816=FACE_OUTER_BOUND ( 'NONE', #10417, .T. ) ;
#7821=AXIS2_PLACEMENT_3D ( 'NONE', #122, #2448, #7411 ) ;
#7822=CARTESIAN_POINT ( 'NONE',  ( 3.426491571325181340, -0.9799999999999436939, 2.360000000000016307 ) ) ;
#7827=DIRECTION ( 'NONE',  ( 0.000000000000000000, 0.000000000000000000, 1.000000000000000000 ) ) ;
#7828=B_SPLINE_CURVE_WITH_KNOTS ( 'NONE', 3,
 ( #3293, #7882, #14839, #11169, #12611, #2133, #5443, #670, #7812, #14762, #13604, #10188, #3150, #1980, #979, #8881, #10038, #6665, #12388, #5670, #6826, #11479, #14694, #4219, #4373, #13525, #3066, #9039, #1904, #6593, #12534, #11554, #8048, #5744, #1213, #9497, #10410, #8281, #6973, #2291, #15072, #2374, #2453, #4517, #12923, #11632, #12695, #14062, #5903, #9188, #10559, #14147 ),
 .UNSPECIFIED., .F., .F.,
 ( 4, 2, 2, 2, 2, 2, 2, 2, 2, 2, 2, 2, 2, 2, 2, 2, 2, 2, 2, 2, 2, 2, 2, 2, 2, 4 ),
 ( 0.000000000000000000, 0.002524598796828807657, 0.003786898195243190886, 0.005049197593657573681, 0.007573796390486340138, 0.008836095788900722933, 0.01009839518731510573, 0.01136069458572948852, 0.01262299398414387305, 0.01514759278097261783, 0.01640989217938699368, 0.01767219157780136607, 0.02019679037463009696, 0.02145908977304446935, 0.02272138917145883827, 0.02398368856987320719, 0.02524598796828757610, 0.02777058676511630700, 0.02903288616353066204, 0.03029518556194501361, 0.03281978435877375144, 0.03408208375718813771, 0.03534438315560252397, 0.03660668255401691024, 0.03786898195243129650, 0.04039358074926006209 ),
 .UNSPECIFIED. ) ;
#7833=FACE_OUTER_BOUND ( 'NONE', #13117, .T. ) ;
#7839=DIRECTION ( 'NONE',  ( -0.7071067811865459074, 8.659560562354951347E-17, -0.7071067811865490160 ) ) ;
#7840=CARTESIAN_POINT ( 'NONE',  ( 3.631700695736539863, 1.967759286096487203, 0.4374246074370377046 ) ) ;
#7841=VECTOR ( 'NONE', #7027, 39.37007874015748143 ) ;
#7845=ADVANCED_FACE ( 'NONE', ( #8129 ), #9454, .F. ) ;
#7846=CARTESIAN_POINT ( 'NONE',  ( 4.215636577467320123, 1.714906460358956553, -0.7183765618090157679 ) ) ;
#7847=ORIENTED_EDGE ( 'NONE', *, *, #10103, .T. ) ;
#7850=AXIS2_PLACEMENT_3D ( 'NONE', #13806, #8018, #3801 ) ;
#7852=CARTESIAN_POINT ( 'NONE',  ( 6.176491571325181340, -1.679378605318048390, 1.272378605318051914 ) ) ;
#7854=DIRECTION ( 'NONE',  ( 1.000000000000000000, 0.000000000000000000, 0.000000000000000000 ) ) ;
#7856=CARTESIAN_POINT ( 'NONE',  ( 3.193060682217703228, 2.480829671764972044, -0.3101105498922617221 ) ) ;
#7862=CARTESIAN_POINT ( 'NONE',  ( 4.039574151569903293, 1.760598961795517781, 0.7330370523027112117 ) ) ;
#7863=CARTESIAN_POINT ( 'NONE',  ( 3.447700738689755795, 2.048569235149967582, -0.2640414659212462767 ) ) ;
#7864=EDGE_LOOP ( 'NONE', ( #2196, #4152, #13589, #13949 ) ) ;
#7867=PLANE ( 'NONE',  #8711 ) ;
#7868=ORIENTED_EDGE ( 'NONE', *, *, #1632, .F. ) ;
#7874=CARTESIAN_POINT ( 'NONE',  ( 6.794491571325179891, 1.679378605318035733, -1.304378605318064821 ) ) ;
#7882=CARTESIAN_POINT ( 'NONE',  ( 3.841336337880575158, 0.8660254037844382635, -0.5000000000000001110 ) ) ;
#7885=CARTESIAN_POINT ( 'NONE',  ( 4.083279076927434303, 0.8905985393163902142, -0.4548455386991649974 ) ) ;
#7890=VERTEX_POINT ( 'NONE', #9350 ) ;
#7891=DIRECTION ( 'NONE',  ( 0.000000000000000000, 0.000000000000000000, -1.000000000000000000 ) ) ;
#7893=LINE ( 'NONE', #7822, #3720 ) ;
#7894=CARTESIAN_POINT ( 'NONE',  ( 3.426491571325181340, -1.575000000000027489, -2.359999999999986109 ) ) ;
#7898=CARTESIAN_POINT ( 'NONE',  ( 3.874999999999999556, 2.782000000000000917, -1.130000000000000560 ) ) ;
#7899=CARTESIAN_POINT ( 'NONE',  ( 2.774999999999999911, 1.679378605318042395, -1.679378605318058604 ) ) ;
#7902=CARTESIAN_POINT ( 'NONE',  ( 6.826491571325181695, -1.679378605318048390, 1.679378605318054163 ) ) ;
#7904=CARTESIAN_POINT ( 'NONE',  ( 4.344846310392954436, 3.137999999999999901, 1.491010071662831171 ) ) ;
#7905=ORIENTED_EDGE ( 'NONE', *, *, #680, .F. ) ;
#7907=DIRECTION ( 'NONE',  ( 0.000000000000000000, 0.000000000000000000, 1.000000000000000000 ) ) ;
#7911=CARTESIAN_POINT ( 'NONE',  ( 3.652054291836392075, 1.959738311896082497, 0.4481273458576563451 ) ) ;
#7913=CARTESIAN_POINT ( 'NONE',  ( 2.774999999999999911, 1.679378605318059048, 1.679378605318041506 ) ) ;
#7914=CIRCLE ( 'NONE', #2034, 0.3750000000000004996 ) ;
#7917=ADVANCED_FACE ( 'NONE', ( #14294 ), #1516, .F. ) ;
#7918=CARTESIAN_POINT ( 'NONE',  ( 3.946809452279758101, 1.834510758173002687, -0.7469057171082090774 ) ) ;
#7921=DIRECTION ( 'NONE',  ( -0.000000000000000000, -1.000000000000000000, -0.000000000000000000 ) ) ;
#7924=EDGE_CURVE ( 'NONE', #4727, #14644, #6266, .T. ) ;
#7929=CARTESIAN_POINT ( 'NONE',  ( 3.875000000000000000, 1.059999999999999165, 0.000000000000000000 ) ) ;
#7931=AXIS2_PLACEMENT_3D ( 'NONE', #13210, #12004, #14365 ) ;
#7932=CARTESIAN_POINT ( 'NONE',  ( 3.426491571325181340, 2.426945040795776443, -0.5999481385559803925 ) ) ;
#7937=CARTESIAN_POINT ( 'NONE',  ( 4.463949327178305282, 1.785655382754484766, 0.4666876780364017652 ) ) ;
#7940=VECTOR ( 'NONE', #4763, 39.37007874015748143 ) ;
#7941=ORIENTED_EDGE ( 'NONE', *, *, #6196, .F. ) ;
#7942=FACE_OUTER_BOUND ( 'NONE', #14866, .T. ) ;
#7943=ORIENTED_EDGE ( 'NONE', *, *, #3660, .F. ) ;
#7950=ADVANCED_FACE ( 'NONE', ( #2683, #3971, #12008, #6356, #6278 ), #503, .T. ) ;
#7961=CARTESIAN_POINT ( 'NONE',  ( 3.875000000000619504, 1.884022191776286714, 0.5000000000000002220 ) ) ;
#7965=CYLINDRICAL_SURFACE ( 'NONE', #4289, 0.9999999999999994449 ) ;
#7967=VERTEX_POINT ( 'NONE', #12227 ) ;
#7970=B_SPLINE_CURVE_WITH_KNOTS ( 'NONE', 3,
 ( #3246, #11279, #3406, #8082, #14949, #4472, #12644, #7911, #7840, #2249, #6692, #6857, #12562, #2087, #6775, #11431 ),
 .UNSPECIFIED., .F., .F.,
 ( 4, 2, 2, 2, 2, 2, 2, 4 ),
 ( 0.001808351910784379481, 0.003649056555375718418, 0.005489761199967057789, 0.007330465844558396726, 0.009171170489149735663, 0.01285257977833238058, 0.01469328442292372125, 0.01653398906751506192 ),
 .UNSPECIFIED. ) ;
#7975=ADVANCED_FACE ( 'NONE', ( #6422, #428 ), #2974, .F. ) ;
#7976=ADVANCED_FACE ( 'NONE', ( #6201 ), #14310, .F. ) ;
#7977=TOROIDAL_SURFACE ( 'NONE', #129, 1.580000000000000071, 0.08000000000000000167 ) ;
#7979=DIRECTION ( 'NONE',  ( 1.000000000000000000, 0.000000000000000000, 0.000000000000000000 ) ) ;
#7980=LINE ( 'NONE', #10197, #2145 ) ;
#7986=DIRECTION ( 'NONE',  ( 0.000000000000000000, 0.000000000000000000, 1.000000000000000000 ) ) ;
#7987=EDGE_LOOP ( 'NONE', ( #7041, #9628, #9585, #12019 ) ) ;
#7999=CARTESIAN_POINT ( 'NONE',  ( 3.688348485839861635, 1.864810863078529168, -0.7265032220550791120 ) ) ;
#8001=AXIS2_PLACEMENT_3D ( 'NONE', #2365, #10550, #1349 ) ;
#8010=CARTESIAN_POINT ( 'NONE',  ( 3.403212434743930537, 2.431262081689471444, -0.5824845941018170770 ) ) ;
#8012=EDGE_CURVE ( 'NONE', #10024, #8675, #4815, .T. ) ;
#8016=DIRECTION ( 'NONE',  ( 0.000000000000000000, 0.000000000000000000, 1.000000000000000000 ) ) ;
#8018=DIRECTION ( 'NONE',  ( -0.000000000000000000, 1.000000000000000000, -0.000000000000000000 ) ) ;
#8019=CARTESIAN_POINT ( 'NONE',  ( 3.944129661530210385, 0.000000000000000000, 0.000000000000000000 ) ) ;
#8020=EDGE_CURVE ( 'NONE', #1969, #3733, #8473, .T. ) ;
#8022=CARTESIAN_POINT ( 'NONE',  ( 4.621713608558009945, 1.748414620571773881, -0.08698231708713202726 ) ) ;
#8027=VERTEX_POINT ( 'NONE', #8574 ) ;
#8036=LINE ( 'NONE', #14984, #6244 ) ;
#8037=DIRECTION ( 'NONE',  ( 0.7071067811865551223, 8.659560562354841646E-17, 0.7071067811865400232 ) ) ;
#8044=CIRCLE ( 'NONE', #2408, 3.000000000000000444 ) ;
#8048=CARTESIAN_POINT ( 'NONE',  ( 3.407628221657749368, 0.9840755583697731179, 0.1784229389202373339 ) ) ;
#8050=CARTESIAN_POINT ( 'NONE',  ( 3.586764729049507050, 1.881086719192986534, -0.7575506356649558404 ) ) ;
#8052=CIRCLE ( 'NONE', #4618, 1.932031071636253650 ) ;
#8053=DIRECTION ( 'NONE',  ( -1.000000000000000000, -0.000000000000000000, -0.000000000000000000 ) ) ;
#8057=CIRCLE ( 'NONE', #3650, 0.2945000000000006501 ) ;
#8058=EDGE_CURVE ( 'NONE', #4107, #5449, #9937, .T. ) ;
#8064=LINE ( 'NONE', #994, #4027 ) ;
#8071=ORIENTED_EDGE ( 'NONE', *, *, #14249, .F. ) ;
#8073=EDGE_LOOP ( 'NONE', ( #631, #12380, #12677, #7352 ) ) ;
#8074=CARTESIAN_POINT ( 'NONE',  ( 3.875000000000000000, 3.137999999999999901, 0.5000000000000002220 ) ) ;
#8078=ORIENTED_EDGE ( 'NONE', *, *, #4284, .F. ) ;
#8082=CARTESIAN_POINT ( 'NONE',  ( 3.782641550552467535, 1.913069021635787736, 0.4919429857632933722 ) ) ;
#8084=CARTESIAN_POINT ( 'NONE',  ( 3.725142412237626655, 1.827585193579217782, -0.7892246468208887755 ) ) ;
#8088=CARTESIAN_POINT ( 'NONE',  ( 3.426491571325181340, 2.021150388955688548, 0.6098287289117807486 ) ) ;
#8091=EDGE_CURVE ( 'NONE', #13105, #2938, #2850, .T. ) ;
#8096=DIRECTION ( 'NONE',  ( 0.000000000000000000, 0.000000000000000000, -1.000000000000000000 ) ) ;
#8100=AXIS2_PLACEMENT_3D ( 'NONE', #7524, #841, #2156 ) ;
#8101=CARTESIAN_POINT ( 'NONE',  ( 4.585279783993691183, 1.802421112337721398, 0.2480258495191786094 ) ) ;
#8104=ORIENTED_EDGE ( 'NONE', *, *, #3931, .F. ) ;
#8113=CARTESIAN_POINT ( 'NONE',  ( 3.874999999999999556, 3.137999999999999901, -1.820000000000000284 ) ) ;
#8114=FACE_OUTER_BOUND ( 'NONE', #11810, .T. ) ;
#8124=ADVANCED_FACE ( 'NONE', ( #4352, #4277, #3203, #881 ), #7867, .T. ) ;
#8129=FACE_OUTER_BOUND ( 'NONE', #15053, .T. ) ;
#8130=EDGE_LOOP ( 'NONE', ( #12701, #6685, #11517, #1862 ) ) ;
#8134=EDGE_CURVE ( 'NONE', #9926, #3188, #8868, .T. ) ;
#8136=AXIS2_PLACEMENT_3D ( 'NONE', #4063, #12170, #13301 ) ;
#8137=CARTESIAN_POINT ( 'NONE',  ( 3.426491571325181340, 0.000000000000000000, 0.000000000000000000 ) ) ;
#8141=CONICAL_SURFACE ( 'NONE', #14473, 1.932031071636253650, 0.2617993877991429685 ) ;
#8142=DIRECTION ( 'NONE',  ( -1.000000000000000000, -0.000000000000000000, -0.000000000000000000 ) ) ;
#8145=ORIENTED_EDGE ( 'NONE', *, *, #8806, .F. ) ;
#8146=CARTESIAN_POINT ( 'NONE',  ( 3.426491571325181340, 0.000000000000000000, 0.000000000000000000 ) ) ;
#8157=CYLINDRICAL_SURFACE ( 'NONE', #9456, 0.3750000000000004996 ) ;
#8159=CARTESIAN_POINT ( 'NONE',  ( 3.692149047776956294, 1.926320256218450711, -0.7271669092250208077 ) ) ;
#8163=PRODUCT_DEFINITION_CONTEXT ( 'detailed design', #6858, 'design' ) ;
#8165=VERTEX_POINT ( 'NONE', #10166 ) ;
#8173=AXIS2_PLACEMENT_3D ( 'NONE', #14585, #4117, #13431 ) ;
#8174=DIRECTION ( 'NONE',  ( 0.000000000000000000, 1.000000000000000000, 0.000000000000000000 ) ) ;
#8175=ADVANCED_FACE ( 'NONE', ( #7942 ), #12593, .T. ) ;
#8177=CARTESIAN_POINT ( 'NONE',  ( 4.671837851815657139, 1.730935268799050686, -0.1503661639408108985 ) ) ;
#8180=ORIENTED_EDGE ( 'NONE', *, *, #14266, .T. ) ;
#8182=AXIS2_PLACEMENT_3D ( 'NONE', #3753, #2526, #8423 ) ;
#8185=EDGE_LOOP ( 'NONE', ( #14882, #9509, #9768, #207 ) ) ;
#8188=CARTESIAN_POINT ( 'NONE',  ( 3.405153689607044232, 3.137999999999999901, 1.491010071662831171 ) ) ;
#8189=VERTEX_POINT ( 'NONE', #5655 ) ;
#8192=CARTESIAN_POINT ( 'NONE',  ( 2.774999999999999911, 2.359999999999994547, -1.575000000000016831 ) ) ;
#8199=DIRECTION ( 'NONE',  ( 0.000000000000000000, 0.000000000000000000, 1.000000000000000000 ) ) ;
#8202=CARTESIAN_POINT ( 'NONE',  ( 4.684642132697897310, 1.733077758969720383, -0.04970726437145756710 ) ) ;
#8204=CARTESIAN_POINT ( 'NONE',  ( 6.176491571325181340, -1.679378605318048390, 1.679378605318054163 ) ) ;
#8207=VERTEX_POINT ( 'NONE', #10023 ) ;
#8211=EDGE_LOOP ( 'NONE', ( #6102, #10540, #9460, #14982 ) ) ;
#8213=CIRCLE ( 'NONE', #4783, 0.07999999999999996003 ) ;
#8215=EDGE_CURVE ( 'NONE', #9027, #13119, #9559, .T. ) ;
#8217=CARTESIAN_POINT ( 'NONE',  ( 3.875000000000000000, 3.137999999999999901, -0.5000000000000002220 ) ) ;
#8219=CARTESIAN_POINT ( 'NONE',  ( 6.787121492585022509, 0.000000000000000000, 0.000000000000000000 ) ) ;
#8220=ORIENTED_EDGE ( 'NONE', *, *, #10558, .T. ) ;
#8223=DIRECTION ( 'NONE',  ( 0.000000000000000000, -1.000000000000000000, 1.836536466328828134E-14 ) ) ;
#8226=CIRCLE ( 'NONE', #15047, 0.7849999999999958122 ) ;
#8229=DIRECTION ( 'NONE',  ( 1.000000000000000000, 0.000000000000000000, 0.000000000000000000 ) ) ;
#8230=ORIENTED_EDGE ( 'NONE', *, *, #11996, .F. ) ;
#8231=DIRECTION ( 'NONE',  ( 0.000000000000000000, 0.000000000000000000, 1.000000000000000000 ) ) ;
#8242=CARTESIAN_POINT ( 'NONE',  ( 4.006803276264902181, 1.767389175965520032, -0.7395693964154066435 ) ) ;
#8245=EDGE_CURVE ( 'NONE', #11008, #15105, #1268, .T. ) ;
#8246=CARTESIAN_POINT ( 'NONE',  ( 2.774999999999999911, -1.574999999999984190, 1.575000000000033040 ) ) ;
#8247=VERTEX_POINT ( 'NONE', #9327 ) ;
#8254=ORIENTED_EDGE ( 'NONE', *, *, #9096, .T. ) ;
#8256=CONICAL_SURFACE ( 'NONE', #7743, 0.1899999999999996136, 0.7853981633974433940 ) ;
#8258=CARTESIAN_POINT ( 'NONE',  ( 5.567023771132172172, 0.000000000000000000, 0.000000000000000000 ) ) ;
#8259=CONICAL_SURFACE ( 'NONE', #13593, 0.2625000000000000111, 0.7853981633974503884 ) ;
#8261=CARTESIAN_POINT ( 'NONE',  ( 4.573996505429533954, 1.741627621165780626, 0.2781619901565121067 ) ) ;
#8263=CARTESIAN_POINT ( 'NONE',  ( 6.794491571325179891, -1.679378605318047946, -2.054378605318054163 ) ) ;
#8266=CARTESIAN_POINT ( 'NONE',  ( 6.826491571325181695, 3.625725956530744935E-16, -2.960629921259841257 ) ) ;
#8267=ORIENTED_EDGE ( 'NONE', *, *, #3639, .T. ) ;
#8269=CYLINDRICAL_SURFACE ( 'NONE', #9219, 0.5000000000000001110 ) ;
#8272=FACE_BOUND ( 'NONE', #2381, .T. ) ;
#8273=ORIENTED_EDGE ( 'NONE', *, *, #2065, .F. ) ;
#8280=CARTESIAN_POINT ( 'NONE',  ( 6.176491571325181340, 1.679378605318059492, 1.679378605318041506 ) ) ;
#8281=CARTESIAN_POINT ( 'NONE',  ( 3.499818328484842755, 0.9437543736653750681, 0.3309102127597038367 ) ) ;
#8283=CARTESIAN_POINT ( 'NONE',  ( 4.637971095798543608, 1.725702751024853931, 0.2671971766050545427 ) ) ;
#8285=CARTESIAN_POINT ( 'NONE',  ( 3.875000000000000000, 1.112678268764263789, 0.000000000000000000 ) ) ;
#8291=DIRECTION ( 'NONE',  ( -1.000000000000000000, -0.000000000000000000, -0.000000000000000000 ) ) ;
#8294=VECTOR ( 'NONE', #14337, 39.37007874015748143 ) ;
#8299=VECTOR ( 'NONE', #11967, 39.37007874015748143 ) ;
#8303=VERTEX_POINT ( 'NONE', #1197 ) ;
#8306=CARTESIAN_POINT ( 'NONE',  ( 6.826491571325181695, -1.679378605318048390, 1.304378605318053497 ) ) ;
#8308=ORIENTED_EDGE ( 'NONE', *, *, #1820, .F. ) ;
#8315=ORIENTED_EDGE ( 'NONE', *, *, #11350, .F. ) ;
#8319=VECTOR ( 'NONE', #13658, 39.37007874015748143 ) ;
#8332=DIRECTION ( 'NONE',  ( 0.000000000000000000, -1.000000000000000000, 4.591341165821855765E-15 ) ) ;
#8333=CARTESIAN_POINT ( 'NONE',  ( 3.426491571325181340, 3.360000000000016751, 0.9799999999999461364 ) ) ;
#8338=LINE ( 'NONE', #2499, #11755 ) ;
#8341=EDGE_LOOP ( 'NONE', ( #7772, #14275, #9335, #5321 ) ) ;
#8342=DIRECTION ( 'NONE',  ( 0.000000000000000000, 0.000000000000000000, -1.000000000000000000 ) ) ;
#8347=CARTESIAN_POINT ( 'NONE',  ( 3.874999999999999556, 2.782000000000002693, 1.509999999999999787 ) ) ;
#8349=CARTESIAN_POINT ( 'NONE',  ( 6.787121492585022509, 0.000000000000000000, 0.000000000000000000 ) ) ;
#8351=FACE_OUTER_BOUND ( 'NONE', #89, .T. ) ;
#8353=EDGE_CURVE ( 'NONE', #7227, #11593, #4556, .T. ) ;
#8356=DIRECTION ( 'NONE',  ( 0.000000000000000000, 0.000000000000000000, -1.000000000000000000 ) ) ;
#8360=CARTESIAN_POINT ( 'NONE',  ( 4.685850439600122819, 1.733285504273739397, -0.02487941436545356572 ) ) ;
#8365=ORIENTED_EDGE ( 'NONE', *, *, #13370, .T. ) ;
#8378=ORIENTED_EDGE ( 'NONE', *, *, #5776, .T. ) ;
#8381=DIRECTION ( 'NONE',  ( 1.000000000000000000, 0.000000000000000000, 0.000000000000000000 ) ) ;
#8393=DIRECTION ( 'NONE',  ( 1.000000000000000000, 0.000000000000000000, 0.000000000000000000 ) ) ;
#8398=CARTESIAN_POINT ( 'NONE',  ( 3.874999999999999556, 3.137999999999999901, 1.130000000000000560 ) ) ;
#8409=CARTESIAN_POINT ( 'NONE',  ( 3.876560711617219379, 3.137999999999999901, 0.000000000000000000 ) ) ;
#8411=CARTESIAN_POINT ( 'NONE',  ( 3.875000000000000000, 1.112678268764263789, 0.000000000000000000 ) ) ;
#8422=CARTESIAN_POINT ( 'NONE',  ( 2.774999999999999911, 2.360000000000000320, -0.9800000000000009814 ) ) ;
#8423=DIRECTION ( 'NONE',  ( 0.000000000000000000, 0.000000000000000000, 1.000000000000000000 ) ) ;
#8424=AXIS2_PLACEMENT_3D ( 'NONE', #5062, #7358, #1521 ) ;
#8432=SHAPE_REPRESENTATION_RELATIONSHIP ( 'NONE' , 'NONE' ,  #9930, #2160 ) ;
#8434=VERTEX_POINT ( 'NONE', #6115 ) ;
#8445=DIRECTION ( 'NONE',  ( 0.000000000000000000, 0.000000000000000000, 1.000000000000000000 ) ) ;
#8461=CARTESIAN_POINT ( 'NONE',  ( 6.176491571325181340, 1.679378605318035733, -1.679378605318065487 ) ) ;
#8470=CARTESIAN_POINT ( 'NONE',  ( 3.621991451083864444, 1.943325121683542989, -0.4314162012240914112 ) ) ;
#8471=DIRECTION ( 'NONE',  ( 1.000000000000000000, 0.000000000000000000, 0.000000000000000000 ) ) ;
#8473=CIRCLE ( 'NONE', #14324, 0.7849999999999992539 ) ;
#8475=CARTESIAN_POINT ( 'NONE',  ( 4.419074073160574656, 1.782004799223066982, -0.5191030992588754334 ) ) ;
#8476=ORIENTED_EDGE ( 'NONE', *, *, #9895, .F. ) ;
#8477=LINE ( 'NONE', #1850, #12286 ) ;
#8478=ORIENTED_EDGE ( 'NONE', *, *, #5816, .F. ) ;
#8480=FACE_OUTER_BOUND ( 'NONE', #8809, .T. ) ;
#8481=VERTEX_POINT ( 'NONE', #1641 ) ;
#8488=EDGE_CURVE ( 'NONE', #4559, #7408, #11904, .T. ) ;
#8492=ADVANCED_FACE ( 'NONE', ( #8480 ), #11152, .F. ) ;
#8494=DIRECTION ( 'NONE',  ( -1.000000000000000000, -0.000000000000000000, -0.000000000000000000 ) ) ;
#8497=CARTESIAN_POINT ( 'NONE',  ( 3.687360920630248451, 1.865009923652485524, 0.7268336272103761431 ) ) ;
#8498=DIRECTION ( 'NONE',  ( 0.000000000000000000, 9.641816448226552334E-15, 1.000000000000000000 ) ) ;
#8503=VERTEX_POINT ( 'NONE', #12206 ) ;
#8510=EDGE_CURVE ( 'NONE', #7967, #7156, #1387, .T. ) ;
#8511=CARTESIAN_POINT ( 'NONE',  ( 3.876560711617219379, -3.000039370078740220, 0.000000000000000000 ) ) ;
#8512=VECTOR ( 'NONE', #6929, 39.37007874015748854 ) ;
#8514=CARTESIAN_POINT ( 'NONE',  ( 6.176491571325181340, 1.679378605318059492, 1.272378605318039257 ) ) ;
#8515=CIRCLE ( 'NONE', #1891, 0.9499999999999992895 ) ;
#8517=ORIENTED_EDGE ( 'NONE', *, *, #9240, .F. ) ;
#8520=CARTESIAN_POINT ( 'NONE',  ( 2.774999999999999911, -0.6999999999999587663, 2.400000000000012790 ) ) ;
#8532=EDGE_CURVE ( 'NONE', #11740, #12941, #2560, .T. ) ;
#8540=EDGE_CURVE ( 'NONE', #9564, #5730, #4327, .T. ) ;
#8545=ORIENTED_EDGE ( 'NONE', *, *, #2822, .F. ) ;
#8547=( GEOMETRIC_REPRESENTATION_CONTEXT ( 3 ) GLOBAL_UNCERTAINTY_ASSIGNED_CONTEXT ( ( #12881 ) ) GLOBAL_UNIT_ASSIGNED_CONTEXT ( ( #2774, #10528, #11596 ) ) REPRESENTATION_CONTEXT ( 'NONE', 'WORKASPACE' ) );
#8548=DIRECTION ( 'NONE',  ( 0.000000000000000000, 0.000000000000000000, -1.000000000000000000 ) ) ;
#8549=DIRECTION ( 'NONE',  ( -1.000000000000000000, -0.000000000000000000, -0.000000000000000000 ) ) ;
#8561=CARTESIAN_POINT ( 'NONE',  ( 4.374985573136147110, 0.9999927865700640739, 0.01697967565367332343 ) ) ;
#8565=LINE ( 'NONE', #4190, #3361 ) ;
#8566=DIRECTION ( 'NONE',  ( 0.000000000000000000, 0.000000000000000000, -1.000000000000000000 ) ) ;
#8571=CARTESIAN_POINT ( 'NONE',  ( 6.826491571325181695, 0.000000000000000000, 0.000000000000000000 ) ) ;
#8574=CARTESIAN_POINT ( 'NONE',  ( 3.426491571325181340, -2.360000000000021636, -1.574999999999999734 ) ) ;
#8575=ORIENTED_EDGE ( 'NONE', *, *, #5401, .F. ) ;
#8583=EDGE_CURVE ( 'NONE', #4442, #14332, #10074, .T. ) ;
#8586=ORIENTED_EDGE ( 'NONE', *, *, #4590, .T. ) ;
#8590=ORIENTED_EDGE ( 'NONE', *, *, #9707, .F. ) ;
#8593=ORIENTED_EDGE ( 'NONE', *, *, #11492, .T. ) ;
#8607=EDGE_LOOP ( 'NONE', ( #13632, #2731, #9117, #1061 ) ) ;
#8612=CARTESIAN_POINT ( 'NONE',  ( 3.875000000000000000, 3.085321731235734610, 0.000000000000000000 ) ) ;
#8614=DIRECTION ( 'NONE',  ( 0.000000000000000000, -1.423315761404775650E-14, -1.000000000000000000 ) ) ;
#8615=EDGE_CURVE ( 'NONE', #12484, #6864, #5306, .T. ) ;
#8618=ORIENTED_EDGE ( 'NONE', *, *, #3436, .T. ) ;
#8622=LINE ( 'NONE', #10840, #10436 ) ;
#8623=CARTESIAN_POINT ( 'NONE',  ( 4.006583522979322076, 0.8753738700246542770, 0.4835050455149407789 ) ) ;
#8626=EDGE_LOOP ( 'NONE', ( #4969, #14444 ) ) ;
#8631=CIRCLE ( 'NONE', #7181, 1.000000000000000888 ) ;
#8634=LINE ( 'NONE', #7487, #14139 ) ;
#8636=PLANE ( 'NONE',  #5728 ) ;
#8645=DIRECTION ( 'NONE',  ( -1.000000000000000000, -0.000000000000000000, -0.000000000000000000 ) ) ;
#8647=AXIS2_PLACEMENT_3D ( 'NONE', #11551, #3601, #5668 ) ;
#8648=DIRECTION ( 'NONE',  ( 0.000000000000000000, 0.000000000000000000, -1.000000000000000000 ) ) ;
#8653=ORIENTED_EDGE ( 'NONE', *, *, #2872, .F. ) ;
#8658=ORIENTED_EDGE ( 'NONE', *, *, #13093, .F. ) ;
#8660=ORIENTED_EDGE ( 'NONE', *, *, #6641, .F. ) ;
#8661=CIRCLE ( 'NONE', #3985, 0.2625000000000000111 ) ;
#8662=ADVANCED_FACE ( 'NONE', ( #13721 ), #8256, .F. ) ;
#8666=DIRECTION ( 'NONE',  ( -0.000000000000000000, -1.000000000000000000, -0.000000000000000000 ) ) ;
#8667=CARTESIAN_POINT ( 'NONE',  ( 3.426491571325181340, 2.359999999999993214, -1.575000000000016831 ) ) ;
#8669=AXIS2_PLACEMENT_3D ( 'NONE', #5313, #14867, #14561 ) ;
#8670=DIRECTION ( 'NONE',  ( 0.000000000000000000, 0.000000000000000000, 1.000000000000000000 ) ) ;
#8673=VERTEX_POINT ( 'NONE', #4792 ) ;
#8674=ORIENTED_EDGE ( 'NONE', *, *, #4284, .T. ) ;
#8675=VERTEX_POINT ( 'NONE', #9544 ) ;
#8680=AXIS2_PLACEMENT_3D ( 'NONE', #10994, #5116, #5251 ) ;
#8681=DIRECTION ( 'NONE',  ( 1.000000000000000000, 0.000000000000000000, 0.000000000000000000 ) ) ;
#8682=DIRECTION ( 'NONE',  ( 0.000000000000000000, 0.000000000000000000, -1.000000000000000000 ) ) ;
#8685=CARTESIAN_POINT ( 'NONE',  ( 4.600967310741519434, 1.805377008994739185, 0.1958307185583574583 ) ) ;
#8689=VECTOR ( 'NONE', #8494, 39.37007874015748143 ) ;
#8691=AXIS2_PLACEMENT_3D ( 'NONE', #3255, #14511, #11518 ) ;
#8696=CARTESIAN_POINT ( 'NONE',  ( 4.370831611789263604, 0.9979212971035885671, 0.06653096183925344409 ) ) ;
#8698=ORIENTED_EDGE ( 'NONE', *, *, #6743, .T. ) ;
#8700=DIRECTION ( 'NONE',  ( 0.000000000000000000, 0.000000000000000000, 1.000000000000000000 ) ) ;
#8701=AXIS2_PLACEMENT_3D ( 'NONE', #8815, #12025, #4224 ) ;
#8706=CARTESIAN_POINT ( 'NONE',  ( 3.389020690428762084, 2.001782680153435745, 0.5706385452936350022 ) ) ;
#8707=CARTESIAN_POINT ( 'NONE',  ( 3.405153689607044232, 3.137999999999999901, -1.491010071662831171 ) ) ;
#8708=ORIENTED_EDGE ( 'NONE', *, *, #14322, .T. ) ;
#8711=AXIS2_PLACEMENT_3D ( 'NONE', #10314, #14974, #8945 ) ;
#8712=ORIENTED_EDGE ( 'NONE', *, *, #15029, .F. ) ;
#8715=ORIENTED_EDGE ( 'NONE', *, *, #6965, .F. ) ;
#8717=DIRECTION ( 'NONE',  ( 0.000000000000000000, 0.000000000000000000, 1.000000000000000000 ) ) ;
#8729=CARTESIAN_POINT ( 'NONE',  ( 3.875000000000000000, 1.059999999999999165, 0.000000000000000000 ) ) ;
#8730=AXIS2_PLACEMENT_3D ( 'NONE', #5182, #10010, #12283 ) ;
#8734=CARTESIAN_POINT ( 'NONE',  ( 4.038269563251255079, 0.8807946909871965380, -0.4737104617346509783 ) ) ;
#8740=LINE ( 'NONE', #14627, #1457 ) ;
#8747=CARTESIAN_POINT ( 'NONE',  ( 6.826491571325181695, 1.679378605318059492, 1.679378605318041506 ) ) ;
#8752=ORIENTED_EDGE ( 'NONE', *, *, #9625, .F. ) ;
#8753=CARTESIAN_POINT ( 'NONE',  ( 3.426491571325181340, -0.9799999999999436939, 2.360000000000016307 ) ) ;
#8755=LINE ( 'NONE', #13407, #9155 ) ;
#8757=CIRCLE ( 'NONE', #14613, 0.3750000000000004996 ) ;
#8758=CARTESIAN_POINT ( 'NONE',  ( 6.176491571325181340, 1.679378605318059492, 1.679378605318041506 ) ) ;
#8759=AXIS2_PLACEMENT_3D ( 'NONE', #337, #6480, #2810 ) ;
#8761=CONICAL_SURFACE ( 'NONE', #9008, 0.2219999999999999751, 0.7853981633974435050 ) ;
#8762=CARTESIAN_POINT ( 'NONE',  ( 4.578072892439084995, 1.801135520826948166, 0.2664308559166134183 ) ) ;
#8764=EDGE_CURVE ( 'NONE', #12204, #4426, #11751, .T. ) ;
#8771=ORIENTED_EDGE ( 'NONE', *, *, #8510, .T. ) ;
#8784=CARTESIAN_POINT ( 'NONE',  ( 6.176491571325181340, 0.000000000000000000, 0.000000000000000000 ) ) ;
#8789=CARTESIAN_POINT ( 'NONE',  ( 4.008086594566573346, 1.746532222454719063, 0.7851401433881748382 ) ) ;
#8790=LINE ( 'NONE', #1511, #4762 ) ;
#8792=ORIENTED_EDGE ( 'NONE', *, *, #13515, .T. ) ;
#8794=CARTESIAN_POINT ( 'NONE',  ( 3.426491571325181340, 3.360000000000016751, 0.9799999999999461364 ) ) ;
#8798=AXIS2_PLACEMENT_3D ( 'NONE', #3930, #1541, #3001 ) ;
#8803=CARTESIAN_POINT ( 'NONE',  ( 6.826491571325181695, 3.649833176986402648E-16, -2.960629921259841257 ) ) ;
#8806=EDGE_CURVE ( 'NONE', #3024, #11151, #13252, .T. ) ;
#8809=EDGE_LOOP ( 'NONE', ( #9259, #6357, #14089, #9210 ) ) ;
#8810=LINE ( 'NONE', #13524, #5341 ) ;
#8811=CARTESIAN_POINT ( 'NONE',  ( 3.572912802749999006, 1.954639998949815771, 0.4011563780351515840 ) ) ;
#8815=CARTESIAN_POINT ( 'NONE',  ( 3.426491571325181340, -1.679378605318059048, -1.679378605318041950 ) ) ;
#8818=ORIENTED_EDGE ( 'NONE', *, *, #582, .T. ) ;
#8821=DIRECTION ( 'NONE',  ( 0.000000000000000000, 0.000000000000000000, -1.000000000000000000 ) ) ;
#8830=DIRECTION ( 'NONE',  ( -1.000000000000000000, -0.000000000000000000, -0.000000000000000000 ) ) ;
#8831=EDGE_LOOP ( 'NONE', ( #6698, #7240 ) ) ;
#8838=DIRECTION ( 'NONE',  ( 0.000000000000000000, 0.000000000000000000, -1.000000000000000000 ) ) ;
#8839=CARTESIAN_POINT ( 'NONE',  ( 4.111670118313984545, 1.798037458796266641, 0.7123029909491147560 ) ) ;
#8842=AXIS2_PLACEMENT_3D ( 'NONE', #3570, #7104, #6018 ) ;
#8843=CARTESIAN_POINT ( 'NONE',  ( 4.217923025938767445, 1.784679989287541346, -0.6680530993927611405 ) ) ;
#8845=ORIENTED_EDGE ( 'NONE', *, *, #1412, .T. ) ;
#8846=ORIENTED_EDGE ( 'NONE', *, *, #7205, .T. ) ;
#8847=CARTESIAN_POINT ( 'NONE',  ( 3.875000000000000000, 1.885381157978844868, -0.5000000000000002220 ) ) ;
#8849=CARTESIAN_POINT ( 'NONE',  ( 3.874999999999999556, 2.750000000000000000, 1.320000000000000062 ) ) ;
#8851=DIRECTION ( 'NONE',  ( 0.000000000000000000, 1.000000000000000000, 0.000000000000000000 ) ) ;
#8853=DIRECTION ( 'NONE',  ( -0.3420201433256623846, 0.000000000000000000, -0.9396926207859106484 ) ) ;
#8854=DIRECTION ( 'NONE',  ( 1.000000000000000000, 0.000000000000000000, 0.000000000000000000 ) ) ;
#8856=EDGE_CURVE ( 'NONE', #14935, #2188, #9715, .T. ) ;
#8857=DIRECTION ( 'NONE',  ( 0.000000000000000000, 0.000000000000000000, -1.000000000000000000 ) ) ;
#8863=CARTESIAN_POINT ( 'NONE',  ( 4.336513449261514275, 1.728610328001806806, 0.5926924422214261412 ) ) ;
#8864=FACE_OUTER_BOUND ( 'NONE', #3226, .T. ) ;
#8867=ORIENTED_EDGE ( 'NONE', *, *, #14572, .F. ) ;
#8868=LINE ( 'NONE', #11463, #1853 ) ;
#8870=ORIENTED_EDGE ( 'NONE', *, *, #5326, .T. ) ;
#8878=VERTEX_POINT ( 'NONE', #10826 ) ;
#8879=CARTESIAN_POINT ( 'NONE',  ( 2.814370078740158210, 0.000000000000000000, 0.000000000000000000 ) ) ;
#8881=CARTESIAN_POINT ( 'NONE',  ( 3.478912079112919109, 0.9522592603935663425, -0.3055730292830077799 ) ) ;
#8882=CARTESIAN_POINT ( 'NONE',  ( 4.203702763460904102, 1.716034727807107529, -0.7239732600819549502 ) ) ;
#8887=VERTEX_POINT ( 'NONE', #7530 ) ;
#8888=EDGE_CURVE ( 'NONE', #1001, #8887, #3871, .T. ) ;
#8894=CARTESIAN_POINT ( 'NONE',  ( 3.874999999999999556, 3.105999999999998984, 1.320000000000000062 ) ) ;
#8896=CYLINDRICAL_SURFACE ( 'NONE', #3303, 1.000000000000000222 ) ;
#8898=EDGE_LOOP ( 'NONE', ( #7613, #11748, #2951, #3644 ) ) ;
#8902=VECTOR ( 'NONE', #9785, 39.37007874015748854 ) ;
#8903=DIRECTION ( 'NONE',  ( 0.000000000000000000, -2.708891287835076765E-14, -1.000000000000000000 ) ) ;
#8904=ORIENTED_EDGE ( 'NONE', *, *, #7106, .F. ) ;
#8905=ORIENTED_EDGE ( 'NONE', *, *, #3480, .T. ) ;
#8907=DIRECTION ( 'NONE',  ( -0.000000000000000000, -1.000000000000000000, -0.000000000000000000 ) ) ;
#8909=LINE ( 'NONE', #4400, #8912 ) ;
#8912=VECTOR ( 'NONE', #4174, 39.37007874015748143 ) ;
#8913=CARTESIAN_POINT ( 'NONE',  ( 4.602321716688412501, 1.805624376861197700, -0.1954697140787868825 ) ) ;
#8917=CARTESIAN_POINT ( 'NONE',  ( 4.112796336321225432, 1.747692466664665600, -0.7127836182515898678 ) ) ;
#8919=ORIENTED_EDGE ( 'NONE', *, *, #8215, .F. ) ;
#8922=DIRECTION ( 'NONE',  ( 0.000000000000000000, -2.708891287835076765E-14, -1.000000000000000000 ) ) ;
#8923=VECTOR ( 'NONE', #387, 39.37007874015748143 ) ;
#8925=CARTESIAN_POINT ( 'NONE',  ( 6.215861650065340527, 0.000000000000000000, 0.000000000000000000 ) ) ;
#8927=CARTESIAN_POINT ( 'NONE',  ( 6.826491571325181695, 1.679378605318035733, -1.304378605318064821 ) ) ;
#8930=DIRECTION ( 'NONE',  ( -0.7071067811865557884, 8.659560562354830553E-17, -0.7071067811865392461 ) ) ;
#8939=CARTESIAN_POINT ( 'NONE',  ( 4.493377435082127391, 1.710570970923634526, 0.5097722557665413934 ) ) ;
#8940=EDGE_CURVE ( 'NONE', #12407, #5002, #6534, .T. ) ;
#8942=ORIENTED_EDGE ( 'NONE', *, *, #12317, .T. ) ;
#8943=ORIENTED_EDGE ( 'NONE', *, *, #3103, .T. ) ;
#8945=DIRECTION ( 'NONE',  ( 0.000000000000000000, -0.000000000000000000, 1.000000000000000000 ) ) ;
#8963=EDGE_CURVE ( 'NONE', #14441, #13413, #10870, .T. ) ;
#8966=CARTESIAN_POINT ( 'NONE',  ( 3.908596656942878500, 0.8665166726997025615, -0.4991519185931051483 ) ) ;
#8970=CARTESIAN_POINT ( 'NONE',  ( 0.000000000000000000, 0.000000000000000000, 0.000000000000000000 ) ) ;
#8973=ADVANCED_FACE ( 'NONE', ( #11197 ), #5547, .F. ) ;
#8976=DIRECTION ( 'NONE',  ( 0.000000000000000000, 0.000000000000000000, 1.000000000000000000 ) ) ;
#8978=FACE_OUTER_BOUND ( 'NONE', #15033, .T. ) ;
#8979=FACE_OUTER_BOUND ( 'NONE', #4540, .T. ) ;
#8980=CIRCLE ( 'NONE', #12873, 2.500000000000000000 ) ;
#8982=EDGE_CURVE ( 'NONE', #1773, #626, #6228, .T. ) ;
#8984=DIRECTION ( 'NONE',  ( 0.000000000000000000, 0.000000000000000000, -1.000000000000000000 ) ) ;
#8986=VECTOR ( 'NONE', #5020, 39.37007874015748143 ) ;
#8997=CARTESIAN_POINT ( 'NONE',  ( 3.876560711617219823, 1.855806856933289506, -0.7500000000000001110 ) ) ;
#9000=FACE_OUTER_BOUND ( 'NONE', #11235, .T. ) ;
#9003=CIRCLE ( 'NONE', #2404, 1.000000000000000000 ) ;
#9006=CARTESIAN_POINT ( 'NONE',  ( 3.874999999999999556, 3.105999999999998984, -1.320000000000000062 ) ) ;
#9007=DIRECTION ( 'NONE',  ( 1.000000000000000000, 0.000000000000000000, 0.000000000000000000 ) ) ;
#9008=AXIS2_PLACEMENT_3D ( 'NONE', #12458, #1974, #11311 ) ;
#9013=FACE_OUTER_BOUND ( 'NONE', #7864, .T. ) ;
#9019=CIRCLE ( 'NONE', #6571, 0.7849999999999969225 ) ;
#9021=AXIS2_PLACEMENT_3D ( 'NONE', #10214, #854, #9221 ) ;
#9022=CARTESIAN_POINT ( 'NONE',  ( 4.417271851176087338, 1.781894997211476595, 0.5209725003072935845 ) ) ;
#9023=CYLINDRICAL_SURFACE ( 'NONE', #11309, 3.000000000000000444 ) ;
#9027=VERTEX_POINT ( 'NONE', #2001 ) ;
#9029=CARTESIAN_POINT ( 'NONE',  ( 3.426491571325181340, 2.360000000000015863, 0.9799999999999454703 ) ) ;
#9039=CARTESIAN_POINT ( 'NONE',  ( 3.379153571854337290, 0.9979286535324267682, 0.06644718038637786872 ) ) ;
#9048=EDGE_CURVE ( 'NONE', #12391, #4893, #8909, .T. ) ;
#9053=EDGE_CURVE ( 'NONE', #355, #843, #9655, .T. ) ;
#9055=ORIENTED_EDGE ( 'NONE', *, *, #6722, .F. ) ;
#9056=FACE_OUTER_BOUND ( 'NONE', #2313, .T. ) ;
#9058=EDGE_CURVE ( 'NONE', #11308, #11151, #566, .T. ) ;
#9062=DIRECTION ( 'NONE',  ( -1.000000000000000000, -0.000000000000000000, -0.000000000000000000 ) ) ;
#9068=CARTESIAN_POINT ( 'NONE',  ( 4.181409934972732501, 1.788377768215813290, -0.6853619333027108906 ) ) ;
#9070=CARTESIAN_POINT ( 'NONE',  ( 3.791764282008899034, 1.827098821033795506, -0.7462103624669557123 ) ) ;
#9071=ORIENTED_EDGE ( 'NONE', *, *, #5236, .F. ) ;
#9072=EDGE_LOOP ( 'NONE', ( #8708, #4237, #7525, #4353 ) ) ;
#9073=EDGE_CURVE ( 'NONE', #7551, #7643, #14791, .T. ) ;
#9077=CIRCLE ( 'NONE', #2236, 0.4070000000000022489 ) ;
#9079=DIRECTION ( 'NONE',  ( 0.000000000000000000, 0.000000000000000000, -1.000000000000000000 ) ) ;
#9084=CARTESIAN_POINT ( 'NONE',  ( 3.153353529948859979, 2.492085072729484985, -0.2007741482994705173 ) ) ;
#9085=DIRECTION ( 'NONE',  ( -1.000000000000000000, -0.000000000000000000, -0.000000000000000000 ) ) ;
#9088=DIRECTION ( 'NONE',  ( 0.000000000000000000, 0.000000000000000000, -1.000000000000000000 ) ) ;
#9089=CARTESIAN_POINT ( 'NONE',  ( 4.247233213520271278, 1.782208133480085444, 0.6529803701610973343 ) ) ;
#9090=CARTESIAN_POINT ( 'NONE',  ( 3.426491571325181340, 2.058905028113295455, -0.2209981660730358233 ) ) ;
#9092=VERTEX_POINT ( 'NONE', #12486 ) ;
#9096=EDGE_CURVE ( 'NONE', #906, #4007, #14505, .T. ) ;
#9098=EDGE_CURVE ( 'NONE', #8887, #8503, #8755, .T. ) ;
#9102=LINE ( 'NONE', #8113, #12424 ) ;
#9103=CARTESIAN_POINT ( 'NONE',  ( 3.426491571325181340, -1.679378605318059048, -1.941878605318027251 ) ) ;
#9108=ORIENTED_EDGE ( 'NONE', *, *, #12989, .T. ) ;
#9109=CYLINDRICAL_SURFACE ( 'NONE', #1173, 0.9499999999999992895 ) ;
#9110=CARTESIAN_POINT ( 'NONE',  ( 3.694556218107261536, 1.926530614425350674, 0.4685710943906171155 ) ) ;
#9111=CARTESIAN_POINT ( 'NONE',  ( 3.504671749944806791, 1.917033125073213995, -0.7259803644674921452 ) ) ;
#9117=ORIENTED_EDGE ( 'NONE', *, *, #1108, .F. ) ;
#9124=AXIS2_PLACEMENT_3D ( 'NONE', #6881, #1194, #15128 ) ;
#9125=DIRECTION ( 'NONE',  ( -1.000000000000000000, -0.000000000000000000, -0.000000000000000000 ) ) ;
#9128=CARTESIAN_POINT ( 'NONE',  ( 3.944129661530210385, 1.867491090171841117, 0.4951980309903491473 ) ) ;
#9130=CARTESIAN_POINT ( 'NONE',  ( 3.426491571325181340, -1.574999999999984190, 1.575000000000033040 ) ) ;
#9133=FACE_OUTER_BOUND ( 'NONE', #4227, .T. ) ;
#9136=ORIENTED_EDGE ( 'NONE', *, *, #9895, .T. ) ;
#9143=ADVANCED_FACE ( 'NONE', ( #3693 ), #10139, .F. ) ;
#9155=VECTOR ( 'NONE', #2943, 39.37007874015748854 ) ;
#9163=CYLINDRICAL_SURFACE ( 'NONE', #3493, 0.1899999999999996136 ) ;
#9166=CARTESIAN_POINT ( 'NONE',  ( 4.543042897114498935, 1.795394141601344140, -0.3444184755256189945 ) ) ;
#9168=ORIENTED_EDGE ( 'NONE', *, *, #14249, .T. ) ;
#9169=AXIS2_PLACEMENT_3D ( 'NONE', #4457, #13695, #10274 ) ;
#9170=ORIENTED_EDGE ( 'NONE', *, *, #307, .F. ) ;
#9173=ORIENTED_EDGE ( 'NONE', *, *, #13476, .F. ) ;
#9179=AXIS2_PLACEMENT_3D ( 'NONE', #4698, #13013, #6149 ) ;
#9188=CARTESIAN_POINT ( 'NONE',  ( 3.808939537174094614, 0.8679352962517474790, 0.4967345602555460204 ) ) ;
#9189=CARTESIAN_POINT ( 'NONE',  ( 4.064258325158515817, 1.735762175202256730, -0.7723679876275294509 ) ) ;
#9191=CARTESIAN_POINT ( 'NONE',  ( 3.944129661530210385, 0.000000000000000000, 0.000000000000000000 ) ) ;
#9192=FACE_OUTER_BOUND ( 'NONE', #780, .T. ) ;
#9193=ORIENTED_EDGE ( 'NONE', *, *, #896, .F. ) ;
#9195=VECTOR ( 'NONE', #5901, 39.37007874015748143 ) ;
#9198=VERTEX_POINT ( 'NONE', #11794 ) ;
#9199=FACE_OUTER_BOUND ( 'NONE', #11186, .T. ) ;
#9210=ORIENTED_EDGE ( 'NONE', *, *, #8134, .F. ) ;
#9211=FACE_OUTER_BOUND ( 'NONE', #9486, .T. ) ;
#9219=AXIS2_PLACEMENT_3D ( 'NONE', #11915, #15135, #2360 ) ;
#9220=FACE_OUTER_BOUND ( 'NONE', #10955, .T. ) ;
#9221=DIRECTION ( 'NONE',  ( 0.000000000000000000, 0.000000000000000000, -1.000000000000000000 ) ) ;
#9225=CARTESIAN_POINT ( 'NONE',  ( 3.895163492705322028, 1.774102321666491511, -0.7976064256867293478 ) ) ;
#9226=VERTEX_POINT ( 'NONE', #11159 ) ;
#9229=CARTESIAN_POINT ( 'NONE',  ( 3.426491571325181340, 1.954234464180151676, 0.6847610993685215863 ) ) ;
#9232=LINE ( 'NONE', #471, #1491 ) ;
#9234=DIRECTION ( 'NONE',  ( -1.000000000000000000, -0.000000000000000000, -0.000000000000000000 ) ) ;
#9236=CARTESIAN_POINT ( 'NONE',  ( 3.140023514803141680, 2.495986062540247019, -0.1444016757220298597 ) ) ;
#9240=EDGE_CURVE ( 'NONE', #1703, #7368, #7216, .T. ) ;
#9241=AXIS2_PLACEMENT_3D ( 'NONE', #2977, #14682, #1810 ) ;
#9245=VECTOR ( 'NONE', #3873, 39.37007874015748854 ) ;
#9246=CARTESIAN_POINT ( 'NONE',  ( 4.616462829641571730, 1.747609168668489366, 0.1239280854323162873 ) ) ;
#9249=EDGE_LOOP ( 'NONE', ( #6338, #12638 ) ) ;
#9259=ORIENTED_EDGE ( 'NONE', *, *, #3844, .F. ) ;
#9260=VECTOR ( 'NONE', #2838, 39.37007874015748143 ) ;
#9261=DIRECTION ( 'NONE',  ( 0.000000000000000000, 0.000000000000000000, -1.000000000000000000 ) ) ;
#9267=AXIS2_PLACEMENT_3D ( 'NONE', #4034, #9777, #8700 ) ;
#9270=CARTESIAN_POINT ( 'NONE',  ( 3.426491571325181340, -1.574999999999999956, 2.360000000000024745 ) ) ;
#9276=DIRECTION ( 'NONE',  ( -1.000000000000000000, -0.000000000000000000, -0.000000000000000000 ) ) ;
#9291=ORIENTED_EDGE ( 'NONE', *, *, #3660, .T. ) ;
#9294=CARTESIAN_POINT ( 'NONE',  ( 6.794491571325179891, 1.679378605318035733, -1.304378605318064821 ) ) ;
#9301=AXIS2_PLACEMENT_3D ( 'NONE', #9639, #12068, #7197 ) ;
#9302=EDGE_CURVE ( 'NONE', #14596, #12391, #12807, .T. ) ;
#9306=CARTESIAN_POINT ( 'NONE',  ( 3.912080264053299672, 1.844581235979443123, -0.7493606589675901875 ) ) ;
#9307=ORIENTED_EDGE ( 'NONE', *, *, #1667, .F. ) ;
#9309=CARTESIAN_POINT ( 'NONE',  ( 2.774999999999999911, -2.360000000000000320, 0.9799999999999999822 ) ) ;
#9311=DIRECTION ( 'NONE',  ( -0.3420201433256623846, 0.000000000000000000, 0.9396926207859106484 ) ) ;
#9313=CARTESIAN_POINT ( 'NONE',  ( 2.774999999999999911, 0.000000000000000000, 0.000000000000000000 ) ) ;
#9315=AXIS2_PLACEMENT_3D ( 'NONE', #11684, #8174, #10380 ) ;
#9317=CARTESIAN_POINT ( 'NONE',  ( 3.181442653385367247, 2.484069017451620898, -0.2831152458680617490 ) ) ;
#9321=CIRCLE ( 'NONE', #5664, 0.5000000000000002220 ) ;
#9322=CARTESIAN_POINT ( 'NONE',  ( 4.516637308352397184, 1.791637356194117681, -0.3913067716919665373 ) ) ;
#9323=VERTEX_POINT ( 'NONE', #7573 ) ;
#9324=DIRECTION ( 'NONE',  ( 0.000000000000000000, 0.000000000000000000, -1.000000000000000000 ) ) ;
#9325=ORIENTED_EDGE ( 'NONE', *, *, #2136, .T. ) ;
#9326=ORIENTED_EDGE ( 'NONE', *, *, #13787, .T. ) ;
#9327=CARTESIAN_POINT ( 'NONE',  ( 3.874999999999999556, 2.750000000000000000, 1.542000000000002258 ) ) ;
#9335=ORIENTED_EDGE ( 'NONE', *, *, #617, .F. ) ;
#9337=DIRECTION ( 'NONE',  ( -1.000000000000000000, -0.000000000000000000, -0.000000000000000000 ) ) ;
#9338=CARTESIAN_POINT ( 'NONE',  ( 6.794491571325181667, 1.679378605318059492, 2.054378605318042172 ) ) ;
#9339=CYLINDRICAL_SURFACE ( 'NONE', #5145, 1.500000000000000222 ) ;
#9341=DIRECTION ( 'NONE',  ( -0.000000000000000000, -1.000000000000000000, -0.000000000000000000 ) ) ;
#9342=EDGE_CURVE ( 'NONE', #1969, #13854, #12301, .T. ) ;
#9344=CARTESIAN_POINT ( 'NONE',  ( 5.546318247523970513, 0.000000000000000000, 0.000000000000000000 ) ) ;
#9347=CARTESIAN_POINT ( 'NONE',  ( 4.673606863172930836, 1.731232082755191914, -0.1365754461054935476 ) ) ;
#9349=DIRECTION ( 'NONE',  ( 0.7071067811865519026, 0.000000000000000000, -0.7071067811865430208 ) ) ;
#9350=CARTESIAN_POINT ( 'NONE',  ( 6.794491571325181667, 1.679378605318059492, 2.054378605318042172 ) ) ;
#9355=ORIENTED_EDGE ( 'NONE', *, *, #6913, .T. ) ;
#9356=DIRECTION ( 'NONE',  ( 0.000000000000000000, 0.000000000000000000, -1.000000000000000000 ) ) ;
#9358=PLANE ( 'NONE',  #15026 ) ;
#9365=CARTESIAN_POINT ( 'NONE',  ( 4.315797241329101475, 2.750000000000000000, -1.570821732971949825 ) ) ;
#9371=AXIS2_PLACEMENT_3D ( 'NONE', #6876, #10236, #9088 ) ;
#9375=AXIS2_PLACEMENT_3D ( 'NONE', #10055, #7676, #613 ) ;
#9382=CARTESIAN_POINT ( 'NONE',  ( 3.818939198319201367, 1.796011530029135717, -0.7986547527183526229 ) ) ;
#9383=ORIENTED_EDGE ( 'NONE', *, *, #13518, .T. ) ;
#9384=ORIENTED_EDGE ( 'NONE', *, *, #3238, .F. ) ;
#9389=FACE_OUTER_BOUND ( 'NONE', #11955, .T. ) ;
#9393=CARTESIAN_POINT ( 'NONE',  ( 3.447448974675020317, 1.983204662126842655, -0.2635305192258420304 ) ) ;
#9397=( GEOMETRIC_REPRESENTATION_CONTEXT ( 3 ) GLOBAL_UNCERTAINTY_ASSIGNED_CONTEXT ( ( #14107 ) ) GLOBAL_UNIT_ASSIGNED_CONTEXT ( ( #1449, #2688, #14516 ) ) REPRESENTATION_CONTEXT ( 'NONE', 'WORKASPACE' ) );
#9398=FACE_OUTER_BOUND ( 'NONE', #14431, .T. ) ;
#9399=EDGE_CURVE ( 'NONE', #10976, #6033, #2071, .T. ) ;
#9400=CARTESIAN_POINT ( 'NONE',  ( 4.602419216495897025, 1.720910125550154213, -0.3479222348275701204 ) ) ;
#9405=CIRCLE ( 'NONE', #7931, 2.500000000000000000 ) ;
#9408=DIRECTION ( 'NONE',  ( 0.000000000000000000, 0.000000000000000000, 1.000000000000000000 ) ) ;
#9410=CARTESIAN_POINT ( 'NONE',  ( 0.000000000000000000, 2.750000000000000000, 0.000000000000000000 ) ) ;
#9411=ORIENTED_EDGE ( 'NONE', *, *, #9073, .F. ) ;
#9416=AXIS2_PLACEMENT_3D ( 'NONE', #4245, #847, #7682 ) ;
#9419=AXIS2_PLACEMENT_3D ( 'NONE', #1847, #11189, #8984 ) ;
#9426=DIRECTION ( 'NONE',  ( 0.000000000000000000, 0.000000000000000000, -1.000000000000000000 ) ) ;
#9431=CARTESIAN_POINT ( 'NONE',  ( 3.426491571325181340, -3.000039370078740220, 0.5999481385559802815 ) ) ;
#9434=AXIS2_PLACEMENT_3D ( 'NONE', #6903, #11787, #12844 ) ;
#9442=LINE ( 'NONE', #9594, #4966 ) ;
#9446=ORIENTED_EDGE ( 'NONE', *, *, #11513, .T. ) ;
#9447=DIRECTION ( 'NONE',  ( -1.000000000000000000, -0.000000000000000000, -0.000000000000000000 ) ) ;
#9449=EDGE_CURVE ( 'NONE', #6091, #3024, #344, .T. ) ;
#9454=CONICAL_SURFACE ( 'NONE', #5046, 0.3750000000000004996, 0.7853981633974547183 ) ;
#9456=AXIS2_PLACEMENT_3D ( 'NONE', #14021, #10753, #12797 ) ;
#9458=FACE_OUTER_BOUND ( 'NONE', #2122, .T. ) ;
#9460=ORIENTED_EDGE ( 'NONE', *, *, #7924, .F. ) ;
#9462=ORIENTED_EDGE ( 'NONE', *, *, #9911, .F. ) ;
#9466=CARTESIAN_POINT ( 'NONE',  ( 6.794491571325179891, -1.679378605318048390, 1.304378605318053497 ) ) ;
#9468=ORIENTED_EDGE ( 'NONE', *, *, #12348, .T. ) ;
#9475=CARTESIAN_POINT ( 'NONE',  ( 3.876560711617219379, 2.749999999999999556, -0.7500000000000001110 ) ) ;
#9476=CARTESIAN_POINT ( 'NONE',  ( 4.544715742067830355, 1.738214473614324573, -0.3411839755103457383 ) ) ;
#9486=EDGE_LOOP ( 'NONE', ( #8145, #5348, #8593, #15131 ) ) ;
#9488=CYLINDRICAL_SURFACE ( 'NONE', #201, 0.3750000000000004996 ) ;
#9492=CARTESIAN_POINT ( 'NONE',  ( 3.675055934133140578, 1.933571379205582863, 0.7235290732629748867 ) ) ;
#9495=AXIS2_PLACEMENT_3D ( 'NONE', #1697, #11033, #5384 ) ;
#9496=CARTESIAN_POINT ( 'NONE',  ( 3.426491571325181340, 0.000000000000000000, 0.000000000000000000 ) ) ;
#9497=CARTESIAN_POINT ( 'NONE',  ( 3.469399777640902460, 0.9562660893803829332, 0.2928328421798268022 ) ) ;
#9498=VECTOR ( 'NONE', #1892, 39.37007874015748854 ) ;
#9500=ORIENTED_EDGE ( 'NONE', *, *, #9342, .F. ) ;
#9501=CARTESIAN_POINT ( 'NONE',  ( 6.794491571325181667, 1.679378605318059492, 1.679378605318041506 ) ) ;
#9504=ORIENTED_EDGE ( 'NONE', *, *, #6508, .T. ) ;
#9505=VECTOR ( 'NONE', #7298, 39.37007874015748854 ) ;
#9509=ORIENTED_EDGE ( 'NONE', *, *, #11199, .T. ) ;
#9510=CARTESIAN_POINT ( 'NONE',  ( 3.875000000000000000, 1.112678268764263789, 0.000000000000000000 ) ) ;
#9511=CIRCLE ( 'NONE', #11446, 0.3750000000000007772 ) ;
#9512=LINE ( 'NONE', #10651, #2806 ) ;
#9517=ORIENTED_EDGE ( 'NONE', *, *, #3238, .T. ) ;
#9518=AXIS2_PLACEMENT_3D ( 'NONE', #11170, #1827, #2842 ) ;
#9519=CARTESIAN_POINT ( 'NONE',  ( 3.441118530312176738, 1.974988295543748329, -0.6122333929865744206 ) ) ;
#9520=LINE ( 'NONE', #8306, #14715 ) ;
#9521=CARTESIAN_POINT ( 'NONE',  ( 3.875000000000000000, 3.085321731235734610, 0.5849999999999996314 ) ) ;
#9522=AXIS2_PLACEMENT_3D ( 'NONE', #12814, #12507, #5565 ) ;
#9525=FACE_OUTER_BOUND ( 'NONE', #11211, .T. ) ;
#9529=DIRECTION ( 'NONE',  ( -1.000000000000000000, -0.000000000000000000, -0.000000000000000000 ) ) ;
#9536=EDGE_CURVE ( 'NONE', #9198, #9590, #11606, .T. ) ;
#9541=AXIS2_PLACEMENT_3D ( 'NONE', #5154, #14468, #13172 ) ;
#9544=CARTESIAN_POINT ( 'NONE',  ( 3.394491571325183088, 1.679378605318059048, 1.941878605318041462 ) ) ;
#9545=DIRECTION ( 'NONE',  ( 0.9396926207859107594, -0.000000000000000000, 0.3420201433256624401 ) ) ;
#9546=DIRECTION ( 'NONE',  ( 1.000000000000000000, 0.000000000000000000, 0.000000000000000000 ) ) ;
#9553=CARTESIAN_POINT ( 'NONE',  ( 4.420609161099084083, 1.729170253341261843, -0.5175182154212143448 ) ) ;
#9559=LINE ( 'NONE', #6956, #618 ) ;
#9560=ORIENTED_EDGE ( 'NONE', *, *, #12163, .T. ) ;
#9564=VERTEX_POINT ( 'NONE', #3506 ) ;
#9568=CARTESIAN_POINT ( 'NONE',  ( 3.834759817877919197, 1.869817227414270588, 0.7491158427897641747 ) ) ;
#9570=AXIS2_PLACEMENT_3D ( 'NONE', #6793, #3339, #8016 ) ;
#9573=CARTESIAN_POINT ( 'NONE',  ( 3.437600372662337200, 2.055609121798811501, 0.6090298485159663100 ) ) ;
#9574=CARTESIAN_POINT ( 'NONE',  ( 4.647180688011975036, 1.726985733735235007, -0.2447955753616387065 ) ) ;
#9578=DIRECTION ( 'NONE',  ( 0.000000000000000000, 0.000000000000000000, -1.000000000000000000 ) ) ;
#9580=EDGE_LOOP ( 'NONE', ( #14518, #3069, #12868, #8771 ) ) ;
#9581=VERTEX_POINT ( 'NONE', #1427 ) ;
#9585=ORIENTED_EDGE ( 'NONE', *, *, #12508, .F. ) ;
#9590=VERTEX_POINT ( 'NONE', #8188 ) ;
#9594=CARTESIAN_POINT ( 'NONE',  ( 3.426491571325181340, -0.9799999999999436939, 2.360000000000016307 ) ) ;
#9595=DIRECTION ( 'NONE',  ( -1.000000000000000000, 0.000000000000000000, 0.000000000000000000 ) ) ;
#9598=ADVANCED_FACE ( 'NONE', ( #7190, #192, #15137, #12829 ), #3742, .F. ) ;
#9599=ORIENTED_EDGE ( 'NONE', *, *, #1373, .T. ) ;
#9600=CARTESIAN_POINT ( 'NONE',  ( 3.426491571325181340, 0.000000000000000000, 0.000000000000000000 ) ) ;
#9603=CARTESIAN_POINT ( 'NONE',  ( 6.215861650065340527, 0.000000000000000000, 0.000000000000000000 ) ) ;
#9610=ORIENTED_EDGE ( 'NONE', *, *, #6617, .T. ) ;
#9611=ORIENTED_EDGE ( 'NONE', *, *, #12964, .T. ) ;
#9615=ADVANCED_FACE ( 'NONE', ( #5811, #11700, #14050, #11845, #8272, #4662 ), #13049, .F. ) ;
#9616=DIRECTION ( 'NONE',  ( -1.000000000000000000, -0.000000000000000000, -0.000000000000000000 ) ) ;
#9618=CARTESIAN_POINT ( 'NONE',  ( 3.538023853514577155, 1.962612250029136307, -0.3701161287706387637 ) ) ;
#9619=DIRECTION ( 'NONE',  ( 0.000000000000000000, 0.000000000000000000, 1.000000000000000000 ) ) ;
#9620=CARTESIAN_POINT ( 'NONE',  ( 3.426491571325181340, 0.000000000000000000, 0.000000000000000000 ) ) ;
#9621=CARTESIAN_POINT ( 'NONE',  ( 2.774999999999999911, -1.679378605318059048, -1.679378605318041950 ) ) ;
#9623=ADVANCED_FACE ( 'NONE', ( #11775 ), #4968, .F. ) ;
#9624=CIRCLE ( 'NONE', #1301, 0.2944999999999856066 ) ;
#9625=EDGE_CURVE ( 'NONE', #2972, #15105, #6004, .T. ) ;
#9628=ORIENTED_EDGE ( 'NONE', *, *, #1168, .F. ) ;
#9629=ORIENTED_EDGE ( 'NONE', *, *, #11142, .F. ) ;
#9633=CARTESIAN_POINT ( 'NONE',  ( 3.426491571325181340, -0.9799999999999436939, 3.360000000000016751 ) ) ;
#9635=VECTOR ( 'NONE', #12918, 39.37007874015748143 ) ;
#9636=CARTESIAN_POINT ( 'NONE',  ( 3.426491571325181340, 1.575000000000016387, 2.359999999999999432 ) ) ;
#9637=DIRECTION ( 'NONE',  ( -1.000000000000000000, -0.000000000000000000, -0.000000000000000000 ) ) ;
#9639=CARTESIAN_POINT ( 'NONE',  ( 3.426491571325181340, 0.000000000000000000, 0.000000000000000000 ) ) ;
#9641=CARTESIAN_POINT ( 'NONE',  ( 6.208491571325183145, -1.679378605318047946, -1.304378605318053053 ) ) ;
#9644=CARTESIAN_POINT ( 'NONE',  ( 3.638344611185302835, 1.884848995134380534, 0.7117177447420894865 ) ) ;
#9645=DIRECTION ( 'NONE',  ( -0.000000000000000000, -1.000000000000000000, -0.000000000000000000 ) ) ;
#9646=ORIENTED_EDGE ( 'NONE', *, *, #3237, .T. ) ;
#9648=LINE ( 'NONE', #2296, #4061 ) ;
#9650=EDGE_LOOP ( 'NONE', ( #12778, #2070, #7038, #1864, #1571, #1663, #5912, #2151, #464, #3708 ) ) ;
#9655=CIRCLE ( 'NONE', #6466, 0.2945000000000006501 ) ;
#9656=ADVANCED_FACE ( 'NONE', ( #7478 ), #3891, .T. ) ;
#9660=ORIENTED_EDGE ( 'NONE', *, *, #8134, .T. ) ;
#9673=CARTESIAN_POINT ( 'NONE',  ( 6.826491571325181695, 1.679378605318059492, 1.679378605318041506 ) ) ;
#9674=ADVANCED_FACE ( 'NONE', ( #13200 ), #5749, .F. ) ;
#9683=VERTEX_POINT ( 'NONE', #14430 ) ;
#9688=DIRECTION ( 'NONE',  ( 0.7071067811865376918, 8.659560562355053653E-17, 0.7071067811865573427 ) ) ;
#9690=DIRECTION ( 'NONE',  ( 0.000000000000000000, -1.000000000000000000, 0.000000000000000000 ) ) ;
#9699=CARTESIAN_POINT ( 'NONE',  ( 4.358375425022244620, 0.9917754135670810989, 0.1321374421498176799 ) ) ;
#9703=ORIENTED_EDGE ( 'NONE', *, *, #4214, .T. ) ;
#9704=CARTESIAN_POINT ( 'NONE',  ( 6.176491571325181340, 1.679378605318059492, 1.679378605318041506 ) ) ;
#9707=EDGE_CURVE ( 'NONE', #159, #12504, #5328, .T. ) ;
#9708=LINE ( 'NONE', #14358, #11457 ) ;
#9709=ADVANCED_FACE ( 'NONE', ( #13424 ), #3959, .F. ) ;
#9710=AXIS2_PLACEMENT_3D ( 'NONE', #190, #14204, #13047 ) ;
#9712=FACE_BOUND ( 'NONE', #7191, .T. ) ;
#9715=CIRCLE ( 'NONE', #3115, 2.000179419058113695 ) ;
#9716=CARTESIAN_POINT ( 'NONE',  ( 3.720984570872676755, 1.852166139790340837, 0.7347827700683455809 ) ) ;
#9719=CARTESIAN_POINT ( 'NONE',  ( 6.096491571325181269, 0.000000000000000000, 0.000000000000000000 ) ) ;
#9720=DIRECTION ( 'NONE',  ( 1.000000000000000000, 0.000000000000000000, 0.000000000000000000 ) ) ;
#9723=CONICAL_SURFACE ( 'NONE', #5083, 0.4070000000000022489, 0.7853981633974547183 ) ;
#9726=ORIENTED_EDGE ( 'NONE', *, *, #5881, .F. ) ;
#9727=LINE ( 'NONE', #12937, #7305 ) ;
#9734=LINE ( 'NONE', #12023, #11941 ) ;
#9737=FACE_OUTER_BOUND ( 'NONE', #11503, .T. ) ;
#9738=ORIENTED_EDGE ( 'NONE', *, *, #12482, .F. ) ;
#9743=AXIS2_PLACEMENT_3D ( 'NONE', #12707, #2233, #12939 ) ;
#9751=DIRECTION ( 'NONE',  ( -1.000000000000000000, -0.000000000000000000, -0.000000000000000000 ) ) ;
#9763=CARTESIAN_POINT ( 'NONE',  ( 4.269212872948124904, 1.781133266760655864, -0.6394758128702182631 ) ) ;
#9764=TOROIDAL_SURFACE ( 'NONE', #9541, 1.580000000000000071, 0.08000000000000000167 ) ;
#9765=CARTESIAN_POINT ( 'NONE',  ( 4.338845464883685388, 1.779384211668088911, -0.5916759243745035590 ) ) ;
#9767=ORIENTED_EDGE ( 'NONE', *, *, #4590, .F. ) ;
#9768=ORIENTED_EDGE ( 'NONE', *, *, #5955, .T. ) ;
#9769=CARTESIAN_POINT ( 'NONE',  ( 3.874999999999999556, 2.750000000000000000, 1.320000000000000062 ) ) ;
#9770=EDGE_CURVE ( 'NONE', #6864, #12484, #14618, .T. ) ;
#9772=CARTESIAN_POINT ( 'NONE',  ( 4.037927003766942136, 0.8807194764073917881, 0.4738554624952319161 ) ) ;
#9774=CARTESIAN_POINT ( 'NONE',  ( 3.874999999999999556, 3.137999999999999901, 1.320000000000000062 ) ) ;
#9776=DIRECTION ( 'NONE',  ( -1.000000000000000000, -0.000000000000000000, -0.000000000000000000 ) ) ;
#9777=DIRECTION ( 'NONE',  ( -0.000000000000000000, -1.000000000000000000, -0.000000000000000000 ) ) ;
#9779=CARTESIAN_POINT ( 'NONE',  ( 3.599442323206996530, 1.969410324051942274, 0.6972124116338633826 ) ) ;
#9783=CARTESIAN_POINT ( 'NONE',  ( 3.825335190572127786, 1.816349960665768037, 0.7486281390988553941 ) ) ;
#9785=DIRECTION ( 'NONE',  ( 8.659560562354890950E-17, 0.7071067811865509034, -0.7071067811865441310 ) ) ;
#9788=ADVANCED_FACE ( 'NONE', ( #12502 ), #4866, .F. ) ;
#9789=DIRECTION ( 'NONE',  ( 0.000000000000000000, -1.000000000000000000, 0.000000000000000000 ) ) ;
#9790=CARTESIAN_POINT ( 'NONE',  ( 5.567023771132172172, 0.000000000000000000, 0.000000000000000000 ) ) ;
#9791=VERTEX_POINT ( 'NONE', #6636 ) ;
#9795=ORIENTED_EDGE ( 'NONE', *, *, #12305, .T. ) ;
#9797=CARTESIAN_POINT ( 'NONE',  ( 2.806999999999999940, -1.679378605318059048, -1.416878605318056872 ) ) ;
#9804=CARTESIAN_POINT ( 'NONE',  ( 2.980731298636167370, 2.750000000000000000, -0.3249191361593797844 ) ) ;
#9814=ADVANCED_FACE ( 'NONE', ( #3260 ), #2187, .T. ) ;
#9817=CONICAL_SURFACE ( 'NONE', #3220, 0.2625000000000000111, 0.7853981633974621568 ) ;
#9819=ADVANCED_FACE ( 'NONE', ( #6870 ), #10376, .F. ) ;
#9826=CARTESIAN_POINT ( 'NONE',  ( 3.426491571325181340, 1.224646799147353207E-16, -1.000000000000000000 ) ) ;
#9830=CARTESIAN_POINT ( 'NONE',  ( 4.134953843058370104, 1.794421708884817113, 0.7041910065148488940 ) ) ;
#9832=EDGE_CURVE ( 'NONE', #10219, #1686, #10077, .T. ) ;
#9834=CARTESIAN_POINT ( 'NONE',  ( 4.393220956986357173, 1.780595993968445034, -0.5448392271506915518 ) ) ;
#9836=ORIENTED_EDGE ( 'NONE', *, *, #2502, .T. ) ;
#9838=DIRECTION ( 'NONE',  ( 1.000000000000000000, 0.000000000000000000, 0.000000000000000000 ) ) ;
#9841=CARTESIAN_POINT ( 'NONE',  ( 4.127139180425047904, 0.9016242830556325805, 0.4329707884123231154 ) ) ;
#9846=DIRECTION ( 'NONE',  ( 0.000000000000000000, 0.000000000000000000, 1.000000000000000000 ) ) ;
#9851=LINE ( 'NONE', #11376, #1527 ) ;
#9855=DIRECTION ( 'NONE',  ( -1.000000000000000000, -0.000000000000000000, -0.000000000000000000 ) ) ;
#9856=EDGE_LOOP ( 'NONE', ( #5922, #629, #11525, #3277, #1321, #7809, #11099, #12271, #6385, #14136, #6198, #12846, #5657, #1177, #11846, #2164, #5952, #13147, #9055, #12371, #66, #405, #7496, #3545, #8575 ) ) ;
#9862=EDGE_LOOP ( 'NONE', ( #1932, #12156, #828, #2254, #10206, #6333, #1996, #5392, #7185 ) ) ;
#9869=DIRECTION ( 'NONE',  ( 0.000000000000000000, 1.000000000000000000, 0.000000000000000000 ) ) ;
#9880=CARTESIAN_POINT ( 'NONE',  ( 4.298848810396105335, 0.9641482059274013583, -0.2657306241200046992 ) ) ;
#9882=ORIENTED_EDGE ( 'NONE', *, *, #13877, .T. ) ;
#9885=VERTEX_POINT ( 'NONE', #1103 ) ;
#9890=DIRECTION ( 'NONE',  ( -1.000000000000000000, -0.000000000000000000, -0.000000000000000000 ) ) ;
#9893=CIRCLE ( 'NONE', #3059, 0.2944999999999976525 ) ;
#9894=CIRCLE ( 'NONE', #9169, 0.1899999999999996136 ) ;
#9895=EDGE_CURVE ( 'NONE', #11537, #6001, #2407, .T. ) ;
#9897=DIRECTION ( 'NONE',  ( 0.000000000000000000, 0.000000000000000000, 1.000000000000000000 ) ) ;
#9899=ORIENTED_EDGE ( 'NONE', *, *, #6538, .F. ) ;
#9908=AXIS2_PLACEMENT_3D ( 'NONE', #2323, #1082, #13938 ) ;
#9909=CONICAL_SURFACE ( 'NONE', #3314, 1.932031071636253650, 0.2617993877991429685 ) ;
#9911=EDGE_CURVE ( 'NONE', #6629, #6179, #1165, .T. ) ;
#9913=CARTESIAN_POINT ( 'NONE',  ( 4.124243424167258532, 1.725694442234845916, -0.7553927200278419685 ) ) ;
#9914=EDGE_LOOP ( 'NONE', ( #5522, #1420 ) ) ;
#9917=EDGE_CURVE ( 'NONE', #11151, #10316, #14122, .T. ) ;
#9918=VECTOR ( 'NONE', #6200, 39.37007874015748854 ) ;
#9922=CARTESIAN_POINT ( 'NONE',  ( 4.348661478442751083, 0.9870318323618022527, 0.1634103574579118534 ) ) ;
#9923=EDGE_CURVE ( 'NONE', #7368, #5558, #10529, .T. ) ;
#9925=DIRECTION ( 'NONE',  ( -0.000000000000000000, 1.000000000000000000, -0.000000000000000000 ) ) ;
#9926=VERTEX_POINT ( 'NONE', #6101 ) ;
#9927=FACE_OUTER_BOUND ( 'NONE', #10653, .T. ) ;
#9930=SHAPE_REPRESENTATION ( 'Inlet Housing', ( #8424 ), #9397 ) ;
#9934=CARTESIAN_POINT ( 'NONE',  ( 4.332693437952970683, 1.707681683440760656, 0.6520824339025526051 ) ) ;
#9937=CIRCLE ( 'NONE', #12126, 0.4849999999999995981 ) ;
#9948=AXIS2_PLACEMENT_3D ( 'NONE', #12980, #13970, #2513 ) ;
#9949=CARTESIAN_POINT ( 'NONE',  ( 6.826491571325181695, 1.679378605318035733, -1.679378605318065487 ) ) ;
#9950=CARTESIAN_POINT ( 'NONE',  ( 3.394491571325182644, 1.679378605318042395, -1.941878605318058337 ) ) ;
#9955=ORIENTED_EDGE ( 'NONE', *, *, #1277, .F. ) ;
#9956=LINE ( 'NONE', #746, #13148 ) ;
#9962=CARTESIAN_POINT ( 'NONE',  ( 3.958564149947915389, 0.8698990160032655794, -0.4932443601560797530 ) ) ;
#9964=ORIENTED_EDGE ( 'NONE', *, *, #5236, .T. ) ;
#9966=ORIENTED_EDGE ( 'NONE', *, *, #775, .T. ) ;
#9968=DIRECTION ( 'NONE',  ( 0.000000000000000000, 0.000000000000000000, -1.000000000000000000 ) ) ;
#9970=DIRECTION ( 'NONE',  ( 0.000000000000000000, 0.000000000000000000, -1.000000000000000000 ) ) ;
#9977=VECTOR ( 'NONE', #8037, 39.37007874015748143 ) ;
#9981=EDGE_LOOP ( 'NONE', ( #3351, #3201, #10292, #12600 ) ) ;
#9984=EDGE_CURVE ( 'NONE', #8675, #906, #11678, .T. ) ;
#9987=EDGE_CURVE ( 'NONE', #1342, #11081, #13185, .T. ) ;
#9995=CARTESIAN_POINT ( 'NONE',  ( 2.774999999999999911, 1.575000000000016387, 2.359999999999999876 ) ) ;
#10007=CARTESIAN_POINT ( 'NONE',  ( 4.205202298494868707, 0.9267662340798809018, 0.3758042580177037850 ) ) ;
#10010=DIRECTION ( 'NONE',  ( 1.000000000000000000, 0.000000000000000000, 0.000000000000000000 ) ) ;
#10013=DIRECTION ( 'NONE',  ( 0.000000000000000000, 1.000000000000000000, -1.836536466328828134E-14 ) ) ;
#10014=EDGE_CURVE ( 'NONE', #2874, #2357, #5096, .T. ) ;
#10018=ADVANCED_FACE ( 'NONE', ( #6317 ), #11924, .F. ) ;
#10019=CARTESIAN_POINT ( 'NONE',  ( 3.843202652328518987, 1.810746292266676605, 0.7496334864260736364 ) ) ;
#10020=DIRECTION ( 'NONE',  ( 0.000000000000000000, 0.000000000000000000, -1.000000000000000000 ) ) ;
#10023=CARTESIAN_POINT ( 'NONE',  ( 3.876560711617219823, 1.855806856933289506, -0.7500000000000001110 ) ) ;
#10024=VERTEX_POINT ( 'NONE', #2866 ) ;
#10026=VECTOR ( 'NONE', #12324, 39.37007874015748143 ) ;
#10032=DIRECTION ( 'NONE',  ( 0.000000000000000000, 8.723548215061523903E-15, 1.000000000000000000 ) ) ;
#10038=CARTESIAN_POINT ( 'NONE',  ( 3.469135854992689616, 0.9563780235308655397, -0.2924688362345267967 ) ) ;
#10039=CARTESIAN_POINT ( 'NONE',  ( 3.944129661530210385, 1.761538328845252188, -0.7935532608319411096 ) ) ;
#10043=ORIENTED_EDGE ( 'NONE', *, *, #10203, .F. ) ;
#10047=CARTESIAN_POINT ( 'NONE',  ( 3.713442968092242946, 1.916698194283638079, -0.7331915495002455652 ) ) ;
#10050=CARTESIAN_POINT ( 'NONE',  ( 3.944129661530210385, 0.000000000000000000, 0.000000000000000000 ) ) ;
#10051=EDGE_LOOP ( 'NONE', ( #7847, #3773, #2592, #6457 ) ) ;
#10054=CARTESIAN_POINT ( 'NONE',  ( 3.875000000000000000, 3.137999999999999901, 0.000000000000000000 ) ) ;
#10055=CARTESIAN_POINT ( 'NONE',  ( 6.826491571325181695, -1.679378605318047946, -1.679378605318053497 ) ) ;
#10058=DIRECTION ( 'NONE',  ( 0.000000000000000000, -1.224646799147353454E-16, 1.000000000000000000 ) ) ;
#10062=AXIS2_PLACEMENT_3D ( 'NONE', #5712, #9545, #10373 ) ;
#10063=DIRECTION ( 'NONE',  ( -0.000000000000000000, -1.000000000000000000, -0.000000000000000000 ) ) ;
#10064=CARTESIAN_POINT ( 'NONE',  ( 4.626513628950617907, 1.810550457394507040, 0.04993882545213381569 ) ) ;
#10066=ORIENTED_EDGE ( 'NONE', *, *, #6414, .T. ) ;
#10067=EDGE_CURVE ( 'NONE', #12843, #14153, #3794, .T. ) ;
#10069=CARTESIAN_POINT ( 'NONE',  ( 4.268616971210836830, 1.710660744896744578, -0.6914058754706146059 ) ) ;
#10071=ORIENTED_EDGE ( 'NONE', *, *, #3342, .F. ) ;
#10074=LINE ( 'NONE', #4335, #6047 ) ;
#10077=LINE ( 'NONE', #8927, #11690 ) ;
#10080=DIRECTION ( 'NONE',  ( 0.3420201433256623846, 0.000000000000000000, 0.9396926207859106484 ) ) ;
#10090=CARTESIAN_POINT ( 'NONE',  ( 4.364820037892395810, 1.707069359036963219, 0.6292106624328539510 ) ) ;
#10091=CARTESIAN_POINT ( 'NONE',  ( 3.827923612805795184, 1.898876434569533256, -0.4983202096988793017 ) ) ;
#10094=DIRECTION ( 'NONE',  ( 0.000000000000000000, 0.000000000000000000, -1.000000000000000000 ) ) ;
#10095=ORIENTED_EDGE ( 'NONE', *, *, #7365, .F. ) ;
#10103=EDGE_CURVE ( 'NONE', #13854, #11243, #10460, .T. ) ;
#10108=CIRCLE ( 'NONE', #3508, 0.7849999999999958122 ) ;
#10109=LINE ( 'NONE', #7654, #4464 ) ;
#10110=CARTESIAN_POINT ( 'NONE',  ( 4.500934089278993078, 1.710778234005743359, -0.5029489024355867643 ) ) ;
#10114=DIRECTION ( 'NONE',  ( 0.000000000000000000, 0.000000000000000000, -1.000000000000000000 ) ) ;
#10117=ORIENTED_EDGE ( 'NONE', *, *, #4221, .T. ) ;
#10119=EDGE_CURVE ( 'NONE', #4965, #4727, #437, .T. ) ;
#10123=FACE_OUTER_BOUND ( 'NONE', #8341, .T. ) ;
#10124=CARTESIAN_POINT ( 'NONE',  ( 2.774999999999999911, -0.9799999999999436939, 2.360000000000016307 ) ) ;
#10128=CARTESIAN_POINT ( 'NONE',  ( 3.760599021723662450, 1.814825219489536678, 0.7947699344343004402 ) ) ;
#10129=VECTOR ( 'NONE', #9645, 39.37007874015748143 ) ;
#10132=VERTEX_POINT ( 'NONE', #6995 ) ;
#10135=DIRECTION ( 'NONE',  ( 1.000000000000000000, 0.000000000000000000, 0.000000000000000000 ) ) ;
#10137=EDGE_CURVE ( 'NONE', #14777, #7182, #13929, .T. ) ;
#10138=CARTESIAN_POINT ( 'NONE',  ( 3.426491571325181340, 0.000000000000000000, 0.000000000000000000 ) ) ;
#10139=CONICAL_SURFACE ( 'NONE', #14770, 0.3750000000000007772, 0.7853981633974557175 ) ;
#10140=CARTESIAN_POINT ( 'NONE',  ( 3.900033994830720552, 1.848181875390886519, -0.7500000000000002220 ) ) ;
#10142=ORIENTED_EDGE ( 'NONE', *, *, #3575, .T. ) ;
#10151=CARTESIAN_POINT ( 'NONE',  ( 3.426491571325181340, 2.062169880637645836, -0.5999481385559802815 ) ) ;
#10158=AXIS2_PLACEMENT_3D ( 'NONE', #4854, #7081, #14317 ) ;
#10159=AXIS2_PLACEMENT_3D ( 'NONE', #9501, #352, #14367 ) ;
#10160=B_SPLINE_CURVE_WITH_KNOTS ( 'NONE', 3,
 ( #11047, #6395, #1630, #474, #12426, #6546, #8839, #9830, #2795, #11206, #4016, #2946, #544, #14564, #13410, #6467, #707, #4177, #14485, #5398, #4096, #8762, #1708, #8685, #6321, #6246, #10064, #7609, #10982, #7535, #4250, #8913, #1781, #13256, #13559, #3101, #5170, #10907, #11126, #624, #7467, #5319, #399, #9763, #12125, #11584, #4632, #9068, #15024, #936, #5551, #1087, #1012, #13643, #10140, #8997 ),
 .UNSPECIFIED., .F., .F.,
 ( 4, 2, 2, 2, 2, 2, 2, 2, 2, 2, 2, 2, 2, 2, 2, 2, 2, 2, 2, 2, 2, 2, 2, 2, 2, 2, 2, 4 ),
 ( 0.01335241406472727557, 0.01712285003613359807, 0.01900806802183678534, 0.01995067701468835816, 0.02089328600753993098, 0.02466372197894622920, 0.02654893996464938177, 0.02843415795035252741, 0.03220459392175881175, 0.03408981190746195045, 0.03597502989316508915, 0.03786024787886822784, 0.03974546586457137348, 0.04351590183597766476, 0.04540111982168081040, 0.04728633780738396297, 0.05105677377879025425, 0.05294199176449340682, 0.05482720975019655940, 0.05671242773589969810, 0.05859764572160285068, 0.06236808169300916971, 0.06425329967871233616, 0.06519590867156389857, 0.06613851766441547486, 0.06990895363582165511, 0.07179417162152473830, 0.07367938960722780761 ),
 .UNSPECIFIED. ) ;
#10162=CARTESIAN_POINT ( 'NONE',  ( 4.145336115082029593, 1.743003941933530587, 0.7011725378991962021 ) ) ;
#10166=CARTESIAN_POINT ( 'NONE',  ( 3.405153689607044232, 2.750000000000000000, -1.491010071662831171 ) ) ;
#10167=EDGE_LOOP ( 'NONE', ( #11654, #7056, #7473, #7242 ) ) ;
#10171=DIRECTION ( 'NONE',  ( -0.3420201433256623846, 0.000000000000000000, -0.9396926207859106484 ) ) ;
#10176=LINE ( 'NONE', #11621, #7707 ) ;
#10179=AXIS2_PLACEMENT_3D ( 'NONE', #11505, #8907, #5696 ) ;
#10181=EDGE_CURVE ( 'NONE', #1151, #4018, #12186, .T. ) ;
#10188=CARTESIAN_POINT ( 'NONE',  ( 3.544798737392580001, 0.9267668399616416641, -0.3758007328785020196 ) ) ;
#10189=CARTESIAN_POINT ( 'NONE',  ( 6.208491571325183145, 1.679378605318059492, 2.054378605318042172 ) ) ;
#10193=ORIENTED_EDGE ( 'NONE', *, *, #13054, .T. ) ;
#10197=CARTESIAN_POINT ( 'NONE',  ( 3.426491571325181340, -0.9799999999999989830, -2.359999999999999876 ) ) ;
#10199=EDGE_CURVE ( 'NONE', #10875, #2564, #12917, .T. ) ;
#10202=DIRECTION ( 'NONE',  ( 0.000000000000000000, 0.000000000000000000, -1.000000000000000000 ) ) ;
#10203=EDGE_CURVE ( 'NONE', #2606, #5449, #1908, .T. ) ;
#10206=ORIENTED_EDGE ( 'NONE', *, *, #11689, .T. ) ;
#10207=DIRECTION ( 'NONE',  ( 0.000000000000000000, 0.000000000000000000, -1.000000000000000000 ) ) ;
#10211=AXIS2_PLACEMENT_3D ( 'NONE', #5737, #13744, #9261 ) ;
#10214=CARTESIAN_POINT ( 'NONE',  ( 6.787121492585022509, 0.000000000000000000, 0.000000000000000000 ) ) ;
#10215=B_SPLINE_CURVE_WITH_KNOTS ( 'NONE', 3,
 ( #10279, #14711, #4239, #10347, #6682, #10128, #5689, #14780, #3091, #6532, #12477, #4315 ),
 .UNSPECIFIED., .F., .F.,
 ( 4, 2, 2, 2, 2, 4 ),
 ( 0.000000000000000000, 0.001826406838012980009, 0.003652813676025960018, 0.007305627352051886209, 0.01095844102807781197, 0.01461125470410373599 ),
 .UNSPECIFIED. ) ;
#10219=VERTEX_POINT ( 'NONE', #9294 ) ;
#10221=DIRECTION ( 'NONE',  ( 0.000000000000000000, 0.000000000000000000, 1.000000000000000000 ) ) ;
#10222=VERTEX_POINT ( 'NONE', #4768 ) ;
#10225=CARTESIAN_POINT ( 'NONE',  ( 3.394491571325183088, 1.679378605318059048, 1.679378605318041506 ) ) ;
#10235=AXIS2_PLACEMENT_3D ( 'NONE', #3772, #2312, #8445 ) ;
#10236=DIRECTION ( 'NONE',  ( -0.000000000000000000, -1.000000000000000000, -0.000000000000000000 ) ) ;
#10239=CARTESIAN_POINT ( 'NONE',  ( 4.004051897178946717, 1.768001349219448626, 0.7400188025467686614 ) ) ;
#10240=DIRECTION ( 'NONE',  ( -1.000000000000000000, -0.000000000000000000, -0.000000000000000000 ) ) ;
#10254=CARTESIAN_POINT ( 'NONE',  ( 3.874999999999999556, 2.750000000000000000, -1.320000000000000062 ) ) ;
#10258=EDGE_CURVE ( 'NONE', #3105, #7033, #10659, .T. ) ;
#10259=ORIENTED_EDGE ( 'NONE', *, *, #8615, .F. ) ;
#10260=EDGE_CURVE ( 'NONE', #12467, #504, #7542, .T. ) ;
#10262=CARTESIAN_POINT ( 'NONE',  ( 3.829348296951585073, 1.894867393789687160, 0.4984412668866745055 ) ) ;
#10265=CARTESIAN_POINT ( 'NONE',  ( 6.208491571325183145, -1.679378605318047946, -1.679378605318053497 ) ) ;
#10272=LINE ( 'NONE', #14928, #13505 ) ;
#10274=DIRECTION ( 'NONE',  ( 0.000000000000000000, 0.000000000000000000, 1.000000000000000000 ) ) ;
#10279=CARTESIAN_POINT ( 'NONE',  ( 3.944129661530210385, 1.761538328845252188, 0.7935532608319412207 ) ) ;
#10281=ORIENTED_EDGE ( 'NONE', *, *, #13877, .F. ) ;
#10286=EDGE_CURVE ( 'NONE', #11264, #1773, #8052, .T. ) ;
#10292=ORIENTED_EDGE ( 'NONE', *, *, #499, .F. ) ;
#10296=ORIENTED_EDGE ( 'NONE', *, *, #1651, .F. ) ;
#10303=CARTESIAN_POINT ( 'NONE',  ( 4.769268701363833074, 3.137999999999999901, 0.3249191361593796734 ) ) ;
#10305=EDGE_CURVE ( 'NONE', #11081, #12243, #3153, .T. ) ;
#10308=CIRCLE ( 'NONE', #7153, 0.2624999999999852451 ) ;
#10309=CYLINDRICAL_SURFACE ( 'NONE', #9371, 0.5000000000000001110 ) ;
#10310=CARTESIAN_POINT ( 'NONE',  ( 4.626188208514882660, 1.723983726829047214, 0.2983432309202477817 ) ) ;
#10312=ORIENTED_EDGE ( 'NONE', *, *, #3781, .T. ) ;
#10314=CARTESIAN_POINT ( 'NONE',  ( 3.876560711617219379, 3.137999999999999901, 0.000000000000000000 ) ) ;
#10316=VERTEX_POINT ( 'NONE', #8520 ) ;
#10317=LINE ( 'NONE', #15057, #9498 ) ;
#10327=DIRECTION ( 'NONE',  ( 0.000000000000000000, 1.000000000000000000, -0.000000000000000000 ) ) ;
#10330=CARTESIAN_POINT ( 'NONE',  ( 4.134613691807048852, 1.724441890029780211, -0.7513151844660320711 ) ) ;
#10331=DIRECTION ( 'NONE',  ( -0.7071067811865429098, 0.000000000000000000, 0.7071067811865521247 ) ) ;
#10332=CARTESIAN_POINT ( 'NONE',  ( 3.944129661530210385, 2.407784495501249742E-16, -1.932031071636253650 ) ) ;
#10333=ORIENTED_EDGE ( 'NONE', *, *, #5978, .F. ) ;
#10338=EDGE_CURVE ( 'NONE', #9926, #9226, #5601, .T. ) ;
#10343=VECTOR ( 'NONE', #11112, 39.37007874015748143 ) ;
#10345=EDGE_LOOP ( 'NONE', ( #1120, #8378, #4729, #4047 ) ) ;
#10347=CARTESIAN_POINT ( 'NONE',  ( 3.851668032307324463, 1.786355384972422966, 0.7987671621174978753 ) ) ;
#10357=AXIS2_PLACEMENT_3D ( 'NONE', #7513, #10960, #6077 ) ;
#10365=CARTESIAN_POINT ( 'NONE',  ( 6.794491571325181667, 1.679378605318059492, 1.304378605318041062 ) ) ;
#10367=CARTESIAN_POINT ( 'NONE',  ( 4.011028178682179757, 1.745898953245868412, -0.7846266810094224553 ) ) ;
#10369=ORIENTED_EDGE ( 'NONE', *, *, #14550, .T. ) ;
#10373=DIRECTION ( 'NONE',  ( 0.3420201433256623846, 0.000000000000000000, -0.9396926207859106484 ) ) ;
#10376=CYLINDRICAL_SURFACE ( 'NONE', #12408, 0.3750000000000004996 ) ;
#10378=CARTESIAN_POINT ( 'NONE',  ( 3.182018581797185774, 2.483907847764145416, 0.2845129745686012512 ) ) ;
#10380=DIRECTION ( 'NONE',  ( 0.000000000000000000, 0.000000000000000000, 1.000000000000000000 ) ) ;
#10381=EDGE_CURVE ( 'NONE', #9226, #12391, #9734, .T. ) ;
#10385=CARTESIAN_POINT ( 'NONE',  ( 4.518491583832497938, 1.735549304995126718, -0.3882790969652222812 ) ) ;
#10387=VECTOR ( 'NONE', #12631, 39.37007874015748854 ) ;
#10388=LINE ( 'NONE', #1265, #6931 ) ;
#10389=ORIENTED_EDGE ( 'NONE', *, *, #13267, .T. ) ;
#10397=CARTESIAN_POINT ( 'NONE',  ( 2.527624975756972425, 2.750000000000000000, -0.9199802545633498640 ) ) ;
#10401=DIRECTION ( 'NONE',  ( 1.000000000000000000, 0.000000000000000000, 0.000000000000000000 ) ) ;
#10402=AXIS2_PLACEMENT_3D ( 'NONE', #3544, #8229, #7157 ) ;
#10406=VECTOR ( 'NONE', #9349, 39.37007874015748854 ) ;
#10408=DIRECTION ( 'NONE',  ( 0.000000000000000000, 0.000000000000000000, 1.000000000000000000 ) ) ;
#10410=CARTESIAN_POINT ( 'NONE',  ( 3.479169036718512409, 0.9521518695376113284, 0.3059096338091180645 ) ) ;
#10411=CARTESIAN_POINT ( 'NONE',  ( 4.181805601875195677, 1.718400334928297468, 0.7333929193435403393 ) ) ;
#10417=EDGE_LOOP ( 'NONE', ( #14412, #4941, #12530, #5716 ) ) ;
#10426=CARTESIAN_POINT ( 'NONE',  ( 3.496294824931886147, 1.921163641483014439, -0.7211466812414543126 ) ) ;
#10434=ORIENTED_EDGE ( 'NONE', *, *, #8353, .T. ) ;
#10436=VECTOR ( 'NONE', #3888, 39.37007874015748143 ) ;
#10445=CARTESIAN_POINT ( 'NONE',  ( 3.722375483330346846, 1.851882672529376439, -0.7344444148597581989 ) ) ;
#10447=EDGE_LOOP ( 'NONE', ( #4351, #14958 ) ) ;
#10448=CARTESIAN_POINT ( 'NONE',  ( 3.426491571325181784, 2.050018311957429784, 0.6006734803707507453 ) ) ;
#10453=EDGE_CURVE ( 'NONE', #13687, #9092, #2099, .T. ) ;
#10454=CARTESIAN_POINT ( 'NONE',  ( 3.426491571325181340, -0.6999999999999989564, -2.399999999999999911 ) ) ;
#10457=LINE ( 'NONE', #11832, #7841 ) ;
#10460=CIRCLE ( 'NONE', #2890, 0.7849999999999992539 ) ;
#10461=CARTESIAN_POINT ( 'NONE',  ( 4.662226822519125236, 1.729394697956203597, 0.1892339305778590608 ) ) ;
#10471=CARTESIAN_POINT ( 'NONE',  ( 6.826491571325181695, 0.000000000000000000, 0.000000000000000000 ) ) ;
#10473=DIRECTION ( 'NONE',  ( -0.000000000000000000, -1.000000000000000000, 0.000000000000000000 ) ) ;
#10478=AXIS2_PLACEMENT_3D ( 'NONE', #13982, #978, #5669 ) ;
#10480=CARTESIAN_POINT ( 'NONE',  ( 3.794247516364918749, 1.884217686586828755, -0.7465934532251186084 ) ) ;
#10486=ORIENTED_EDGE ( 'NONE', *, *, #10014, .T. ) ;
#10489=CARTESIAN_POINT ( 'NONE',  ( 4.394316455220915074, 1.707002683764069939, 0.6062743810478267159 ) ) ;
#10493=FACE_OUTER_BOUND ( 'NONE', #505, .T. ) ;
#10498=ORIENTED_EDGE ( 'NONE', *, *, #14962, .T. ) ;
#10502=LINE ( 'NONE', #7148, #7229 ) ;
#10505=AXIS2_PLACEMENT_3D ( 'NONE', #9673, #1470, #9970 ) ;
#10508=DIRECTION ( 'NONE',  ( -1.000000000000000000, -0.000000000000000000, -0.000000000000000000 ) ) ;
#10509=CARTESIAN_POINT ( 'NONE',  ( 3.875000000000000000, 1.112678268764263789, -0.5849999999999996314 ) ) ;
#10513=CARTESIAN_POINT ( 'NONE',  ( 3.875000000000000000, 1.059999999999999165, 0.000000000000000000 ) ) ;
#10514=DIRECTION ( 'NONE',  ( 0.3420201433256623846, 0.000000000000000000, 0.9396926207859106484 ) ) ;
#10515=ORIENTED_EDGE ( 'NONE', *, *, #700, .T. ) ;
#10517=CIRCLE ( 'NONE', #3184, 1.932031071636253650 ) ;
#10521=CARTESIAN_POINT ( 'NONE',  ( 3.543808504702383289, 1.925955906416788377, -0.6728280703062919921 ) ) ;
#10523=VERTEX_POINT ( 'NONE', #4261 ) ;
#10527=PLANE ( 'NONE',  #14449 ) ;
#10528=( NAMED_UNIT ( * ) PLANE_ANGLE_UNIT ( ) SI_UNIT ( $, .RADIAN. ) );
#10529=LINE ( 'NONE', #10454, #3140 ) ;
#10531=AXIS2_PLACEMENT_3D ( 'NONE', #8258, #5795, #3730 ) ;
#10534=DIRECTION ( 'NONE',  ( 0.000000000000000000, 1.000000000000000000, -0.000000000000000000 ) ) ;
#10535=LINE ( 'NONE', #4723, #726 ) ;
#10539=CARTESIAN_POINT ( 'NONE',  ( 4.606889440629292842, 1.746155438930072856, -0.1743145812842641362 ) ) ;
#10540=ORIENTED_EDGE ( 'NONE', *, *, #7363, .T. ) ;
#10546=FACE_OUTER_BOUND ( 'NONE', #7386, .T. ) ;
#10550=DIRECTION ( 'NONE',  ( -1.000000000000000000, -0.000000000000000000, -0.000000000000000000 ) ) ;
#10558=EDGE_CURVE ( 'NONE', #11081, #6020, #12030, .T. ) ;
#10559=CARTESIAN_POINT ( 'NONE',  ( 3.841842303834268169, 0.8660254037844385966, 0.5000000000000003331 ) ) ;
#10560=CARTESIAN_POINT ( 'NONE',  ( 4.484040318217246579, 1.709965233507263260, 0.5205613024012289980 ) ) ;
#10563=LINE ( 'NONE', #5673, #10885 ) ;
#10576=CARTESIAN_POINT ( 'NONE',  ( 3.411612174842781009, 2.070834547792271607, -0.5884920204652813736 ) ) ;
#10579=CARTESIAN_POINT ( 'NONE',  ( 3.944129661530210385, 0.000000000000000000, 0.000000000000000000 ) ) ;
#10584=ADVANCED_FACE ( 'NONE', ( #7442 ), #2849, .T. ) ;
#10587=CARTESIAN_POINT ( 'NONE',  ( 6.208491571325183145, 1.679378605318035733, -1.679378605318065487 ) ) ;
#10595=ORIENTED_EDGE ( 'NONE', *, *, #7365, .T. ) ;
#10600=DIRECTION ( 'NONE',  ( -0.000000000000000000, -1.000000000000000000, -0.000000000000000000 ) ) ;
#10604=ORIENTED_EDGE ( 'NONE', *, *, #3012, .T. ) ;
#10605=CARTESIAN_POINT ( 'NONE',  ( 3.394491571325182644, 1.679378605318042395, -1.679378605318058604 ) ) ;
#10609=MANIFOLD_SOLID_BREP ( 'Fillet4', #11324 ) ;
#10611=CARTESIAN_POINT ( 'NONE',  ( 4.573675675097676141, 1.800317658760837158, -0.2789865180029196257 ) ) ;
#10617=AXIS2_PLACEMENT_3D ( 'NONE', #2680, #14291, #7351 ) ;
#10619=EDGE_LOOP ( 'NONE', ( #9966, #187, #7257, #11742 ) ) ;
#10621=FACE_OUTER_BOUND ( 'NONE', #1563, .T. ) ;
#10622=DIRECTION ( 'NONE',  ( 0.000000000000000000, 0.000000000000000000, 1.000000000000000000 ) ) ;
#10624=LINE ( 'NONE', #14137, #14342 ) ;
#10626=CARTESIAN_POINT ( 'NONE',  ( 3.426491571325181340, 2.062169880637645836, 0.5999481385559802815 ) ) ;
#10628=DIRECTION ( 'NONE',  ( 0.000000000000000000, 0.000000000000000000, -1.000000000000000000 ) ) ;
#10629=AXIS2_PLACEMENT_3D ( 'NONE', #10587, #14097, #12952 ) ;
#10631=DIRECTION ( 'NONE',  ( -1.000000000000000000, -0.000000000000000000, -0.000000000000000000 ) ) ;
#10634=CARTESIAN_POINT ( 'NONE',  ( 4.669107278503995317, 1.730498534900028362, 0.1593143144689976309 ) ) ;
#10636=ORIENTED_EDGE ( 'NONE', *, *, #9923, .T. ) ;
#10643=CARTESIAN_POINT ( 'NONE',  ( 6.176491571325181340, 0.000000000000000000, 0.000000000000000000 ) ) ;
#10647=DIRECTION ( 'NONE',  ( -0.000000000000000000, -1.000000000000000000, -0.000000000000000000 ) ) ;
#10649=AXIS2_PLACEMENT_3D ( 'NONE', #60, #7136, #14994 ) ;
#10650=ADVANCED_FACE ( 'NONE', ( #7662 ), #11178, .F. ) ;
#10651=CARTESIAN_POINT ( 'NONE',  ( 3.426491571325181340, 0.9799999999999438050, -2.360000000000016307 ) ) ;
#10653=EDGE_LOOP ( 'NONE', ( #4024, #9307, #1968, #19 ) ) ;
#10656=CARTESIAN_POINT ( 'NONE',  ( 3.507351867251836897, 2.016901088656855467, -0.6530382159986841684 ) ) ;
#10659=LINE ( 'NONE', #12862, #13392 ) ;
#10663=ORIENTED_EDGE ( 'NONE', *, *, #14653, .T. ) ;
#10664=DIRECTION ( 'NONE',  ( -1.000000000000000000, -0.000000000000000000, -0.000000000000000000 ) ) ;
#10674=ORIENTED_EDGE ( 'NONE', *, *, #14111, .T. ) ;
#10681=PLANE ( 'NONE',  #10062 ) ;
#10683=ORIENTED_EDGE ( 'NONE', *, *, #11951, .T. ) ;
#10684=CARTESIAN_POINT ( 'NONE',  ( 3.694934205048947984, 1.926420985531493768, -0.4670271297431359270 ) ) ;
#10685=CARTESIAN_POINT ( 'NONE',  ( 3.874999999999999556, 2.750000000000000000, -1.320000000000000062 ) ) ;
#10686=DIRECTION ( 'NONE',  ( -1.000000000000000000, -0.000000000000000000, -0.000000000000000000 ) ) ;
#10687=ADVANCED_FACE ( 'NONE', ( #9199 ), #5858, .T. ) ;
#10692=FACE_OUTER_BOUND ( 'NONE', #1914, .T. ) ;
#10696=ORIENTED_EDGE ( 'NONE', *, *, #10199, .F. ) ;
#10699=SHAPE_DEFINITION_REPRESENTATION ( #14213, #9930 ) ;
#10710=CARTESIAN_POINT ( 'NONE',  ( 3.875000000000619504, 1.884022191776286714, 0.5000000000000002220 ) ) ;
#10713=CYLINDRICAL_SURFACE ( 'NONE', #11634, 0.3750000000000004996 ) ;
#10716=EDGE_LOOP ( 'NONE', ( #6208, #14164, #7307, #7035 ) ) ;
#10722=ORIENTED_EDGE ( 'NONE', *, *, #3082, .F. ) ;
#10730=CIRCLE ( 'NONE', #4128, 1.000000000000000222 ) ;
#10734=FACE_OUTER_BOUND ( 'NONE', #14684, .T. ) ;
#10735=AXIS2_PLACEMENT_3D ( 'NONE', #1461, #5992, #5849 ) ;
#10737=CARTESIAN_POINT ( 'NONE',  ( 3.426491571325181340, 1.987932976489903414, 0.2209981660730357955 ) ) ;
#10739=ORIENTED_EDGE ( 'NONE', *, *, #11199, .F. ) ;
#10740=ADVANCED_FACE ( 'NONE', ( #4454 ), #1066, .F. ) ;
#10743=ORIENTED_EDGE ( 'NONE', *, *, #10338, .F. ) ;
#10753=DIRECTION ( 'NONE',  ( -1.000000000000000000, -0.000000000000000000, -0.000000000000000000 ) ) ;
#10754=VERTEX_POINT ( 'NONE', #2060 ) ;
#10762=ADVANCED_FACE ( 'NONE', ( #3531 ), #3228, .T. ) ;
#10763=CARTESIAN_POINT ( 'NONE',  ( 3.874999999999999556, 3.105999999999998984, -1.320000000000000062 ) ) ;
#10766=CARTESIAN_POINT ( 'NONE',  ( 3.426491571325181340, 0.9800000000000039790, 2.359999999999999876 ) ) ;
#10767=ORIENTED_EDGE ( 'NONE', *, *, #11842, .T. ) ;
#10768=CYLINDRICAL_SURFACE ( 'NONE', #3015, 0.7500000000000001110 ) ;
#10769=ORIENTED_EDGE ( 'NONE', *, *, #10258, .F. ) ;
#10772=ORIENTED_EDGE ( 'NONE', *, *, #4862, .F. ) ;
#10780=CARTESIAN_POINT ( 'NONE',  ( 2.774999999999999911, 1.575000000000016387, 2.359999999999999432 ) ) ;
#10783=AXIS2_PLACEMENT_3D ( 'NONE', #12050, #11762, #1260 ) ;
#10785=CARTESIAN_POINT ( 'NONE',  ( 6.208491571325183145, -1.679378605318048390, 1.304378605318053497 ) ) ;
#10787=CARTESIAN_POINT ( 'NONE',  ( 3.622127693352770184, 1.891608983934359500, 0.7060953400642342448 ) ) ;
#10789=ORIENTED_EDGE ( 'NONE', *, *, #13411, .F. ) ;
#10790=CARTESIAN_POINT ( 'NONE',  ( 5.567023771132172172, 0.000000000000000000, 1.580000000000000071 ) ) ;
#10795=EDGE_CURVE ( 'NONE', #10219, #4487, #9511, .T. ) ;
#10797=ORIENTED_EDGE ( 'NONE', *, *, #725, .F. ) ;
#10798=CIRCLE ( 'NONE', #13219, 0.4070000000000022489 ) ;
#10811=DIRECTION ( 'NONE',  ( 0.000000000000000000, 0.000000000000000000, -1.000000000000000000 ) ) ;
#10812=VERTEX_POINT ( 'NONE', #12622 ) ;
#10814=DIRECTION ( 'NONE',  ( 1.000000000000000000, -0.000000000000000000, -0.000000000000000000 ) ) ;
#10817=AXIS2_PLACEMENT_3D ( 'NONE', #11267, #11190, #10202 ) ;
#10821=ADVANCED_FACE ( 'NONE', ( #11869 ), #3640, .T. ) ;
#10826=CARTESIAN_POINT ( 'NONE',  ( 2.774999999999999911, 2.360000000000015863, 0.9799999999999454703 ) ) ;
#10828=CARTESIAN_POINT ( 'NONE',  ( 3.426491571325181340, 0.9800000000000039790, 2.359999999999999876 ) ) ;
#10834=CARTESIAN_POINT ( 'NONE',  ( 4.367450314957311619, 1.706859693599265926, -0.6280954649258110312 ) ) ;
#10840=CARTESIAN_POINT ( 'NONE',  ( 2.527624975756972425, 3.137999999999999901, 0.9199802545633498640 ) ) ;
#10843=ORIENTED_EDGE ( 'NONE', *, *, #3781, .F. ) ;
#10844=AXIS2_PLACEMENT_3D ( 'NONE', #13299, #12168, #1681 ) ;
#10845=LINE ( 'NONE', #6263, #2632 ) ;
#10846=CARTESIAN_POINT ( 'NONE',  ( 2.807000000000000384, 1.679378605318059048, 1.679378605318041506 ) ) ;
#10847=EDGE_CURVE ( 'NONE', #3733, #11243, #9727, .T. ) ;
#10854=DIRECTION ( 'NONE',  ( 0.000000000000000000, 0.000000000000000000, 1.000000000000000000 ) ) ;
#10856=CARTESIAN_POINT ( 'NONE',  ( 3.669034062028589283, 1.848124941201018112, 0.7795100282588544038 ) ) ;
#10862=DIRECTION ( 'NONE',  ( 1.000000000000000000, 0.000000000000000000, 0.000000000000000000 ) ) ;
#10864=ORIENTED_EDGE ( 'NONE', *, *, #4647, .F. ) ;
#10868=ORIENTED_EDGE ( 'NONE', *, *, #156, .T. ) ;
#10870=CIRCLE ( 'NONE', #13042, 1.000000000000000222 ) ;
#10871=DIMENSIONAL_EXPONENTS ( 1.000000000000000000, 0.000000000000000000, 0.000000000000000000, 0.000000000000000000, 0.000000000000000000, 0.000000000000000000, 0.000000000000000000 ) ;
#10872=CONICAL_SURFACE ( 'NONE', #11855, 0.1899999999999996136, 0.7853981633974435050 ) ;
#10874=CARTESIAN_POINT ( 'NONE',  ( 6.794491571325181667, 1.679378605318059492, 1.679378605318041506 ) ) ;
#10875=VERTEX_POINT ( 'NONE', #12015 ) ;
#10879=DIRECTION ( 'NONE',  ( -1.000000000000000000, -0.000000000000000000, -0.000000000000000000 ) ) ;
#10880=ORIENTED_EDGE ( 'NONE', *, *, #4896, .T. ) ;
#10885=VECTOR ( 'NONE', #10331, 39.37007874015748143 ) ;
#10892=VECTOR ( 'NONE', #9529, 39.37007874015748143 ) ;
#10894=CARTESIAN_POINT ( 'NONE',  ( 3.876560711617219379, -3.000039370078740220, -0.7500000000000001110 ) ) ;
#10895=EDGE_CURVE ( 'NONE', #15105, #2972, #8044, .T. ) ;
#10901=DIRECTION ( 'NONE',  ( 0.000000000000000000, 0.000000000000000000, -1.000000000000000000 ) ) ;
#10907=CARTESIAN_POINT ( 'NONE',  ( 4.485106214549655412, 1.787785851493574274, -0.4390631173008620047 ) ) ;
#10913=ADVANCED_FACE ( 'NONE', ( #4991 ), #12083, .T. ) ;
#10914=AXIS2_PLACEMENT_3D ( 'NONE', #8411, #4897, #4814 ) ;
#10921=DIRECTION ( 'NONE',  ( 0.000000000000000000, 0.000000000000000000, 1.000000000000000000 ) ) ;
#10928=CARTESIAN_POINT ( 'NONE',  ( 3.492055192262802699, 2.024943995107577166, 0.6451593962764085033 ) ) ;
#10932=CARTESIAN_POINT ( 'NONE',  ( 3.790134320942320389, 1.827873989719922321, 0.7454134881782992217 ) ) ;
#10935=CARTESIAN_POINT ( 'NONE',  ( 0.000000000000000000, 0.000000000000000000, 1.500000000000000222 ) ) ;
#10937=ORIENTED_EDGE ( 'NONE', *, *, #10137, .F. ) ;
#10939=VECTOR ( 'NONE', #4510, 39.37007874015748854 ) ;
#10940=ADVANCED_FACE ( 'NONE', ( #361 ), #5065, .F. ) ;
#10944=DIRECTION ( 'NONE',  ( 0.000000000000000000, 0.000000000000000000, 1.000000000000000000 ) ) ;
#10950=DIRECTION ( 'NONE',  ( 1.000000000000000000, 0.000000000000000000, 0.000000000000000000 ) ) ;
#10955=EDGE_LOOP ( 'NONE', ( #4602, #14124, #5478, #5174 ) ) ;
#10956=AXIS2_PLACEMENT_3D ( 'NONE', #9313, #9546, #12808 ) ;
#10957=CARTESIAN_POINT ( 'NONE',  ( 3.874999999999999556, 3.137999999999999901, -1.320000000000000062 ) ) ;
#10960=DIRECTION ( 'NONE',  ( 1.000000000000000000, -0.000000000000000000, -0.000000000000000000 ) ) ;
#10973=FACE_OUTER_BOUND ( 'NONE', #6672, .T. ) ;
#10976=VERTEX_POINT ( 'NONE', #9950 ) ;
#10977=DIRECTION ( 'NONE',  ( -1.000000000000000000, -0.000000000000000000, -0.000000000000000000 ) ) ;
#10982=CARTESIAN_POINT ( 'NONE',  ( 4.625398766514281945, 1.810313843597131100, -0.04860614483416566406 ) ) ;
#10983=B_SPLINE_CURVE_WITH_KNOTS ( 'NONE', 3,
 ( #6545, #6319, #11122, #2868, #7463, #7684, #5318, #5097, #7396, #14419, #13186, #12343 ),
 .UNSPECIFIED., .F., .F.,
 ( 4, 2, 2, 2, 2, 4 ),
 ( 4.252726876253797924E-17, 0.0004594653927451592497, 0.0009189307854902759986, 0.001837861570980509496, 0.002756792356470742777, 0.003675723141960976492 ),
 .UNSPECIFIED. ) ;
#10986=CARTESIAN_POINT ( 'NONE',  ( 4.285697740953402501, 1.709640378115386383, -0.6816790960877695538 ) ) ;
#10989=EDGE_LOOP ( 'NONE', ( #6498, #2717, #9882, #9767 ) ) ;
#10992=DIRECTION ( 'NONE',  ( 0.000000000000000000, 0.000000000000000000, -1.000000000000000000 ) ) ;
#10994=CARTESIAN_POINT ( 'NONE',  ( 3.426491571325181340, 1.574999999999994849, -1.575000000000022160 ) ) ;
#11002=CARTESIAN_POINT ( 'NONE',  ( 6.787121492585022509, 1.224646799147353207E-16, 1.000000000000000000 ) ) ;
#11003=FACE_BOUND ( 'NONE', #12430, .T. ) ;
#11006=CARTESIAN_POINT ( 'NONE',  ( 3.874999999999999556, 2.750000000000000000, -1.542000000000000037 ) ) ;
#11007=DIRECTION ( 'NONE',  ( -1.000000000000000000, -0.000000000000000000, -0.000000000000000000 ) ) ;
#11008=VERTEX_POINT ( 'NONE', #8803 ) ;
#11017=( GEOMETRIC_REPRESENTATION_CONTEXT ( 3 ) GLOBAL_UNCERTAINTY_ASSIGNED_CONTEXT ( ( #5556 ) ) GLOBAL_UNIT_ASSIGNED_CONTEXT ( ( #1489, #1560, #5101 ) ) REPRESENTATION_CONTEXT ( 'NONE', 'WORKASPACE' ) );
#11022=ORIENTED_EDGE ( 'NONE', *, *, #8245, .F. ) ;
#11029=ORIENTED_EDGE ( 'NONE', *, *, #12956, .F. ) ;
#11031=DIRECTION ( 'NONE',  ( -1.000000000000000000, -0.000000000000000000, -0.000000000000000000 ) ) ;
#11033=DIRECTION ( 'NONE',  ( 1.000000000000000000, 0.000000000000000000, 0.000000000000000000 ) ) ;
#11037=DIRECTION ( 'NONE',  ( -0.7071067811865429098, 0.000000000000000000, 0.7071067811865521247 ) ) ;
#11039=ORIENTED_EDGE ( 'NONE', *, *, #14661, .T. ) ;
#11046=DIRECTION ( 'NONE',  ( -1.000000000000000000, 0.000000000000000000, 0.000000000000000000 ) ) ;
#11047=CARTESIAN_POINT ( 'NONE',  ( 3.876560711617219379, 1.855806856933289950, 0.7500000000000001110 ) ) ;
#11051=CARTESIAN_POINT ( 'NONE',  ( 4.161191225369840652, 1.720662318184893680, -0.7422136750874308575 ) ) ;
#11057=CIRCLE ( 'NONE', #14723, 0.5000000000000002220 ) ;
#11059=CARTESIAN_POINT ( 'NONE',  ( 4.368421302294625441, 0.9967228440525767175, -0.08252939445393610296 ) ) ;
#11065=CARTESIAN_POINT ( 'NONE',  ( 3.426491571325181340, 0.000000000000000000, 0.000000000000000000 ) ) ;
#11069=CARTESIAN_POINT ( 'NONE',  ( 4.307438648313010710, 1.779872554500928628, 0.6141414098449724523 ) ) ;
#11070=LINE ( 'NONE', #14589, #5485 ) ;
#11071=ORIENTED_EDGE ( 'NONE', *, *, #9536, .F. ) ;
#11077=AXIS2_PLACEMENT_3D ( 'NONE', #6444, #1913, #6600 ) ;
#11081=VERTEX_POINT ( 'NONE', #9797 ) ;
#11082=DIRECTION ( 'NONE',  ( 0.000000000000000000, 0.000000000000000000, -1.000000000000000000 ) ) ;
#11095=DIRECTION ( 'NONE',  ( -1.000000000000000000, -0.000000000000000000, -0.000000000000000000 ) ) ;
#11097=CARTESIAN_POINT ( 'NONE',  ( 4.098045170698160433, 0.8941794442107894314, -0.4477920867524256554 ) ) ;
#11099=ORIENTED_EDGE ( 'NONE', *, *, #2305, .F. ) ;
#11105=CARTESIAN_POINT ( 'NONE',  ( 6.826491571325181695, -1.679378605318047946, -1.272378605318051248 ) ) ;
#11107=DIRECTION ( 'NONE',  ( 0.000000000000000000, 0.000000000000000000, 1.000000000000000000 ) ) ;
#11109=CARTESIAN_POINT ( 'NONE',  ( 3.876560711617219379, -3.000039370078740220, 0.7500000000000001110 ) ) ;
#11112=DIRECTION ( 'NONE',  ( -1.000000000000000000, -0.000000000000000000, -0.000000000000000000 ) ) ;
#11115=ORIENTED_EDGE ( 'NONE', *, *, #7488, .T. ) ;
#11119=ADVANCED_FACE ( 'NONE', ( #3139 ), #8761, .F. ) ;
#11121=CIRCLE ( 'NONE', #9179, 2.960629921259842146 ) ;
#11122=CARTESIAN_POINT ( 'NONE',  ( 3.426491571325181784, 2.050035007886724436, -0.6006740390345088887 ) ) ;
#11124=CIRCLE ( 'NONE', #6490, 1.500000000000000222 ) ;
#11126=CARTESIAN_POINT ( 'NONE',  ( 4.470399241404178881, 1.786230780441887545, -0.4587633099568068085 ) ) ;
#11130=ORIENTED_EDGE ( 'NONE', *, *, #10260, .T. ) ;
#11132=VERTEX_POINT ( 'NONE', #2208 ) ;
#11140=CARTESIAN_POINT ( 'NONE',  ( 3.394491571325183088, -1.679378605318041950, 1.679378605318059048 ) ) ;
#11142=EDGE_CURVE ( 'NONE', #7890, #14925, #891, .T. ) ;
#11149=CARTESIAN_POINT ( 'NONE',  ( 4.572644766289085005, 1.800139870985668411, 0.2814996426995059475 ) ) ;
#11151=VERTEX_POINT ( 'NONE', #5586 ) ;
#11152=CONICAL_SURFACE ( 'NONE', #13585, 0.2625000000000000111, 0.7853981633974621568 ) ;
#11153=ORIENTED_EDGE ( 'NONE', *, *, #1358, .F. ) ;
#11154=DIRECTION ( 'NONE',  ( 0.000000000000000000, 0.000000000000000000, -1.000000000000000000 ) ) ;
#11159=CARTESIAN_POINT ( 'NONE',  ( 3.394491571325183088, -1.679378605318041950, 1.941878605318059003 ) ) ;
#11162=DIRECTION ( 'NONE',  ( 0.000000000000000000, 0.000000000000000000, 1.000000000000000000 ) ) ;
#11165=PLANE ( 'NONE',  #11612 ) ;
#11167=VERTEX_POINT ( 'NONE', #11471 ) ;
#11169=CARTESIAN_POINT ( 'NONE',  ( 3.759899079166374669, 0.8734932728588881146, -0.4868506001230482050 ) ) ;
#11170=CARTESIAN_POINT ( 'NONE',  ( 3.394491571325183088, -1.679378605318041950, 1.679378605318059048 ) ) ;
#11173=CARTESIAN_POINT ( 'NONE',  ( 6.794491571325179891, -1.679378605318048390, 2.054378605318054607 ) ) ;
#11174=ORIENTED_EDGE ( 'NONE', *, *, #9302, .F. ) ;
#11178=CYLINDRICAL_SURFACE ( 'NONE', #445, 0.1899999999999996136 ) ;
#11183=DIRECTION ( 'NONE',  ( -1.000000000000000000, -0.000000000000000000, -0.000000000000000000 ) ) ;
#11184=CYLINDRICAL_SURFACE ( 'NONE', #650, 0.2625000000000000111 ) ;
#11186=EDGE_LOOP ( 'NONE', ( #8308, #14692, #6202, #1290, #1933, #13993 ) ) ;
#11188=AXIS2_PLACEMENT_3D ( 'NONE', #5168, #9616, #3945 ) ;
#11189=DIRECTION ( 'NONE',  ( -1.000000000000000000, -0.000000000000000000, -0.000000000000000000 ) ) ;
#11190=DIRECTION ( 'NONE',  ( -1.000000000000000000, -0.000000000000000000, -0.000000000000000000 ) ) ;
#11197=FACE_OUTER_BOUND ( 'NONE', #3787, .T. ) ;
#11198=VECTOR ( 'NONE', #7446, 39.37007874015748143 ) ;
#11199=EDGE_CURVE ( 'NONE', #7267, #8189, #9102, .T. ) ;
#11204=VECTOR ( 'NONE', #76, 39.37007874015748143 ) ;
#11205=DIRECTION ( 'NONE',  ( 0.000000000000000000, 0.000000000000000000, 1.000000000000000000 ) ) ;
#11206=CARTESIAN_POINT ( 'NONE',  ( 4.203741336932380612, 1.785315657883247864, 0.6766739387161787578 ) ) ;
#11207=ORIENTED_EDGE ( 'NONE', *, *, #13190, .F. ) ;
#11208=CIRCLE ( 'NONE', #6579, 0.2944999999999987073 ) ;
#11209=ADVANCED_FACE ( 'NONE', ( #12832 ), #5508, .T. ) ;
#11211=EDGE_LOOP ( 'NONE', ( #11383, #2092, #11695, #2353 ) ) ;
#11212=ORIENTED_EDGE ( 'NONE', *, *, #6641, .T. ) ;
#11218=CARTESIAN_POINT ( 'NONE',  ( 3.908162907339028269, 0.8665001417438028541, 0.4991805435374154776 ) ) ;
#11219=DIRECTION ( 'NONE',  ( -1.000000000000000000, -0.000000000000000000, -0.000000000000000000 ) ) ;
#11225=DIRECTION ( 'NONE',  ( 0.000000000000000000, 0.000000000000000000, -1.000000000000000000 ) ) ;
#11230=CARTESIAN_POINT ( 'NONE',  ( 4.121281386195119190, 1.726130368164997320, 0.7563743875758589530 ) ) ;
#11231=CARTESIAN_POINT ( 'NONE',  ( 3.715374161931121133, 1.936069962591262517, -0.4743889576438739542 ) ) ;
#11232=ORIENTED_EDGE ( 'NONE', *, *, #7763, .T. ) ;
#11233=EDGE_CURVE ( 'NONE', #843, #355, #8057, .T. ) ;
#11235=EDGE_LOOP ( 'NONE', ( #13794, #764, #1710, #13401 ) ) ;
#11238=ORIENTED_EDGE ( 'NONE', *, *, #3057, .F. ) ;
#11239=CIRCLE ( 'NONE', #7821, 0.2219999999999999751 ) ;
#11243=VERTEX_POINT ( 'NONE', #10780 ) ;
#11251=CARTESIAN_POINT ( 'NONE',  ( 3.897779889561915567, 1.772923893090484926, -0.7985164159195319300 ) ) ;
#11253=EDGE_CURVE ( 'NONE', #7544, #2357, #1431, .T. ) ;
#11255=LINE ( 'NONE', #13834, #15046 ) ;
#11258=AXIS2_PLACEMENT_3D ( 'NONE', #13620, #6172, #11906 ) ;
#11260=DIRECTION ( 'NONE',  ( 0.000000000000000000, 0.000000000000000000, 1.000000000000000000 ) ) ;
#11264=VERTEX_POINT ( 'NONE', #1504 ) ;
#11265=FACE_OUTER_BOUND ( 'NONE', #15079, .T. ) ;
#11266=CIRCLE ( 'NONE', #10783, 0.5000000000000002220 ) ;
#11267=CARTESIAN_POINT ( 'NONE',  ( 6.096491571325181269, 0.000000000000000000, 0.000000000000000000 ) ) ;
#11270=FACE_OUTER_BOUND ( 'NONE', #6218, .T. ) ;
#11272=EDGE_LOOP ( 'NONE', ( #1517, #7318, #7543, #5404, #12005 ) ) ;
#11273=CARTESIAN_POINT ( 'NONE',  ( 3.405153689607044232, 3.137999999999999901, -1.491010071662831171 ) ) ;
#11274=EDGE_LOOP ( 'NONE', ( #6066, #5604, #5941, #6298 ) ) ;
#11275=CARTESIAN_POINT ( 'NONE',  ( 2.774999999999999911, 1.679378605318059048, 1.679378605318041506 ) ) ;
#11279=CARTESIAN_POINT ( 'NONE',  ( 3.851708199487537954, 1.891837914331504944, 0.5000000000000002220 ) ) ;
#11280=ORIENTED_EDGE ( 'NONE', *, *, #7055, .F. ) ;
#11285=ORIENTED_EDGE ( 'NONE', *, *, #14788, .T. ) ;
#11294=EDGE_LOOP ( 'NONE', ( #3300, #3858, #924, #2948 ) ) ;
#11295=CARTESIAN_POINT ( 'NONE',  ( 3.874999999999999556, 3.137999999999999901, 1.542000000000000037 ) ) ;
#11298=CARTESIAN_POINT ( 'NONE',  ( 4.527399619855013491, 1.736316896047668701, 0.3745023640388373543 ) ) ;
#11299=CARTESIAN_POINT ( 'NONE',  ( 3.474165694507085345, 2.035929352673752302, -0.3024794417911187416 ) ) ;
#11302=ORIENTED_EDGE ( 'NONE', *, *, #4004, .F. ) ;
#11304=EDGE_LOOP ( 'NONE', ( #6502, #8273, #8845, #12009 ) ) ;
#11305=ORIENTED_EDGE ( 'NONE', *, *, #13053, .T. ) ;
#11307=CARTESIAN_POINT ( 'NONE',  ( 3.394491571325182644, 1.679378605318042395, -1.679378605318058604 ) ) ;
#11308=VERTEX_POINT ( 'NONE', #3676 ) ;
#11309=AXIS2_PLACEMENT_3D ( 'NONE', #2112, #13502, #877 ) ;
#11311=DIRECTION ( 'NONE',  ( 0.000000000000000000, 0.000000000000000000, 1.000000000000000000 ) ) ;
#11313=DIRECTION ( 'NONE',  ( 0.000000000000000000, 0.000000000000000000, -1.000000000000000000 ) ) ;
#11314=ADVANCED_FACE ( 'NONE', ( #7269 ), #9488, .F. ) ;
#11320=CIRCLE ( 'NONE', #10844, 0.3750000000000007772 ) ;
#11322=CARTESIAN_POINT ( 'NONE',  ( 3.426491571325181340, 1.954234464180151676, -0.6847610993685215863 ) ) ;
#11324=CLOSED_SHELL ( 'NONE', ( #5543, #7732, #13081, #11813, #6265, #14347, #9143, #7521, #5631, #2916, #12137, #13984, #11484, #13715, #9788, #3732, #5966, #5542, #8492, #4542, #316, #5928, #3067, #11369, #9674, #8662, #11760, #12157, #457, #496, #2798, #7917, #11844, #11314, #6811, #1859, #12365, #6663, #13735, #7577, #13189, #5571, #7126, #14192, #14484, #10940, #7950, #7975, #10687, #3431, #449, #10913, #9615, #6935, #4230, #13289, #9709, #1617, #7279, #9623, #11797, #10584, #13446, #341, #8175, #6582, #13692, #7094, #745, #13925, #12584, #2696, #4915, #9656, #8973, #13330, #4554, #7007, #13904, #5770, #14736, #15015, #13998, #2557, #6602, #4470, #7783, #9819, #14896, #12438, #4958, #1490, #11508, #11925, #4945, #10762, #11209, #2589, #4499, #10650, #9598, #8124, #10740, #12400, #11119, #6341, #10018, #418, #4802, #5597, #5217, #5845, #6350, #630, #5296, #3827, #2229, #7243, #11548, #3554, #7845, #3187, #7616, #13142, #11864, #12957, #6945, #1169, #7976, #12121 ) ) ;
#11334=DIRECTION ( 'NONE',  ( 0.000000000000000000, -8.723548215061523903E-15, -1.000000000000000000 ) ) ;
#11338=CARTESIAN_POINT ( 'NONE',  ( 2.774999999999999911, -1.679378605318059048, -1.679378605318041950 ) ) ;
#11347=DIRECTION ( 'NONE',  ( 0.000000000000000000, 0.000000000000000000, -1.000000000000000000 ) ) ;
#11348=AXIS2_PLACEMENT_3D ( 'NONE', #2862, #8393, #10901 ) ;
#11349=FACE_OUTER_BOUND ( 'NONE', #11304, .T. ) ;
#11350=EDGE_CURVE ( 'NONE', #8027, #13304, #9019, .T. ) ;
#11351=AXIS2_PLACEMENT_3D ( 'NONE', #14779, #4314, #12792 ) ;
#11354=ORIENTED_EDGE ( 'NONE', *, *, #307, .T. ) ;
#11359=ORIENTED_EDGE ( 'NONE', *, *, #13826, .T. ) ;
#11361=AXIS2_PLACEMENT_3D ( 'NONE', #9949, #738, #13444 ) ;
#11362=AXIS2_PLACEMENT_3D ( 'NONE', #981, #14276, #4679 ) ;
#11365=CARTESIAN_POINT ( 'NONE',  ( 3.394491571325182644, 1.679378605318042395, -1.679378605318058604 ) ) ;
#11366=ORIENTED_EDGE ( 'NONE', *, *, #6713, .T. ) ;
#11367=CARTESIAN_POINT ( 'NONE',  ( 3.167133238847447352, 2.488124734743586863, 0.2437657924683038213 ) ) ;
#11369=ADVANCED_FACE ( 'NONE', ( #7194 ), #13872, .F. ) ;
#11373=AXIS2_PLACEMENT_3D ( 'NONE', #14533, #13529, #7659 ) ;
#11376=CARTESIAN_POINT ( 'NONE',  ( 4.315797241329101475, 3.137999999999999901, 1.570821732971949825 ) ) ;
#11377=EDGE_CURVE ( 'NONE', #11969, #6443, #15112, .T. ) ;
#11378=CARTESIAN_POINT ( 'NONE',  ( 4.392975333536766946, 1.728401786935677142, 0.5451410124394034939 ) ) ;
#11379=CARTESIAN_POINT ( 'NONE',  ( 3.521151862607384775, 2.014578117734890927, -0.3540225754882596609 ) ) ;
#11383=ORIENTED_EDGE ( 'NONE', *, *, #12184, .F. ) ;
#11388=ORIENTED_EDGE ( 'NONE', *, *, #3237, .F. ) ;
#11390=DIRECTION ( 'NONE',  ( -0.3420201433256623846, 0.000000000000000000, -0.9396926207859106484 ) ) ;
#11396=ORIENTED_EDGE ( 'NONE', *, *, #4389, .F. ) ;
#11398=DIRECTION ( 'NONE',  ( -0.000000000000000000, -1.000000000000000000, -0.000000000000000000 ) ) ;
#11399=CARTESIAN_POINT ( 'NONE',  ( 3.537273379829105391, 1.962792557789169390, 0.3716385091526580031 ) ) ;
#11400=CARTESIAN_POINT ( 'NONE',  ( 3.992613899125291521, 1.750100385050365137, -0.7873164154455231101 ) ) ;
#11423=CIRCLE ( 'NONE', #6836, 0.5000000000000001110 ) ;
#11425=CARTESIAN_POINT ( 'NONE',  ( 2.806999999999999496, -1.679378605318041950, 1.416878605318058870 ) ) ;
#11431=CARTESIAN_POINT ( 'NONE',  ( 3.426491571325181340, 2.058905028113295455, 0.2209981660730358233 ) ) ;
#11432=AXIS2_PLACEMENT_3D ( 'NONE', #13175, #6304, #2711 ) ;
#11434=AXIS2_PLACEMENT_3D ( 'NONE', #10471, #14048, #11773 ) ;
#11435=CARTESIAN_POINT ( 'NONE',  ( 3.621938390628993254, 1.891483488391046519, -0.7066767728939699067 ) ) ;
#11444=CARTESIAN_POINT ( 'NONE',  ( 3.874999999999999556, 2.782000000000002693, 1.320000000000000062 ) ) ;
#11446=AXIS2_PLACEMENT_3D ( 'NONE', #5609, #5913, #7891 ) ;
#11455=AXIS2_PLACEMENT_3D ( 'NONE', #5738, #5663, #11390 ) ;
#11456=CARTESIAN_POINT ( 'NONE',  ( 2.774999999999999911, 1.679378605318059048, 1.679378605318041506 ) ) ;
#11457=VECTOR ( 'NONE', #1575, 39.37007874015748143 ) ;
#11458=CARTESIAN_POINT ( 'NONE',  ( 4.641150712690939706, 1.726156072897443661, -0.2600928543580103836 ) ) ;
#11459=EDGE_CURVE ( 'NONE', #4426, #9791, #3393, .T. ) ;
#11460=DIRECTION ( 'NONE',  ( -0.000000000000000000, -1.000000000000000000, -0.000000000000000000 ) ) ;
#11463=CARTESIAN_POINT ( 'NONE',  ( 3.394491571325183088, -1.679378605318041950, 1.416878605318058870 ) ) ;
#11468=VERTEX_POINT ( 'NONE', #13495 ) ;
#11471=CARTESIAN_POINT ( 'NONE',  ( 3.875000000000000444, 1.884022191776434152, -0.5000000000000002220 ) ) ;
#11475=FACE_OUTER_BOUND ( 'NONE', #6781, .T. ) ;
#11478=DIRECTION ( 'NONE',  ( -1.000000000000000000, -0.000000000000000000, -0.000000000000000000 ) ) ;
#11479=CARTESIAN_POINT ( 'NONE',  ( 3.392289215558335957, 0.9914592393105061685, -0.1313972205204200216 ) ) ;
#11484=ADVANCED_FACE ( 'NONE', ( #1721 ), #11943, .F. ) ;
#11485=DIRECTION ( 'NONE',  ( 0.000000000000000000, 0.000000000000000000, -1.000000000000000000 ) ) ;
#11488=ORIENTED_EDGE ( 'NONE', *, *, #582, .F. ) ;
#11490=ORIENTED_EDGE ( 'NONE', *, *, #10895, .F. ) ;
#11491=CARTESIAN_POINT ( 'NONE',  ( 3.426491571325181340, 0.000000000000000000, 0.000000000000000000 ) ) ;
#11492=EDGE_CURVE ( 'NONE', #6091, #11308, #6409, .T. ) ;
#11493=DIRECTION ( 'NONE',  ( 0.000000000000000000, -0.7071067811865568986, -0.7071067811865381358 ) ) ;
#11494=EDGE_CURVE ( 'NONE', #9564, #11740, #7703, .T. ) ;
#11500=FACE_OUTER_BOUND ( 'NONE', #7716, .T. ) ;
#11503=EDGE_LOOP ( 'NONE', ( #2238, #14901, #1377, #10296 ) ) ;
#11504=CARTESIAN_POINT ( 'NONE',  ( 3.426491571325181340, 2.360000000000000320, -0.9800000000000009814 ) ) ;
#11505=CARTESIAN_POINT ( 'NONE',  ( 3.874999999999999556, 3.137999999999999901, -1.320000000000000062 ) ) ;
#11508=ADVANCED_FACE ( 'NONE', ( #7553 ), #13427, .T. ) ;
#11510=EDGE_CURVE ( 'NONE', #3105, #7097, #677, .T. ) ;
#11511=LINE ( 'NONE', #5632, #7326 ) ;
#11513=EDGE_CURVE ( 'NONE', #14596, #9885, #4266, .T. ) ;
#11514=FACE_OUTER_BOUND ( 'NONE', #7603, .T. ) ;
#11515=CARTESIAN_POINT ( 'NONE',  ( 4.049162079869311981, 1.738313153752170992, -0.7765995666616979376 ) ) ;
#11517=ORIENTED_EDGE ( 'NONE', *, *, #255, .F. ) ;
#11518=DIRECTION ( 'NONE',  ( 0.000000000000000000, 0.000000000000000000, -1.000000000000000000 ) ) ;
#11519=EDGE_LOOP ( 'NONE', ( #3789, #9168, #13851, #13270 ) ) ;
#11520=AXIS2_PLACEMENT_3D ( 'NONE', #13665, #168, #2159 ) ;
#11522=DIRECTION ( 'NONE',  ( -1.000000000000000000, -0.000000000000000000, -0.000000000000000000 ) ) ;
#11525=ORIENTED_EDGE ( 'NONE', *, *, #10181, .F. ) ;
#11529=EDGE_CURVE ( 'NONE', #8673, #14941, #13894, .T. ) ;
#11532=CARTESIAN_POINT ( 'NONE',  ( 4.626491436490355547, 1.749163294474629149, 0.03662930866317349460 ) ) ;
#11533=ORIENTED_EDGE ( 'NONE', *, *, #6439, .T. ) ;
#11534=CARTESIAN_POINT ( 'NONE',  ( 2.774999999999999911, 0.000000000000000000, 0.000000000000000000 ) ) ;
#11537=VERTEX_POINT ( 'NONE', #11295 ) ;
#11539=ORIENTED_EDGE ( 'NONE', *, *, #3765, .T. ) ;
#11544=DIRECTION ( 'NONE',  ( 0.000000000000000000, 0.000000000000000000, 1.000000000000000000 ) ) ;
#11547=LINE ( 'NONE', #9103, #6688 ) ;
#11548=ADVANCED_FACE ( 'NONE', ( #9013 ), #1912, .F. ) ;
#11551=CARTESIAN_POINT ( 'NONE',  ( 3.873439288382781065, 3.137999999999999901, 6.065921084684207584E-32 ) ) ;
#11554=CARTESIAN_POINT ( 'NONE',  ( 3.401947036691211679, 0.9867933195744326147, 0.1627677899319876775 ) ) ;
#11555=CARTESIAN_POINT ( 'NONE',  ( 4.313863554662043853, 1.707918880701486009, 0.6659606377349818196 ) ) ;
#11562=DIRECTION ( 'NONE',  ( 0.000000000000000000, 0.000000000000000000, 1.000000000000000000 ) ) ;
#11567=CARTESIAN_POINT ( 'NONE',  ( 3.426491571325181340, 2.360000000000000320, -0.9800000000000009814 ) ) ;
#11571=ORIENTED_EDGE ( 'NONE', *, *, #7380, .T. ) ;
#11574=FACE_OUTER_BOUND ( 'NONE', #1216, .T. ) ;
#11575=ORIENTED_EDGE ( 'NONE', *, *, #6233, .T. ) ;
#11576=EDGE_CURVE ( 'NONE', #2690, #13739, #1957, .T. ) ;
#11577=DIRECTION ( 'NONE',  ( -1.000000000000000000, -0.000000000000000000, -0.000000000000000000 ) ) ;
#11578=EDGE_LOOP ( 'NONE', ( #14032, #2458, #10193, #9955 ) ) ;
#11579=FACE_OUTER_BOUND ( 'NONE', #12336, .T. ) ;
#11581=VECTOR ( 'NONE', #7128, 39.37007874015748143 ) ;
#11584=CARTESIAN_POINT ( 'NONE',  ( 4.215098385813337067, 1.784975328382307769, -0.6693622412112683051 ) ) ;
#11585=AXIS2_PLACEMENT_3D ( 'NONE', #3213, #894, #4439 ) ;
#11586=DIRECTION ( 'NONE',  ( 0.000000000000000000, 0.000000000000000000, 1.000000000000000000 ) ) ;
#11588=CARTESIAN_POINT ( 'NONE',  ( 3.706496129713269916, 1.834319089984349116, -0.7862230264085732223 ) ) ;
#11589=ORIENTED_EDGE ( 'NONE', *, *, #5525, .T. ) ;
#11590=ORIENTED_EDGE ( 'NONE', *, *, #4165, .T. ) ;
#11593=VERTEX_POINT ( 'NONE', #10303 ) ;
#11596=( NAMED_UNIT ( * ) SI_UNIT ( $, .STERADIAN. ) SOLID_ANGLE_UNIT ( ) );
#11598=VECTOR ( 'NONE', #5626, 39.37007874015748143 ) ;
#11599=DIRECTION ( 'NONE',  ( 0.000000000000000000, 0.000000000000000000, 1.000000000000000000 ) ) ;
#11601=CARTESIAN_POINT ( 'NONE',  ( 3.161631830458323744, 2.489685336282108086, -0.2285170720271093858 ) ) ;
#11604=CARTESIAN_POINT ( 'NONE',  ( 3.394491571325180423, -1.679378605318059048, -1.679378605318041950 ) ) ;
#11606=CIRCLE ( 'NONE', #2815, 0.5000000000000001110 ) ;
#11607=CARTESIAN_POINT ( 'NONE',  ( 4.682886128176067864, 1.732772449459274888, 0.07708318348993609126 ) ) ;
#11609=CIRCLE ( 'NONE', #3797, 1.000000000000000222 ) ;
#11612=AXIS2_PLACEMENT_3D ( 'NONE', #665, #5366, #10032 ) ;
#11615=VERTEX_POINT ( 'NONE', #12505 ) ;
#11616=ORIENTED_EDGE ( 'NONE', *, *, #6620, .F. ) ;
#11621=CARTESIAN_POINT ( 'NONE',  ( 4.769268701363833074, 3.137999999999999901, 0.3249191361593796734 ) ) ;
#11627=DIRECTION ( 'NONE',  ( 0.7071067811865429098, 0.000000000000000000, -0.7071067811865521247 ) ) ;
#11630=CARTESIAN_POINT ( 'NONE',  ( 3.426491571325181340, -2.399999999999999911, 0.7000000000000007327 ) ) ;
#11632=CARTESIAN_POINT ( 'NONE',  ( 3.697049110852476339, 0.8839984663495870088, 0.4675429765723205788 ) ) ;
#11634=AXIS2_PLACEMENT_3D ( 'NONE', #14222, #210, #11722 ) ;
#11635=ORIENTED_EDGE ( 'NONE', *, *, #7488, .F. ) ;
#11641=AXIS2_PLACEMENT_3D ( 'NONE', #11750, #1249, #5935 ) ;
#11643=ORIENTED_EDGE ( 'NONE', *, *, #8215, .T. ) ;
#11646=DIRECTION ( 'NONE',  ( 0.000000000000000000, 0.000000000000000000, -1.000000000000000000 ) ) ;
#11651=DIRECTION ( 'NONE',  ( 0.000000000000000000, 0.000000000000000000, -1.000000000000000000 ) ) ;
#11653=DIRECTION ( 'NONE',  ( -1.000000000000000000, -0.000000000000000000, -0.000000000000000000 ) ) ;
#11654=ORIENTED_EDGE ( 'NONE', *, *, #501, .F. ) ;
#11657=CYLINDRICAL_SURFACE ( 'NONE', #5468, 0.2624999999999997335 ) ;
#11667=CARTESIAN_POINT ( 'NONE',  ( 3.566714410367414434, 1.985790321547726833, -0.6832061603422943108 ) ) ;
#11670=CIRCLE ( 'NONE', #5567, 0.2625000000000000111 ) ;
#11678=LINE ( 'NONE', #1183, #9245 ) ;
#11681=CIRCLE ( 'NONE', #14606, 2.500000000000000000 ) ;
#11684=CARTESIAN_POINT ( 'NONE',  ( 3.875000000000000000, 1.059999999999999165, 0.000000000000000000 ) ) ;
#11689=EDGE_CURVE ( 'NONE', #7182, #4577, #13902, .T. ) ;
#11690=VECTOR ( 'NONE', #9234, 39.37007874015748143 ) ;
#11691=CARTESIAN_POINT ( 'NONE',  ( 4.489587877062135135, 1.733016502558613725, -0.4335731954417103573 ) ) ;
#11695=ORIENTED_EDGE ( 'NONE', *, *, #4004, .T. ) ;
#11700=FACE_BOUND ( 'NONE', #569, .T. ) ;
#11702=CIRCLE ( 'NONE', #9743, 0.1899999999999996136 ) ;
#11720=MECHANICAL_DESIGN_GEOMETRIC_PRESENTATION_REPRESENTATION('',(#6345),#8547);
#11721=DIRECTION ( 'NONE',  ( -1.000000000000000000, -0.000000000000000000, -0.000000000000000000 ) ) ;
#11722=DIRECTION ( 'NONE',  ( 0.000000000000000000, 0.000000000000000000, 1.000000000000000000 ) ) ;
#11728=EDGE_LOOP ( 'NONE', ( #8943, #5784 ) ) ;
#11734=EDGE_CURVE ( 'NONE', #6033, #10976, #5617, .T. ) ;
#11736=DIRECTION ( 'NONE',  ( 0.000000000000000000, 0.000000000000000000, -1.000000000000000000 ) ) ;
#11740=VERTEX_POINT ( 'NONE', #29 ) ;
#11742=ORIENTED_EDGE ( 'NONE', *, *, #4165, .F. ) ;
#11746=CARTESIAN_POINT ( 'NONE',  ( 2.774999999999999911, 0.000000000000000000, 1.039370078740158965 ) ) ;
#11747=CARTESIAN_POINT ( 'NONE',  ( 3.874999999999999556, 2.782000000000002693, 1.130000000000000560 ) ) ;
#11748=ORIENTED_EDGE ( 'NONE', *, *, #5436, .T. ) ;
#11750=CARTESIAN_POINT ( 'NONE',  ( 6.215861650065340527, 0.000000000000000000, 0.000000000000000000 ) ) ;
#11751=LINE ( 'NONE', #1020, #3856 ) ;
#11755=VECTOR ( 'NONE', #2577, 39.37007874015748143 ) ;
#11756=CARTESIAN_POINT ( 'NONE',  ( 3.592530085043205368, 1.950116979243637028, -0.4132115743265128982 ) ) ;
#11759=EDGE_CURVE ( 'NONE', #7512, #11167, #6986, .T. ) ;
#11760=ADVANCED_FACE ( 'NONE', ( #1487 ), #6170, .F. ) ;
#11762=DIRECTION ( 'NONE',  ( 0.000000000000000000, 1.000000000000000000, 0.000000000000000000 ) ) ;
#11764=CIRCLE ( 'NONE', #11520, 2.960629921259841257 ) ;
#11765=CARTESIAN_POINT ( 'NONE',  ( 4.605209778948695210, 1.806214611443159646, 0.1785906071940129292 ) ) ;
#11767=DIRECTION ( 'NONE',  ( -1.000000000000000000, -0.000000000000000000, -0.000000000000000000 ) ) ;
#11773=DIRECTION ( 'NONE',  ( 0.000000000000000000, 0.000000000000000000, -1.000000000000000000 ) ) ;
#11775=FACE_OUTER_BOUND ( 'NONE', #4523, .T. ) ;
#11777=LINE ( 'NONE', #11994, #12389 ) ;
#11779=CARTESIAN_POINT ( 'NONE',  ( 6.208491571325183145, 1.679378605318035733, -2.054378605318066153 ) ) ;
#11781=CARTESIAN_POINT ( 'NONE',  ( 3.426491571325181340, 2.360000000000015863, 0.9799999999999454703 ) ) ;
#11783=DIRECTION ( 'NONE',  ( 1.000000000000000000, 0.000000000000000000, 0.000000000000000000 ) ) ;
#11785=CARTESIAN_POINT ( 'NONE',  ( 4.585000156914120772, 1.718796672713930551, -0.3806726929799386094 ) ) ;
#11786=ORIENTED_EDGE ( 'NONE', *, *, #2996, .F. ) ;
#11787=DIRECTION ( 'NONE',  ( 1.000000000000000000, 0.000000000000000000, 0.000000000000000000 ) ) ;
#11789=EDGE_LOOP ( 'NONE', ( #2032, #10515, #717, #8104 ) ) ;
#11790=ORIENTED_EDGE ( 'NONE', *, *, #6431, .F. ) ;
#11792=CARTESIAN_POINT ( 'NONE',  ( 3.426491571325181340, 0.000000000000000000, 1.000000000000000000 ) ) ;
#11794=CARTESIAN_POINT ( 'NONE',  ( 4.344846310392954436, 3.137999999999999901, 1.491010071662831171 ) ) ;
#11797=ADVANCED_FACE ( 'NONE', ( #3875 ), #1780, .F. ) ;
#11799=DIRECTION ( 'NONE',  ( 0.000000000000000000, 0.000000000000000000, -1.000000000000000000 ) ) ;
#11802=CARTESIAN_POINT ( 'NONE',  ( 3.437516310781153273, 2.055659281767487023, -0.6089580415532643842 ) ) ;
#11806=DIRECTION ( 'NONE',  ( 0.000000000000000000, 0.000000000000000000, -1.000000000000000000 ) ) ;
#11808=AXIS2_PLACEMENT_3D ( 'NONE', #11338, #4393, #14938 ) ;
#11810=EDGE_LOOP ( 'NONE', ( #5064, #13651, #964, #1442 ) ) ;
#11813=ADVANCED_FACE ( 'NONE', ( #12123 ), #12688, .F. ) ;
#11816=DIRECTION ( 'NONE',  ( 0.000000000000000000, 0.000000000000000000, -1.000000000000000000 ) ) ;
#11817=LINE ( 'NONE', #7012, #14803 ) ;
#11822=CIRCLE ( 'NONE', #13498, 1.502725933896874810 ) ;
#11824=CARTESIAN_POINT ( 'NONE',  ( 3.426491571325181784, 2.032298649151902392, 0.6051796186069025030 ) ) ;
#11830=CARTESIAN_POINT ( 'NONE',  ( 3.573766445277532622, 1.954426848217328594, -0.3997464416171771506 ) ) ;
#11831=DIRECTION ( 'NONE',  ( -0.000000000000000000, -1.000000000000000000, -0.000000000000000000 ) ) ;
#11832=CARTESIAN_POINT ( 'NONE',  ( 3.426491571325181340, 2.359999999999993214, -1.575000000000016831 ) ) ;
#11842=EDGE_CURVE ( 'NONE', #4719, #6847, #10983, .T. ) ;
#11844=ADVANCED_FACE ( 'NONE', ( #12048 ), #1629, .F. ) ;
#11845=FACE_BOUND ( 'NONE', #4466, .T. ) ;
#11846=ORIENTED_EDGE ( 'NONE', *, *, #6878, .F. ) ;
#11849=CARTESIAN_POINT ( 'NONE',  ( 3.874999999999999556, 2.750000000000000000, -1.320000000000000062 ) ) ;
#11850=CARTESIAN_POINT ( 'NONE',  ( 3.544732980980179970, 1.997075164250705859, 0.6728923706171071606 ) ) ;
#11851=LINE ( 'NONE', #7346, #9635 ) ;
#11852=EDGE_CURVE ( 'NONE', #4913, #7544, #5860, .T. ) ;
#11853=AXIS2_PLACEMENT_3D ( 'NONE', #7801, #4585, #4508 ) ;
#11855=AXIS2_PLACEMENT_3D ( 'NONE', #3006, #2072, #7827 ) ;
#11858=CARTESIAN_POINT ( 'NONE',  ( 4.681089581896493712, 1.732453011165680401, 0.09841563256873263332 ) ) ;
#11864=ADVANCED_FACE ( 'NONE', ( #705 ), #12433, .T. ) ;
#11865=DIRECTION ( 'NONE',  ( -0.000000000000000000, 1.000000000000000000, -0.000000000000000000 ) ) ;
#11866=CARTESIAN_POINT ( 'NONE',  ( 2.774999999999999911, 2.399999999999999911, -0.7000000000000007327 ) ) ;
#11868=ORIENTED_EDGE ( 'NONE', *, *, #11377, .T. ) ;
#11869=FACE_OUTER_BOUND ( 'NONE', #12013, .T. ) ;
#11870=CIRCLE ( 'NONE', #5260, 2.960629921259841257 ) ;
#11871=CONICAL_SURFACE ( 'NONE', #363, 0.4070000000000022489, 0.7853981633974547183 ) ;
#11876=AXIS2_PLACEMENT_3D ( 'NONE', #824, #5674, #4378 ) ;
#11880=DIRECTION ( 'NONE',  ( 0.000000000000000000, 0.000000000000000000, 1.000000000000000000 ) ) ;
#11882=EDGE_LOOP ( 'NONE', ( #6647, #1145, #4621, #11071, #11354, #4985, #5554, #12772, #928 ) ) ;
#11890=CARTESIAN_POINT ( 'NONE',  ( 6.176491571325181340, -1.679378605318047946, -1.272378605318051248 ) ) ;
#11894=ORIENTED_EDGE ( 'NONE', *, *, #3103, .F. ) ;
#11904=CIRCLE ( 'NONE', #4080, 0.5000000000000001110 ) ;
#11906=DIRECTION ( 'NONE',  ( 0.000000000000000000, 0.000000000000000000, -1.000000000000000000 ) ) ;
#11907=DIRECTION ( 'NONE',  ( 0.000000000000000000, -1.224646799147354933E-16, 1.000000000000000000 ) ) ;
#11910=CARTESIAN_POINT ( 'NONE',  ( 6.826491571325181695, 1.272861240058668140E-16, 1.039370078740158965 ) ) ;
#11911=ORIENTED_EDGE ( 'NONE', *, *, #4610, .T. ) ;
#11913=DIRECTION ( 'NONE',  ( -0.7071067811865450192, 0.000000000000000000, 0.7071067811865499042 ) ) ;
#11915=CARTESIAN_POINT ( 'NONE',  ( 3.874999999999999556, 3.137999999999999901, -1.320000000000000062 ) ) ;
#11921=DIRECTION ( 'NONE',  ( -0.000000000000000000, -1.000000000000000000, -0.000000000000000000 ) ) ;
#11923=DIRECTION ( 'NONE',  ( 0.000000000000000000, 0.000000000000000000, 1.000000000000000000 ) ) ;
#11924=CONICAL_SURFACE ( 'NONE', #4606, 0.1899999999999996136, 0.7853981633974435050 ) ;
#11925=ADVANCED_FACE ( 'NONE', ( #9220 ), #3323, .T. ) ;
#11929=CARTESIAN_POINT ( 'NONE',  ( 3.546155925590385838, 1.898807144323297003, 0.7421470037383380847 ) ) ;
#11933=DIRECTION ( 'NONE',  ( 0.000000000000000000, 0.000000000000000000, 1.000000000000000000 ) ) ;
#11937=CIRCLE ( 'NONE', #3880, 0.7500000000000001110 ) ;
#11941=VECTOR ( 'NONE', #10879, 39.37007874015748143 ) ;
#11943=CONICAL_SURFACE ( 'NONE', #6100, 0.3750000000000004996, 0.7853981633974376209 ) ;
#11944=DIRECTION ( 'NONE',  ( 0.000000000000000000, 1.000000000000000000, -2.708891287835076134E-14 ) ) ;
#11945=VECTOR ( 'NONE', #12238, 39.37007874015748143 ) ;
#11947=AXIS2_PLACEMENT_3D ( 'NONE', #7561, #7415, #3752 ) ;
#11951=EDGE_CURVE ( 'NONE', #3309, #5002, #12643, .T. ) ;
#11955=EDGE_LOOP ( 'NONE', ( #10880, #4274, #9170, #4773 ) ) ;
#11967=DIRECTION ( 'NONE',  ( -1.000000000000000000, -0.000000000000000000, -0.000000000000000000 ) ) ;
#11969=VERTEX_POINT ( 'NONE', #14873 ) ;
#11970=ORIENTED_EDGE ( 'NONE', *, *, #8020, .T. ) ;
#11973=CIRCLE ( 'NONE', #1940, 0.1899999999999996136 ) ;
#11974=CARTESIAN_POINT ( 'NONE',  ( 2.814370078740158210, 0.000000000000000000, 0.000000000000000000 ) ) ;
#11975=DIRECTION ( 'NONE',  ( -1.000000000000000000, -0.000000000000000000, -0.000000000000000000 ) ) ;
#11976=EDGE_CURVE ( 'NONE', #6847, #3928, #6359, .T. ) ;
#11978=CARTESIAN_POINT ( 'NONE',  ( 2.774999999999999911, 0.9799999999999438050, -2.360000000000016307 ) ) ;
#11980=CARTESIAN_POINT ( 'NONE',  ( 3.875000000000000444, 1.884022191776434152, -0.5000000000000002220 ) ) ;
#11984=EDGE_LOOP ( 'NONE', ( #2117, #8254 ) ) ;
#11989=CARTESIAN_POINT ( 'NONE',  ( 5.567023771132172172, 0.000000000000000000, 0.000000000000000000 ) ) ;
#11990=CARTESIAN_POINT ( 'NONE',  ( 3.426491571325181340, 1.679378605318042395, -1.416878605318058870 ) ) ;
#11994=CARTESIAN_POINT ( 'NONE',  ( 3.426491571325181340, -2.360000000000021636, -1.574999999999999734 ) ) ;
#11996=EDGE_CURVE ( 'NONE', #3733, #12843, #7162, .T. ) ;
#11998=DIRECTION ( 'NONE',  ( -1.000000000000000000, -0.000000000000000000, -0.000000000000000000 ) ) ;
#11999=AXIS2_PLACEMENT_3D ( 'NONE', #7913, #2009, #856 ) ;
#12000=CARTESIAN_POINT ( 'NONE',  ( 2.774999999999999911, -1.679378605318041950, 1.679378605318059048 ) ) ;
#12001=B_SPLINE_CURVE_WITH_KNOTS ( 'NONE', 3,
 ( #12399, #13618, #10480, #10047, #13903, #13536, #14704, #3081, #6604, #1920 ),
 .UNSPECIFIED., .F., .F.,
 ( 4, 2, 2, 2, 4 ),
 ( 0.07367938960722780761, 0.07700688573806144244, 0.08033438186889507726, 0.08366187799972872596, 0.08698937413056236079 ),
 .UNSPECIFIED. ) ;
#12003=CARTESIAN_POINT ( 'NONE',  ( 3.400138847590578273, 1.967011420863446824, 0.6697528156307519520 ) ) ;
#12004=DIRECTION ( 'NONE',  ( 1.000000000000000000, 0.000000000000000000, 0.000000000000000000 ) ) ;
#12005=ORIENTED_EDGE ( 'NONE', *, *, #13053, .F. ) ;
#12008=FACE_BOUND ( 'NONE', #5514, .T. ) ;
#12009=ORIENTED_EDGE ( 'NONE', *, *, #6617, .F. ) ;
#12013=EDGE_LOOP ( 'NONE', ( #7471, #3738, #15077, #10043 ) ) ;
#12014=AXIS2_PLACEMENT_3D ( 'NONE', #8612, #13110, #7531 ) ;
#12015=CARTESIAN_POINT ( 'NONE',  ( 6.208491571325183145, -1.679378605318047946, -2.054378605318054163 ) ) ;
#12016=EDGE_CURVE ( 'NONE', #12243, #11081, #2930, .T. ) ;
#12019=ORIENTED_EDGE ( 'NONE', *, *, #13476, .T. ) ;
#12023=CARTESIAN_POINT ( 'NONE',  ( 3.426491571325181340, -1.679378605318041950, 1.941878605318059003 ) ) ;
#12024=PRODUCT ( 'Inlet Housing', 'Inlet Housing', '', ( #13268 ) ) ;
#12025=DIRECTION ( 'NONE',  ( -1.000000000000000000, -0.000000000000000000, -0.000000000000000000 ) ) ;
#12028=VERTEX_POINT ( 'NONE', #3780 ) ;
#12030=LINE ( 'NONE', #1539, #7088 ) ;
#12033=LINE ( 'NONE', #14402, #1696 ) ;
#12040=AXIS2_PLACEMENT_3D ( 'NONE', #8747, #4166, #2857 ) ;
#12041=EDGE_LOOP ( 'NONE', ( #3026, #12736, #2224, #13560 ) ) ;
#12043=EDGE_LOOP ( 'NONE', ( #10797, #575, #1665, #1295 ) ) ;
#12048=FACE_OUTER_BOUND ( 'NONE', #11789, .T. ) ;
#12050=CARTESIAN_POINT ( 'NONE',  ( 3.875000000000000000, 3.137999999999999901, 0.000000000000000000 ) ) ;
#12053=CIRCLE ( 'NONE', #4986, 2.500000000000000444 ) ;
#12060=DIRECTION ( 'NONE',  ( -1.000000000000000000, -0.000000000000000000, -0.000000000000000000 ) ) ;
#12065=DIRECTION ( 'NONE',  ( 1.000000000000000000, 0.000000000000000000, 0.000000000000000000 ) ) ;
#12066=CARTESIAN_POINT ( 'NONE',  ( 3.426491571325181340, 2.426945040795776443, 0.5999481385559803925 ) ) ;
#12068=DIRECTION ( 'NONE',  ( 1.000000000000000000, 0.000000000000000000, 0.000000000000000000 ) ) ;
#12072=CARTESIAN_POINT ( 'NONE',  ( 3.521351135077507521, 2.009251905947152306, 0.6613697195036538634 ) ) ;
#12073=DIRECTION ( 'NONE',  ( 1.000000000000000000, 0.000000000000000000, 0.000000000000000000 ) ) ;
#12076=LINE ( 'NONE', #14442, #9918 ) ;
#12077=DIRECTION ( 'NONE',  ( 0.000000000000000000, 0.000000000000000000, -1.000000000000000000 ) ) ;
#12083=CYLINDRICAL_SURFACE ( 'NONE', #6320, 0.7500000000000001110 ) ;
#12086=CIRCLE ( 'NONE', #4775, 0.2220000000000021678 ) ;
#12092=CARTESIAN_POINT ( 'NONE',  ( 6.794491571325179891, -1.679378605318047946, -2.054378605318054163 ) ) ;
#12095=AXIS2_PLACEMENT_3D ( 'NONE', #117, #1347, #1201 ) ;
#12102=FACE_OUTER_BOUND ( 'NONE', #6777, .T. ) ;
#12107=CIRCLE ( 'NONE', #13086, 0.2219999999999999751 ) ;
#12109=DIRECTION ( 'NONE',  ( 0.000000000000000000, 1.000000000000000000, 0.000000000000000000 ) ) ;
#12110=EDGE_CURVE ( 'NONE', #6131, #4759, #459, .T. ) ;
#12111=CARTESIAN_POINT ( 'NONE',  ( 3.874999999999999556, 3.137999999999999901, -1.320000000000000062 ) ) ;
#12113=ORIENTED_EDGE ( 'NONE', *, *, #3480, .F. ) ;
#12114=VERTEX_POINT ( 'NONE', #11105 ) ;
#12119=AXIS2_PLACEMENT_3D ( 'NONE', #5545, #12556, #10058 ) ;
#12121=ADVANCED_FACE ( 'NONE', ( #301 ), #9764, .F. ) ;
#12123=FACE_OUTER_BOUND ( 'NONE', #12041, .T. ) ;
#12124=DIRECTION ( 'NONE',  ( 0.000000000000000000, 0.000000000000000000, -1.000000000000000000 ) ) ;
#12125=CARTESIAN_POINT ( 'NONE',  ( 4.247991639008878550, 1.782319238603491174, -0.6520378312758601247 ) ) ;
#12126=AXIS2_PLACEMENT_3D ( 'NONE', #7796, #731, #6649 ) ;
#12128=EDGE_CURVE ( 'NONE', #5697, #3188, #4160, .T. ) ;
#12130=CARTESIAN_POINT ( 'NONE',  ( 4.508361655903602383, 1.711445479664179592, -0.4931022144224059822 ) ) ;
#12131=ORIENTED_EDGE ( 'NONE', *, *, #12366, .T. ) ;
#12135=CARTESIAN_POINT ( 'NONE',  ( 3.426491571325181340, 1.679378605318042395, -1.679378605318058604 ) ) ;
#12136=DIRECTION ( 'NONE',  ( 0.000000000000000000, 0.000000000000000000, 1.000000000000000000 ) ) ;
#12137=ADVANCED_FACE ( 'NONE', ( #7379 ), #7814, .F. ) ;
#12140=DIRECTION ( 'NONE',  ( 0.000000000000000000, -4.591341165822195764E-16, -1.000000000000000000 ) ) ;
#12142=DIRECTION ( 'NONE',  ( -1.000000000000000000, -0.000000000000000000, -0.000000000000000000 ) ) ;
#12147=DIRECTION ( 'NONE',  ( 1.000000000000000000, 0.000000000000000000, 0.000000000000000000 ) ) ;
#12149=CARTESIAN_POINT ( 'NONE',  ( 3.441224298305551432, 1.974937406882123714, 0.6122973898694716866 ) ) ;
#12153=CARTESIAN_POINT ( 'NONE',  ( 3.426491571325181340, 1.963962403007655677, 0.6625976281079839492 ) ) ;
#12154=DIRECTION ( 'NONE',  ( -1.000000000000000000, -0.000000000000000000, -0.000000000000000000 ) ) ;
#12155=ORIENTED_EDGE ( 'NONE', *, *, #9984, .T. ) ;
#12156=ORIENTED_EDGE ( 'NONE', *, *, #5955, .F. ) ;
#12157=ADVANCED_FACE ( 'NONE', ( #12102 ), #3995, .F. ) ;
#12163=EDGE_CURVE ( 'NONE', #14925, #1229, #5629, .T. ) ;
#12168=DIRECTION ( 'NONE',  ( 1.000000000000000000, 0.000000000000000000, 0.000000000000000000 ) ) ;
#12170=DIRECTION ( 'NONE',  ( 1.000000000000000000, 0.000000000000000000, 0.000000000000000000 ) ) ;
#12182=DIRECTION ( 'NONE',  ( 0.000000000000000000, 0.000000000000000000, -1.000000000000000000 ) ) ;
#12184=EDGE_CURVE ( 'NONE', #5449, #14644, #1695, .T. ) ;
#12186=CIRCLE ( 'NONE', #10735, 1.000000000000000222 ) ;
#12189=CIRCLE ( 'NONE', #2915, 0.7849999999999969225 ) ;
#12190=CARTESIAN_POINT ( 'NONE',  ( 6.787121492585022509, 0.000000000000000000, 3.000000000000000444 ) ) ;
#12191=EDGE_LOOP ( 'NONE', ( #13812, #7770, #2384, #3232 ) ) ;
#12192=ORIENTED_EDGE ( 'NONE', *, *, #9984, .F. ) ;
#12198=CARTESIAN_POINT ( 'NONE',  ( 3.394491571325180423, -1.679378605318059048, -1.679378605318041950 ) ) ;
#12204=VERTEX_POINT ( 'NONE', #2710 ) ;
#12206=CARTESIAN_POINT ( 'NONE',  ( 2.774999999999999911, 1.272861240058668140E-16, -1.039370078740158965 ) ) ;
#12208=CARTESIAN_POINT ( 'NONE',  ( 4.374151734133344682, 0.9995751005560787883, 0.03350973656221049174 ) ) ;
#12212=CARTESIAN_POINT ( 'NONE',  ( 3.426491571325181340, 2.058905028113295455, -0.2209981660730358233 ) ) ;
#12213=CARTESIAN_POINT ( 'NONE',  ( 3.265716245508940574, 2.461786362941181139, 0.4361376382133447804 ) ) ;
#12216=EDGE_CURVE ( 'NONE', #8675, #6443, #12033, .T. ) ;
#12220=CARTESIAN_POINT ( 'NONE',  ( 6.826491571325181695, 0.000000000000000000, 2.960629921259841257 ) ) ;
#12221=EDGE_CURVE ( 'NONE', #7301, #14777, #8740, .T. ) ;
#12223=DIRECTION ( 'NONE',  ( 0.000000000000000000, 0.000000000000000000, -1.000000000000000000 ) ) ;
#12227=CARTESIAN_POINT ( 'NONE',  ( 5.567023771132172172, 0.000000000000000000, 1.500000000000000222 ) ) ;
#12233=DIRECTION ( 'NONE',  ( -1.000000000000000000, -0.000000000000000000, -0.000000000000000000 ) ) ;
#12235=AXIS2_PLACEMENT_3D ( 'NONE', #5188, #274, #10854 ) ;
#12236=DIMENSIONAL_EXPONENTS ( 1.000000000000000000, 0.000000000000000000, 0.000000000000000000, 0.000000000000000000, 0.000000000000000000, 0.000000000000000000, 0.000000000000000000 ) ;
#12238=DIRECTION ( 'NONE',  ( -0.7071067811865460184, 0.000000000000000000, 0.7071067811865490160 ) ) ;
#12240=DIRECTION ( 'NONE',  ( 1.000000000000000000, 0.000000000000000000, 0.000000000000000000 ) ) ;
#12243=VERTEX_POINT ( 'NONE', #2778 ) ;
#12244=CARTESIAN_POINT ( 'NONE',  ( 4.250664904820700585, 0.9439471567310199207, -0.3303580885322055516 ) ) ;
#12249=ORIENTED_EDGE ( 'NONE', *, *, #14591, .F. ) ;
#12251=CARTESIAN_POINT ( 'NONE',  ( 6.794491571325179891, -1.679378605318048390, 1.679378605318054163 ) ) ;
#12254=LINE ( 'NONE', #4236, #6567 ) ;
#12269=CARTESIAN_POINT ( 'NONE',  ( 3.944129661530210385, 1.867491090171841339, -0.4951980309903490363 ) ) ;
#12270=VECTOR ( 'NONE', #4849, 39.37007874015748143 ) ;
#12271=ORIENTED_EDGE ( 'NONE', *, *, #12869, .F. ) ;
#12274=EDGE_LOOP ( 'NONE', ( #3418, #12386, #5583, #3566 ) ) ;
#12282=ORIENTED_EDGE ( 'NONE', *, *, #13411, .T. ) ;
#12283=DIRECTION ( 'NONE',  ( 0.000000000000000000, 0.000000000000000000, -1.000000000000000000 ) ) ;
#12284=CARTESIAN_POINT ( 'NONE',  ( 3.283006985701197866, 2.457536269194010359, 0.4593688321371918737 ) ) ;
#12285=DIRECTION ( 'NONE',  ( -1.000000000000000000, -0.000000000000000000, -0.000000000000000000 ) ) ;
#12286=VECTOR ( 'NONE', #8903, 39.37007874015748143 ) ;
#12289=CARTESIAN_POINT ( 'NONE',  ( 4.544485495091622695, 1.738146795016368262, 0.3429988673886200101 ) ) ;
#12301=LINE ( 'NONE', #435, #3555 ) ;
#12305=EDGE_CURVE ( 'NONE', #9581, #1151, #4305, .T. ) ;
#12306=DIRECTION ( 'NONE',  ( 0.000000000000000000, 0.000000000000000000, -1.000000000000000000 ) ) ;
#12308=CARTESIAN_POINT ( 'NONE',  ( 6.826491571325181695, 1.679378605318035733, -1.272378605318063016 ) ) ;
#12317=EDGE_CURVE ( 'NONE', #694, #12204, #11973, .T. ) ;
#12324=DIRECTION ( 'NONE',  ( 0.000000000000000000, 9.641816448226552334E-15, 1.000000000000000000 ) ) ;
#12336=EDGE_LOOP ( 'NONE', ( #8545, #14765, #13360, #9291 ) ) ;
#12342=AXIS2_PLACEMENT_3D ( 'NONE', #8146, #11577, #2316 ) ;
#12343=CARTESIAN_POINT ( 'NONE',  ( 3.426491571325181340, 1.954234464180151676, -0.6847610993685215863 ) ) ;
#12348=EDGE_CURVE ( 'NONE', #8207, #4719, #12001, .T. ) ;
#12349=ORIENTED_EDGE ( 'NONE', *, *, #11759, .T. ) ;
#12357=CARTESIAN_POINT ( 'NONE',  ( 4.370923089943242523, 0.9979667740156152878, -0.06586474272559393606 ) ) ;
#12358=CARTESIAN_POINT ( 'NONE',  ( 6.826491571325181695, -1.679378605318048390, 1.679378605318054163 ) ) ;
#12361=DIRECTION ( 'NONE',  ( 0.000000000000000000, -1.000000000000000000, 0.000000000000000000 ) ) ;
#12365=ADVANCED_FACE ( 'NONE', ( #3512 ), #9339, .T. ) ;
#12366=EDGE_CURVE ( 'NONE', #694, #6001, #5455, .T. ) ;
#12369=CARTESIAN_POINT ( 'NONE',  ( 4.351048328242368868, 1.728421760757865355, 0.5811182005463045863 ) ) ;
#12370=CARTESIAN_POINT ( 'NONE',  ( 3.781939775458268205, 1.913296957465108861, -0.4918119683718932267 ) ) ;
#12371=ORIENTED_EDGE ( 'NONE', *, *, #9917, .F. ) ;
#12374=ORIENTED_EDGE ( 'NONE', *, *, #7664, .T. ) ;
#12377=VERTEX_POINT ( 'NONE', #3439 ) ;
#12379=DIRECTION ( 'NONE',  ( 0.000000000000000000, 0.000000000000000000, -1.000000000000000000 ) ) ;
#12380=ORIENTED_EDGE ( 'NONE', *, *, #14106, .T. ) ;
#12381=CARTESIAN_POINT ( 'NONE',  ( 6.826491571325181695, 0.000000000000000000, 0.000000000000000000 ) ) ;
#12385=CARTESIAN_POINT ( 'NONE',  ( 2.774999999999999911, 0.9799999999999436939, -3.360000000000016751 ) ) ;
#12386=ORIENTED_EDGE ( 'NONE', *, *, #3641, .T. ) ;
#12388=CARTESIAN_POINT ( 'NONE',  ( 3.426585660050375903, 0.9751674090406495798, -0.2235762390674587985 ) ) ;
#12389=VECTOR ( 'NONE', #47, 39.37007874015748143 ) ;
#12390=CARTESIAN_POINT ( 'NONE',  ( 4.373886831741767622, 1.706962534117436592, -0.6224998300045747612 ) ) ;
#12391=VERTEX_POINT ( 'NONE', #6892 ) ;
#12393=CARTESIAN_POINT ( 'NONE',  ( 3.426491571325181340, -0.6999999999999587663, 2.400000000000012790 ) ) ;
#12398=CIRCLE ( 'NONE', #9495, 0.3750000000000004996 ) ;
#12399=CARTESIAN_POINT ( 'NONE',  ( 3.876560711617219823, 1.855806856933289506, -0.7500000000000001110 ) ) ;
#12400=ADVANCED_FACE ( 'NONE', ( #8114 ), #5879, .F. ) ;
#12404=CARTESIAN_POINT ( 'NONE',  ( 3.426491571325181340, 3.360000000000000320, -0.9800000000000012035 ) ) ;
#12405=EDGE_CURVE ( 'NONE', #3309, #12028, #13672, .T. ) ;
#12406=DIRECTION ( 'NONE',  ( 0.000000000000000000, -1.000000000000000000, 0.000000000000000000 ) ) ;
#12407=VERTEX_POINT ( 'NONE', #3820 ) ;
#12408=AXIS2_PLACEMENT_3D ( 'NONE', #12358, #11219, #716 ) ;
#12420=CIRCLE ( 'NONE', #10478, 0.5000000000000001110 ) ;
#12424=VECTOR ( 'NONE', #7045, 39.37007874015748143 ) ;
#12426=CARTESIAN_POINT ( 'NONE',  ( 4.064979089242817700, 1.806308836204446822, 0.7263547114196443610 ) ) ;
#12430=EDGE_LOOP ( 'NONE', ( #12819, #10604 ) ) ;
#12432=EDGE_CURVE ( 'NONE', #7033, #14200, #11239, .T. ) ;
#12433=CONICAL_SURFACE ( 'NONE', #13409, 2.960629921259841257, 0.7853981633974552734 ) ;
#12438=ADVANCED_FACE ( 'NONE', ( #12916 ), #3678, .F. ) ;
#12442=CARTESIAN_POINT ( 'NONE',  ( 2.774999999999999911, -1.575000000000027489, -1.574999999999989297 ) ) ;
#12444=CARTESIAN_POINT ( 'NONE',  ( 3.394491571325183088, 1.679378605318059048, 1.679378605318041506 ) ) ;
#12445=CARTESIAN_POINT ( 'NONE',  ( 4.529882331337859114, 1.713284349967738818, 0.4645268969338811615 ) ) ;
#12451=VERTEX_POINT ( 'NONE', #11779 ) ;
#12458=CARTESIAN_POINT ( 'NONE',  ( 3.874999999999999556, 3.137999999999999901, 1.320000000000000062 ) ) ;
#12459=DIRECTION ( 'NONE',  ( -1.000000000000000000, -0.000000000000000000, -0.000000000000000000 ) ) ;
#12463=DIRECTION ( 'NONE',  ( -1.000000000000000000, -0.000000000000000000, -0.000000000000000000 ) ) ;
#12467=VERTEX_POINT ( 'NONE', #1505 ) ;
#12472=FACE_OUTER_BOUND ( 'NONE', #10051, .T. ) ;
#12475=CARTESIAN_POINT ( 'NONE',  ( 3.426491571325181340, 0.9800000000000039790, 3.360000000000000320 ) ) ;
#12477=CARTESIAN_POINT ( 'NONE',  ( 3.464728362965293851, 1.935613442860778299, 0.7069208286046223533 ) ) ;
#12482=EDGE_CURVE ( 'NONE', #8673, #6629, #1946, .T. ) ;
#12483=DIRECTION ( 'NONE',  ( 0.000000000000000000, 1.000000000000000000, 0.000000000000000000 ) ) ;
#12484=VERTEX_POINT ( 'NONE', #6190 ) ;
#12485=EDGE_CURVE ( 'NONE', #12941, #4204, #10517, .T. ) ;
#12486=CARTESIAN_POINT ( 'NONE',  ( 2.980731298636167370, 2.750000000000000000, 0.3249191361593797844 ) ) ;
#12491=LINE ( 'NONE', #3325, #14849 ) ;
#12493=CARTESIAN_POINT ( 'NONE',  ( 4.152466769471746311, 1.791617367317514864, -0.6983344528546440166 ) ) ;
#12500=DIRECTION ( 'NONE',  ( 1.000000000000000000, 0.000000000000000000, 0.000000000000000000 ) ) ;
#12502=FACE_OUTER_BOUND ( 'NONE', #12979, .T. ) ;
#12504=VERTEX_POINT ( 'NONE', #2519 ) ;
#12505=CARTESIAN_POINT ( 'NONE',  ( 3.876560711617219379, 1.855806856933289950, 0.7500000000000001110 ) ) ;
#12507=DIRECTION ( 'NONE',  ( -1.000000000000000000, -0.000000000000000000, -0.000000000000000000 ) ) ;
#12508=EDGE_CURVE ( 'NONE', #13413, #10132, #9708, .T. ) ;
#12509=CIRCLE ( 'NONE', #13241, 0.4070000000000022489 ) ;
#12511=EDGE_CURVE ( 'NONE', #6601, #11615, #2523, .T. ) ;
#12512=CARTESIAN_POINT ( 'NONE',  ( 4.380579497543963363, 1.706994051371499177, 0.6171253673838056342 ) ) ;
#12513=CARTESIAN_POINT ( 'NONE',  ( 3.538134827540111438, 2.007021158475892797, -0.3702066563325129289 ) ) ;
#12516=DIRECTION ( 'NONE',  ( 0.7071067811865376918, 0.000000000000000000, -0.7071067811865573427 ) ) ;
#12519=ORIENTED_EDGE ( 'NONE', *, *, #11513, .F. ) ;
#12524=CARTESIAN_POINT ( 'NONE',  ( 6.176491571325181340, -1.679378605318047946, -1.679378605318053497 ) ) ;
#12530=ORIENTED_EDGE ( 'NONE', *, *, #8510, .F. ) ;
#12534=CARTESIAN_POINT ( 'NONE',  ( 3.392241908693700125, 0.9914823872279339145, 0.1312138895577312503 ) ) ;
#12535=CARTESIAN_POINT ( 'NONE',  ( 3.694525655941882203, 1.838693524946998004, -0.7841639951857555246 ) ) ;
#12541=CARTESIAN_POINT ( 'NONE',  ( 3.426491571325181340, -1.679378605318059048, -1.973878605318027724 ) ) ;
#12548=CARTESIAN_POINT ( 'NONE',  ( 6.826491571325181695, 1.679378605318035733, -1.679378605318065487 ) ) ;
#12549=DIRECTION ( 'NONE',  ( -1.000000000000000000, -0.000000000000000000, -0.000000000000000000 ) ) ;
#12553=DIRECTION ( 'NONE',  ( 0.000000000000000000, 0.000000000000000000, 1.000000000000000000 ) ) ;
#12555=PRODUCT_DEFINITION_FORMATION_WITH_SPECIFIED_SOURCE ( 'ANY', '', #12024, .NOT_KNOWN. ) ;
#12556=DIRECTION ( 'NONE',  ( -0.000000000000000000, 1.000000000000000000, 1.224646799147353207E-16 ) ) ;
#12562=CARTESIAN_POINT ( 'NONE',  ( 3.475703039784956871, 2.035382413711712246, 0.3018570397846632170 ) ) ;
#12568=ORIENTED_EDGE ( 'NONE', *, *, #11492, .F. ) ;
#12572=ORIENTED_EDGE ( 'NONE', *, *, #12128, .F. ) ;
#12576=DIRECTION ( 'NONE',  ( 0.000000000000000000, 1.000000000000000000, 0.000000000000000000 ) ) ;
#12584=ADVANCED_FACE ( 'NONE', ( #13577 ), #2887, .T. ) ;
#12588=CARTESIAN_POINT ( 'NONE',  ( 4.640170961443040198, 1.726011380923590188, 0.2628431377593381524 ) ) ;
#12592=ORIENTED_EDGE ( 'NONE', *, *, #13054, .F. ) ;
#12593=CYLINDRICAL_SURFACE ( 'NONE', #7255, 2.500000000000000000 ) ;
#12596=EDGE_CURVE ( 'NONE', #2681, #4332, #12189, .T. ) ;
#12597=CARTESIAN_POINT ( 'NONE',  ( 2.774999999999999911, -1.575000000000027489, -2.359999999999986109 ) ) ;
#12600=ORIENTED_EDGE ( 'NONE', *, *, #3850, .F. ) ;
#12604=CARTESIAN_POINT ( 'NONE',  ( 6.794491571325179891, -1.679378605318048390, 1.304378605318053497 ) ) ;
#12611=CARTESIAN_POINT ( 'NONE',  ( 3.743903362372427601, 0.8757526003188027541, -0.4827919802056128140 ) ) ;
#12614=CYLINDRICAL_SURFACE ( 'NONE', #10649, 0.2624999999999852451 ) ;
#12615=AXIS2_PLACEMENT_3D ( 'NONE', #12135, #12060, #10992 ) ;
#12617=ORIENTED_EDGE ( 'NONE', *, *, #5685, .T. ) ;
#12622=CARTESIAN_POINT ( 'NONE',  ( 2.774999999999999911, -2.360000000000016751, -0.9799999999999431388 ) ) ;
#12625=CARTESIAN_POINT ( 'NONE',  ( 3.874999999999999556, 2.750000000000000000, -1.542000000000000037 ) ) ;
#12631=DIRECTION ( 'NONE',  ( -0.7071067811865452413, 8.659560562354959975E-17, -0.7071067811865496822 ) ) ;
#12635=VERTEX_POINT ( 'NONE', #641 ) ;
#12638=ORIENTED_EDGE ( 'NONE', *, *, #156, .F. ) ;
#12642=EDGE_CURVE ( 'NONE', #638, #3395, #4110, .T. ) ;
#12643=LINE ( 'NONE', #4325, #7344 ) ;
#12644=CARTESIAN_POINT ( 'NONE',  ( 3.693889022407033096, 1.943894859932088881, 0.4666066016349538215 ) ) ;
#12648=CARTESIAN_POINT ( 'NONE',  ( 3.964297589650334075, 1.829743176842955510, -0.7450599964799213826 ) ) ;
#12650=VECTOR ( 'NONE', #14470, 39.37007874015748854 ) ;
#12651=VERTEX_POINT ( 'NONE', #14583 ) ;
#12654=ORIENTED_EDGE ( 'NONE', *, *, #10795, .F. ) ;
#12661=ORIENTED_EDGE ( 'NONE', *, *, #13918, .T. ) ;
#12666=VECTOR ( 'NONE', #5209, 39.37007874015748143 ) ;
#12670=AXIS2_PLACEMENT_3D ( 'NONE', #5945, #8471, #3729 ) ;
#12671=CARTESIAN_POINT ( 'NONE',  ( 4.625991625415837305, 1.810439985556918430, -0.03431761865087439717 ) ) ;
#12672=DIRECTION ( 'NONE',  ( 1.000000000000000000, 0.000000000000000000, 0.000000000000000000 ) ) ;
#12676=ORIENTED_EDGE ( 'NONE', *, *, #8963, .T. ) ;
#12677=ORIENTED_EDGE ( 'NONE', *, *, #12724, .T. ) ;
#12678=EDGE_CURVE ( 'NONE', #6416, #4777, #935, .T. ) ;
#12683=ORIENTED_EDGE ( 'NONE', *, *, #6344, .F. ) ;
#12688=CONICAL_SURFACE ( 'NONE', #6109, 1.000000000000000000, 0.7853981633974517207 ) ;
#12695=CARTESIAN_POINT ( 'NONE',  ( 3.712368062279605141, 0.8810275311047641722, 0.4730969127157453880 ) ) ;
#12696=CARTESIAN_POINT ( 'NONE',  ( 2.774999999999999911, -1.574999999999999956, 2.360000000000024745 ) ) ;
#12698=DIRECTION ( 'NONE',  ( 0.000000000000000000, 0.000000000000000000, -1.000000000000000000 ) ) ;
#12701=ORIENTED_EDGE ( 'NONE', *, *, #4214, .F. ) ;
#12707=CARTESIAN_POINT ( 'NONE',  ( 3.874999999999999556, 2.782000000000002693, 1.320000000000000062 ) ) ;
#12711=CARTESIAN_POINT ( 'NONE',  ( 3.875000000000000000, 1.112678268764263789, 0.5849999999999996314 ) ) ;
#12714=CIRCLE ( 'NONE', #2212, 0.2624999999999852451 ) ;
#12721=LINE ( 'NONE', #4552, #8512 ) ;
#12724=EDGE_CURVE ( 'NONE', #7890, #6474, #1187, .T. ) ;
#12731=CIRCLE ( 'NONE', #2492, 3.000000000000000444 ) ;
#12736=ORIENTED_EDGE ( 'NONE', *, *, #1157, .T. ) ;
#12741=CARTESIAN_POINT ( 'NONE',  ( 4.612938997950140951, 1.807748895277201839, 0.1434262448729105577 ) ) ;
#12752=DIRECTION ( 'NONE',  ( -1.000000000000000000, -0.000000000000000000, -0.000000000000000000 ) ) ;
#12754=CARTESIAN_POINT ( 'NONE',  ( 3.874999999999999556, 2.782000000000002693, 1.320000000000000062 ) ) ;
#12762=CARTESIAN_POINT ( 'NONE',  ( 3.426491571325181340, 0.9800000000000039790, 3.360000000000000320 ) ) ;
#12764=CARTESIAN_POINT ( 'NONE',  ( 4.586868767028525973, 1.718843021825377626, 0.3797541001213830536 ) ) ;
#12765=VERTEX_POINT ( 'NONE', #6710 ) ;
#12766=FACE_OUTER_BOUND ( 'NONE', #8898, .T. ) ;
#12768=EDGE_LOOP ( 'NONE', ( #1098, #12155, #4163, #63 ) ) ;
#12770=EDGE_CURVE ( 'NONE', #5690, #13527, #4097, .T. ) ;
#12772=ORIENTED_EDGE ( 'NONE', *, *, #1632, .T. ) ;
#12778=ORIENTED_EDGE ( 'NONE', *, *, #235, .F. ) ;
#12784=EDGE_LOOP ( 'NONE', ( #10696, #13681, #2998, #12592 ) ) ;
#12786=ORIENTED_EDGE ( 'NONE', *, *, #12216, .F. ) ;
#12791=EDGE_CURVE ( 'NONE', #694, #9791, #7178, .T. ) ;
#12792=DIRECTION ( 'NONE',  ( 0.000000000000000000, 0.000000000000000000, 1.000000000000000000 ) ) ;
#12793=DIRECTION ( 'NONE',  ( 0.000000000000000000, 0.000000000000000000, -1.000000000000000000 ) ) ;
#12797=DIRECTION ( 'NONE',  ( 0.000000000000000000, 0.000000000000000000, 1.000000000000000000 ) ) ;
#12799=CARTESIAN_POINT ( 'NONE',  ( 3.643830797058309479, 1.947962297878459204, -0.7137606667491679380 ) ) ;
#12802=EDGE_CURVE ( 'NONE', #14777, #8189, #11423, .T. ) ;
#12806=CARTESIAN_POINT ( 'NONE',  ( 3.874999999999999556, 3.137999999999999901, -1.098000000000000087 ) ) ;
#12807=CIRCLE ( 'NONE', #5494, 0.2625000000000000111 ) ;
#12808=DIRECTION ( 'NONE',  ( 0.000000000000000000, 0.000000000000000000, -1.000000000000000000 ) ) ;
#12812=CIRCLE ( 'NONE', #101, 0.4070000000000022489 ) ;
#12814=CARTESIAN_POINT ( 'NONE',  ( 3.426491571325181340, 3.360000000000000320, -0.9800000000000012035 ) ) ;
#12818=CARTESIAN_POINT ( 'NONE',  ( 4.593428806625106553, 1.719801573518523474, -0.3651073496023718445 ) ) ;
#12819=ORIENTED_EDGE ( 'NONE', *, *, #8091, .T. ) ;
#12820=VECTOR ( 'NONE', #6732, 39.37007874015748854 ) ;
#12824=EDGE_LOOP ( 'NONE', ( #8618, #2445 ) ) ;
#12825=ORIENTED_EDGE ( 'NONE', *, *, #12216, .T. ) ;
#12829=FACE_OUTER_BOUND ( 'NONE', #9862, .T. ) ;
#12832=FACE_OUTER_BOUND ( 'NONE', #12858, .T. ) ;
#12838=CARTESIAN_POINT ( 'NONE',  ( 6.826491571325181695, -1.679378605318048390, 2.086378605318056412 ) ) ;
#12839=CARTESIAN_POINT ( 'NONE',  ( 3.426491571325181340, -1.679378605318059048, -1.384878605318056399 ) ) ;
#12842=CARTESIAN_POINT ( 'NONE',  ( 4.646274775377375654, 1.726933778515093332, 0.2437811747078761637 ) ) ;
#12843=VERTEX_POINT ( 'NONE', #10766 ) ;
#12844=DIRECTION ( 'NONE',  ( 0.000000000000000000, 0.000000000000000000, -1.000000000000000000 ) ) ;
#12846=ORIENTED_EDGE ( 'NONE', *, *, #13370, .F. ) ;
#12847=ORIENTED_EDGE ( 'NONE', *, *, #12802, .T. ) ;
#12851=CARTESIAN_POINT ( 'NONE',  ( 3.944129661530210385, 0.000000000000000000, 0.000000000000000000 ) ) ;
#12858=EDGE_LOOP ( 'NONE', ( #10937, #7016, #10663, #5934 ) ) ;
#12860=CIRCLE ( 'NONE', #12615, 0.2944999999999976525 ) ;
#12862=CARTESIAN_POINT ( 'NONE',  ( 3.874999999999999556, 2.750000000000000000, -1.098000000000000087 ) ) ;
#12863=ORIENTED_EDGE ( 'NONE', *, *, #6175, .T. ) ;
#12868=ORIENTED_EDGE ( 'NONE', *, *, #14090, .T. ) ;
#12869=EDGE_CURVE ( 'NONE', #5558, #391, #6060, .T. ) ;
#12873=AXIS2_PLACEMENT_3D ( 'NONE', #3190, #12500, #14659 ) ;
#12875=DIRECTION ( 'NONE',  ( 0.000000000000000000, 0.000000000000000000, 1.000000000000000000 ) ) ;
#12878=ORIENTED_EDGE ( 'NONE', *, *, #10305, .F. ) ;
#12881=UNCERTAINTY_MEASURE_WITH_UNIT (LENGTH_MEASURE( 1.000000000000000082E-05 ), #2774, 'distance_accuracy_value', 'NONE');
#12883=ORIENTED_EDGE ( 'NONE', *, *, #3575, .F. ) ;
#12885=DIRECTION ( 'NONE',  ( -0.000000000000000000, 4.591341165821855765E-15, 1.000000000000000000 ) ) ;
#12898=CARTESIAN_POINT ( 'NONE',  ( 4.626594302918601187, 1.810567462571540664, -0.01639964552859272603 ) ) ;
#12899=ORIENTED_EDGE ( 'NONE', *, *, #11842, .F. ) ;
#12905=DIRECTION ( 'NONE',  ( -1.150251786806006500E-15, 0.000000000000000000, 1.000000000000000000 ) ) ;
#12909=DIRECTION ( 'NONE',  ( -1.000000000000000000, 0.000000000000000000, 0.000000000000000000 ) ) ;
#12916=FACE_OUTER_BOUND ( 'NONE', #170, .T. ) ;
#12917=CIRCLE ( 'NONE', #933, 0.3750000000000004996 ) ;
#12918=DIRECTION ( 'NONE',  ( -1.000000000000000000, -0.000000000000000000, -0.000000000000000000 ) ) ;
#12923=CARTESIAN_POINT ( 'NONE',  ( 3.667128492022511566, 0.8905039771886829048, 0.4550300979733812867 ) ) ;
#12924=CARTESIAN_POINT ( 'NONE',  ( 4.608301153546221052, 1.721636985526682206, -0.3364488613251436222 ) ) ;
#12925=EDGE_CURVE ( 'NONE', #11243, #14153, #3019, .T. ) ;
#12927=AXIS2_PLACEMENT_3D ( 'NONE', #6301, #2709, #4796 ) ;
#12928=DIRECTION ( 'NONE',  ( 0.000000000000000000, 0.000000000000000000, 1.000000000000000000 ) ) ;
#12929=CARTESIAN_POINT ( 'NONE',  ( 5.567023771132172172, 0.000000000000000000, 0.000000000000000000 ) ) ;
#12934=CARTESIAN_POINT ( 'NONE',  ( 6.787121492585022509, 3.673940397442060361E-16, -3.000000000000000444 ) ) ;
#12936=EDGE_LOOP ( 'NONE', ( #11022, #3108, #855, #11490 ) ) ;
#12937=CARTESIAN_POINT ( 'NONE',  ( 3.426491571325181340, 1.575000000000016387, 2.359999999999999432 ) ) ;
#12938=CARTESIAN_POINT ( 'NONE',  ( 3.875000000000000000, 3.085321731235734610, 0.000000000000000000 ) ) ;
#12939=DIRECTION ( 'NONE',  ( 0.000000000000000000, 0.000000000000000000, 1.000000000000000000 ) ) ;
#12941=VERTEX_POINT ( 'NONE', #12269 ) ;
#12952=DIRECTION ( 'NONE',  ( 0.000000000000000000, 0.000000000000000000, -1.000000000000000000 ) ) ;
#12956=EDGE_CURVE ( 'NONE', #11615, #8207, #10160, .T. ) ;
#12957=ADVANCED_FACE ( 'NONE', ( #11349 ), #5365, .F. ) ;
#12960=ORIENTED_EDGE ( 'NONE', *, *, #11734, .T. ) ;
#12964=EDGE_CURVE ( 'NONE', #6953, #10875, #11511, .T. ) ;
#12965=DIRECTION ( 'NONE',  ( 0.000000000000000000, 0.000000000000000000, -1.000000000000000000 ) ) ;
#12966=EDGE_LOOP ( 'NONE', ( #7360, #6030, #10868, #11786 ) ) ;
#12967=CIRCLE ( 'NONE', #9315, 0.5000000000000002220 ) ;
#12979=EDGE_LOOP ( 'NONE', ( #3608, #6234, #2487, #10281 ) ) ;
#12980=CARTESIAN_POINT ( 'NONE',  ( 2.774999999999999911, -1.679378605318041950, 1.679378605318059048 ) ) ;
#12986=CARTESIAN_POINT ( 'NONE',  ( 3.773638191489542493, 1.892500311876669894, 0.7431788962619894079 ) ) ;
#12987=VECTOR ( 'NONE', #3415, 39.37007874015748143 ) ;
#12989=EDGE_CURVE ( 'NONE', #4487, #9683, #12721, .T. ) ;
#12993=CARTESIAN_POINT ( 'NONE',  ( 3.992641157495913085, 1.749621749097510115, 0.7883586273357179319 ) ) ;
#12996=DIRECTION ( 'NONE',  ( 1.000000000000000000, 0.000000000000000000, 0.000000000000000000 ) ) ;
#12997=ORIENTED_EDGE ( 'NONE', *, *, #8583, .T. ) ;
#12999=CARTESIAN_POINT ( 'NONE',  ( 6.215861650065340527, 3.673940397442060361E-16, -3.000000000000000444 ) ) ;
#13005=EDGE_CURVE ( 'NONE', #11969, #355, #12491, .T. ) ;
#13011=DIRECTION ( 'NONE',  ( 0.000000000000000000, 0.000000000000000000, -1.000000000000000000 ) ) ;
#13013=DIRECTION ( 'NONE',  ( -1.000000000000000000, -0.000000000000000000, -0.000000000000000000 ) ) ;
#13014=ORIENTED_EDGE ( 'NONE', *, *, #11576, .T. ) ;
#13018=CARTESIAN_POINT ( 'NONE',  ( 3.944129661530210385, 0.000000000000000000, 0.000000000000000000 ) ) ;
#13022=CARTESIAN_POINT ( 'NONE',  ( 3.426491571325181340, 0.000000000000000000, 0.000000000000000000 ) ) ;
#13025=ORIENTED_EDGE ( 'NONE', *, *, #11233, .T. ) ;
#13026=ORIENTED_EDGE ( 'NONE', *, *, #12770, .F. ) ;
#13028=CARTESIAN_POINT ( 'NONE',  ( 3.426491571325181340, 2.056041051583894497, 0.5999481385562638325 ) ) ;
#13033=CARTESIAN_POINT ( 'NONE',  ( 3.876560711617219379, 2.750000000000000000, 0.000000000000000000 ) ) ;
#13036=CONICAL_SURFACE ( 'NONE', #11585, 0.2624999999999852451, 0.7853981633974428389 ) ;
#13042=AXIS2_PLACEMENT_3D ( 'NONE', #7323, #11975, #314 ) ;
#13045=EDGE_LOOP ( 'NONE', ( #4459, #5265, #14423, #12683 ) ) ;
#13047=DIRECTION ( 'NONE',  ( 0.000000000000000000, 0.000000000000000000, 1.000000000000000000 ) ) ;
#13049=PLANE ( 'NONE',  #12095 ) ;
#13052=DIRECTION ( 'NONE',  ( 0.000000000000000000, 0.000000000000000000, 1.000000000000000000 ) ) ;
#13053=EDGE_CURVE ( 'NONE', #4833, #3395, #7970, .T. ) ;
#13054=EDGE_CURVE ( 'NONE', #2564, #5506, #2173, .T. ) ;
#13055=DIRECTION ( 'NONE',  ( -1.000000000000000000, -0.000000000000000000, -0.000000000000000000 ) ) ;
#13058=CARTESIAN_POINT ( 'NONE',  ( 6.826491571325181695, 0.000000000000000000, 0.000000000000000000 ) ) ;
#13063=DIRECTION ( 'NONE',  ( 0.7071067811865450192, 8.659560562354962440E-17, 0.7071067811865499042 ) ) ;
#13064=FACE_BOUND ( 'NONE', #1016, .T. ) ;
#13076=DIRECTION ( 'NONE',  ( -1.000000000000000000, 0.000000000000000000, 0.000000000000000000 ) ) ;
#13077=AXIS2_PLACEMENT_3D ( 'NONE', #2910, #12233, #3359 ) ;
#13078=TOROIDAL_SURFACE ( 'NONE', #3076, 0.5849999999999996314, 0.1000000000000000056 ) ;
#13079=DIRECTION ( 'NONE',  ( -1.000000000000000000, -0.000000000000000000, -0.000000000000000000 ) ) ;
#13081=ADVANCED_FACE ( 'NONE', ( #9458 ), #7049, .F. ) ;
#13086=AXIS2_PLACEMENT_3D ( 'NONE', #6126, #14286, #5967 ) ;
#13089=ORIENTED_EDGE ( 'NONE', *, *, #6175, .F. ) ;
#13091=CARTESIAN_POINT ( 'NONE',  ( 6.208491571325183145, -1.679378605318048390, 1.679378605318054163 ) ) ;
#13093=EDGE_CURVE ( 'NONE', #7368, #14441, #11681, .T. ) ;
#13096=AXIS2_PLACEMENT_3D ( 'NONE', #8409, #13891, #12905 ) ;
#13100=DIRECTION ( 'NONE',  ( 0.000000000000000000, 0.000000000000000000, -1.000000000000000000 ) ) ;
#13104=ORIENTED_EDGE ( 'NONE', *, *, #9048, .F. ) ;
#13105=VERTEX_POINT ( 'NONE', #303 ) ;
#13107=CARTESIAN_POINT ( 'NONE',  ( 3.426491571325181340, 0.6999999999999599876, -2.400000000000011458 ) ) ;
#13110=DIRECTION ( 'NONE',  ( 0.000000000000000000, 1.000000000000000000, 0.000000000000000000 ) ) ;
#13112=CARTESIAN_POINT ( 'NONE',  ( 3.817400053824495654, 1.897687926027022520, -0.4968051402951919604 ) ) ;
#13117=EDGE_LOOP ( 'NONE', ( #12249, #13887, #13725, #7116 ) ) ;
#13118=CARTESIAN_POINT ( 'NONE',  ( 3.874999999999999556, 2.782000000000000917, -1.509999999999999787 ) ) ;
#13119=VERTEX_POINT ( 'NONE', #11746 ) ;
#13124=DIRECTION ( 'NONE',  ( -1.000000000000000000, -0.000000000000000000, -0.000000000000000000 ) ) ;
#13130=DIRECTION ( 'NONE',  ( 0.000000000000000000, 0.000000000000000000, -1.000000000000000000 ) ) ;
#13137=CARTESIAN_POINT ( 'NONE',  ( 3.426491571325181340, 1.575000000000000178, -2.360000000000018971 ) ) ;
#13139=CARTESIAN_POINT ( 'NONE',  ( 6.794491571325179891, -1.679378605318047946, -1.304378605318053053 ) ) ;
#13142=ADVANCED_FACE ( 'NONE', ( #239 ), #14350, .T. ) ;
#13145=ORIENTED_EDGE ( 'NONE', *, *, #13461, .T. ) ;
#13147=ORIENTED_EDGE ( 'NONE', *, *, #7639, .F. ) ;
#13148=VECTOR ( 'NONE', #4443, 39.37007874015748854 ) ;
#13150=DIRECTION ( 'NONE',  ( -1.000000000000000000, -0.000000000000000000, -0.000000000000000000 ) ) ;
#13151=DIRECTION ( 'NONE',  ( 0.000000000000000000, 0.000000000000000000, -1.000000000000000000 ) ) ;
#13158=ORIENTED_EDGE ( 'NONE', *, *, #10381, .F. ) ;
#13163=VERTEX_POINT ( 'NONE', #4782 ) ;
#13172=DIRECTION ( 'NONE',  ( 0.000000000000000000, 0.000000000000000000, -1.000000000000000000 ) ) ;
#13175=CARTESIAN_POINT ( 'NONE',  ( 3.426491571325181340, 0.000000000000000000, 0.000000000000000000 ) ) ;
#13179=ORIENTED_EDGE ( 'NONE', *, *, #2904, .F. ) ;
#13181=EDGE_LOOP ( 'NONE', ( #1142, #6783, #1561, #9646 ) ) ;
#13183=DIRECTION ( 'NONE',  ( -1.000000000000000000, -0.000000000000000000, -0.000000000000000000 ) ) ;
#13185=LINE ( 'NONE', #2723, #6085 ) ;
#13186=CARTESIAN_POINT ( 'NONE',  ( 3.426491571325181340, 1.958272580636415405, -0.6732367908064789130 ) ) ;
#13189=ADVANCED_FACE ( 'NONE', ( #3932 ), #11184, .F. ) ;
#13190=EDGE_CURVE ( 'NONE', #6615, #6953, #12398, .T. ) ;
#13191=CARTESIAN_POINT ( 'NONE',  ( 4.456236641444369262, 1.708450350955834418, -0.5507572246836857088 ) ) ;
#13192=EDGE_LOOP ( 'NONE', ( #8267, #4129, #9383, #12349, #351, #14806 ) ) ;
#13199=CARTESIAN_POINT ( 'NONE',  ( 4.358578070590652942, 0.9918745563571595980, -0.1313582112852187400 ) ) ;
#13200=FACE_OUTER_BOUND ( 'NONE', #5325, .T. ) ;
#13205=CARTESIAN_POINT ( 'NONE',  ( 6.826491571325181695, -1.679378605318047946, -1.679378605318053497 ) ) ;
#13209=CARTESIAN_POINT ( 'NONE',  ( 3.527413420661385413, 1.933330931508713268, 0.6651649055560091561 ) ) ;
#13210=CARTESIAN_POINT ( 'NONE',  ( 2.774999999999999911, 0.000000000000000000, 0.000000000000000000 ) ) ;
#13219=AXIS2_PLACEMENT_3D ( 'NONE', #8758, #2792, #1405 ) ;
#13220=DIRECTION ( 'NONE',  ( 0.000000000000000000, 0.000000000000000000, 1.000000000000000000 ) ) ;
#13234=LENGTH_MEASURE_WITH_UNIT ( LENGTH_MEASURE( 0.02539999999999999897 ), #3489 );
#13236=DIRECTION ( 'NONE',  ( 0.000000000000000000, 0.000000000000000000, -1.000000000000000000 ) ) ;
#13241=AXIS2_PLACEMENT_3D ( 'NONE', #8280, #4906, #2524 ) ;
#13245=EDGE_CURVE ( 'NONE', #638, #14935, #13852, .T. ) ;
#13251=CIRCLE ( 'NONE', #9375, 0.4070000000000022489 ) ;
#13252=LINE ( 'NONE', #470, #8986 ) ;
#13255=CARTESIAN_POINT ( 'NONE',  ( 6.826491571325181695, -1.679378605318048390, 1.679378605318054163 ) ) ;
#13256=CARTESIAN_POINT ( 'NONE',  ( 4.559481147695757741, 1.797976069233882646, -0.3110169328516964038 ) ) ;
#13261=EDGE_LOOP ( 'NONE', ( #1890, #14829, #882, #14424 ) ) ;
#13266=FACE_OUTER_BOUND ( 'NONE', #7687, .T. ) ;
#13267=EDGE_CURVE ( 'NONE', #1703, #12765, #7980, .T. ) ;
#13268=PRODUCT_CONTEXT ( 'NONE', #4706, 'mechanical' ) ;
#13270=ORIENTED_EDGE ( 'NONE', *, *, #7664, .F. ) ;
#13273=CARTESIAN_POINT ( 'NONE',  ( 3.426491571325181340, 0.7000000000000026201, 2.400000000000000355 ) ) ;
#13277=FACE_OUTER_BOUND ( 'NONE', #14130, .T. ) ;
#13278=DIRECTION ( 'NONE',  ( 0.000000000000000000, -1.000000000000000000, 0.000000000000000000 ) ) ;
#13280=VECTOR ( 'NONE', #11460, 39.37007874015748143 ) ;
#13282=DIRECTION ( 'NONE',  ( -1.000000000000000000, -0.000000000000000000, -0.000000000000000000 ) ) ;
#13285=DIRECTION ( 'NONE',  ( 1.000000000000000000, 0.000000000000000000, 0.000000000000000000 ) ) ;
#13288=CARTESIAN_POINT ( 'NONE',  ( 6.208491571325183145, 1.679378605318059492, 1.679378605318041506 ) ) ;
#13289=ADVANCED_FACE ( 'NONE', ( #12472 ), #2148, .T. ) ;
#13290=DIRECTION ( 'NONE',  ( -1.000000000000000000, -0.000000000000000000, -0.000000000000000000 ) ) ;
#13292=CARTESIAN_POINT ( 'NONE',  ( 6.826491571325181695, -1.679378605318047946, -2.086378605318055968 ) ) ;
#13294=CIRCLE ( 'NONE', #10629, 0.3750000000000007772 ) ;
#13299=CARTESIAN_POINT ( 'NONE',  ( 6.794491571325179891, 1.679378605318035733, -1.679378605318065487 ) ) ;
#13301=DIRECTION ( 'NONE',  ( 0.000000000000000000, 0.000000000000000000, -1.000000000000000000 ) ) ;
#13303=CARTESIAN_POINT ( 'NONE',  ( 6.176491571325181340, 1.679378605318035733, -1.679378605318065487 ) ) ;
#13304=VERTEX_POINT ( 'NONE', #7894 ) ;
#13312=AXIS2_PLACEMENT_3D ( 'NONE', #12000, #2816, #345 ) ;
#13313=AXIS2_PLACEMENT_3D ( 'NONE', #14789, #6686, #14865 ) ;
#13314=LINE ( 'NONE', #2635, #15025 ) ;
#13316=VERTEX_POINT ( 'NONE', #10124 ) ;
#13319=ORIENTED_EDGE ( 'NONE', *, *, #5525, .F. ) ;
#13321=VECTOR ( 'NONE', #6598, 39.37007874015748143 ) ;
#13330=ADVANCED_FACE ( 'NONE', ( #8979 ), #8896, .F. ) ;
#13340=CARTESIAN_POINT ( 'NONE',  ( 4.217173919807448712, 0.9311135807922138463, 0.3649311961389214987 ) ) ;
#13342=DIRECTION ( 'NONE',  ( 0.000000000000000000, 0.000000000000000000, 1.000000000000000000 ) ) ;
#13344=LINE ( 'NONE', #412, #14841 ) ;
#13345=DIRECTION ( 'NONE',  ( 0.000000000000000000, 0.000000000000000000, -1.000000000000000000 ) ) ;
#13346=DIRECTION ( 'NONE',  ( -0.000000000000000000, 1.000000000000000000, -0.000000000000000000 ) ) ;
#13352=CARTESIAN_POINT ( 'NONE',  ( 3.341229073668624316, 1.997163125837124076, 0.6280186637500814184 ) ) ;
#13353=LINE ( 'NONE', #6274, #8902 ) ;
#13355=AXIS2_PLACEMENT_3D ( 'NONE', #11065, #12285, #6484 ) ;
#13360=ORIENTED_EDGE ( 'NONE', *, *, #4647, .T. ) ;
#13361=VECTOR ( 'NONE', #13150, 39.37007874015748143 ) ;
#13370=EDGE_CURVE ( 'NONE', #10812, #2681, #8064, .T. ) ;
#13381=CARTESIAN_POINT ( 'NONE',  ( 5.546318247523970513, 2.103182086337546510E-16, -1.502725933896874810 ) ) ;
#13392=VECTOR ( 'NONE', #2393, 39.37007874015748143 ) ;
#13394=AXIS2_PLACEMENT_3D ( 'NONE', #4191, #560, #9846 ) ;
#13395=VECTOR ( 'NONE', #11831, 39.37007874015748143 ) ;
#13401=ORIENTED_EDGE ( 'NONE', *, *, #2303, .F. ) ;
#13403=ORIENTED_EDGE ( 'NONE', *, *, #13901, .T. ) ;
#13407=CARTESIAN_POINT ( 'NONE',  ( 2.774999999999999911, 1.272861240058668140E-16, -1.039370078740158965 ) ) ;
#13408=LINE ( 'NONE', #6239, #14211 ) ;
#13409=AXIS2_PLACEMENT_3D ( 'NONE', #1707, #11046, #5238 ) ;
#13410=CARTESIAN_POINT ( 'NONE',  ( 4.386459485047407902, 1.780485827611695493, 0.5505562060287755299 ) ) ;
#13411=EDGE_CURVE ( 'NONE', #5690, #1151, #833, .T. ) ;
#13413=VERTEX_POINT ( 'NONE', #5531 ) ;
#13418=EDGE_CURVE ( 'NONE', #7097, #3105, #9894, .T. ) ;
#13419=ORIENTED_EDGE ( 'NONE', *, *, #13093, .T. ) ;
#13422=CARTESIAN_POINT ( 'NONE',  ( 4.322772591681486531, 0.9749115779099136736, 0.2230826791404775244 ) ) ;
#13424=FACE_OUTER_BOUND ( 'NONE', #5466, .T. ) ;
#13427=PLANE ( 'NONE',  #7314 ) ;
#13431=DIRECTION ( 'NONE',  ( 0.000000000000000000, 0.000000000000000000, 1.000000000000000000 ) ) ;
#13432=CARTESIAN_POINT ( 'NONE',  ( 3.426491571325181340, -3.360000000000000320, 0.9799999999999999822 ) ) ;
#13433=CARTESIAN_POINT ( 'NONE',  ( 4.045956536581743812, 1.738919081015790846, 0.7773475529263453865 ) ) ;
#13434=DIRECTION ( 'NONE',  ( -1.000000000000000000, -0.000000000000000000, -0.000000000000000000 ) ) ;
#13436=ORIENTED_EDGE ( 'NONE', *, *, #14550, .F. ) ;
#13437=CARTESIAN_POINT ( 'NONE',  ( 3.874999999999999556, 3.137999999999999901, -1.130000000000000560 ) ) ;
#13438=ORIENTED_EDGE ( 'NONE', *, *, #1769, .T. ) ;
#13441=PLANE ( 'NONE',  #9241 ) ;
#13444=DIRECTION ( 'NONE',  ( 0.000000000000000000, 0.000000000000000000, -1.000000000000000000 ) ) ;
#13446=ADVANCED_FACE ( 'NONE', ( #7294 ), #9358, .F. ) ;
#13448=CIRCLE ( 'NONE', #5651, 0.4070000000000022489 ) ;
#13450=ORIENTED_EDGE ( 'NONE', *, *, #501, .T. ) ;
#13452=CARTESIAN_POINT ( 'NONE',  ( 3.426491571325181340, 1.987932976489903414, 0.2209981660730357955 ) ) ;
#13459=DIRECTION ( 'NONE',  ( 0.000000000000000000, 0.000000000000000000, 1.000000000000000000 ) ) ;
#13461=EDGE_CURVE ( 'NONE', #15105, #4070, #10502, .T. ) ;
#13464=CARTESIAN_POINT ( 'NONE',  ( 3.874999999999999556, 3.137999999999999901, 1.320000000000000062 ) ) ;
#13470=DIRECTION ( 'NONE',  ( 0.000000000000000000, 0.000000000000000000, 1.000000000000000000 ) ) ;
#13472=ORIENTED_EDGE ( 'NONE', *, *, #3537, .F. ) ;
#13476=EDGE_CURVE ( 'NONE', #13413, #5032, #9512, .T. ) ;
#13483=ORIENTED_EDGE ( 'NONE', *, *, #4824, .T. ) ;
#13484=ORIENTED_EDGE ( 'NONE', *, *, #1277, .T. ) ;
#13488=EDGE_CURVE ( 'NONE', #14644, #4727, #5499, .T. ) ;
#13490=FACE_OUTER_BOUND ( 'NONE', #8130, .T. ) ;
#13492=DIRECTION ( 'NONE',  ( 0.000000000000000000, 0.000000000000000000, 1.000000000000000000 ) ) ;
#13493=ORIENTED_EDGE ( 'NONE', *, *, #11996, .T. ) ;
#13495=CARTESIAN_POINT ( 'NONE',  ( 6.215861650065340527, 0.000000000000000000, 3.000000000000000444 ) ) ;
#13498=AXIS2_PLACEMENT_3D ( 'NONE', #3472, #6000, #8231 ) ;
#13501=CARTESIAN_POINT ( 'NONE',  ( 4.014119211518829111, 1.817012082641814574, 0.7380940613581021825 ) ) ;
#13502=DIRECTION ( 'NONE',  ( -1.000000000000000000, -0.000000000000000000, -0.000000000000000000 ) ) ;
#13505=VECTOR ( 'NONE', #4455, 39.37007874015748143 ) ;
#13515=EDGE_CURVE ( 'NONE', #4759, #6131, #12812, .T. ) ;
#13516=DIRECTION ( 'NONE',  ( 1.000000000000000000, 0.000000000000000000, 0.000000000000000000 ) ) ;
#13518=EDGE_CURVE ( 'NONE', #2188, #7512, #334, .T. ) ;
#13521=LINE ( 'NONE', #3062, #11945 ) ;
#13524=CARTESIAN_POINT ( 'NONE',  ( 3.426491571325181340, -1.679378605318041950, 1.416878605318058870 ) ) ;
#13525=CARTESIAN_POINT ( 'NONE',  ( 3.374989204712153246, 1.000005397643052074, 0.01633309950357363094 ) ) ;
#13526=CARTESIAN_POINT ( 'NONE',  ( 4.040517861103548825, 1.740199758096359961, -0.7780251460681402165 ) ) ;
#13527=VERTEX_POINT ( 'NONE', #1148 ) ;
#13528=CARTESIAN_POINT ( 'NONE',  ( 3.891802077818124150, 0.8660254037844385966, -0.5000000000000002220 ) ) ;
#13529=DIRECTION ( 'NONE',  ( 1.000000000000000000, 0.000000000000000000, 0.000000000000000000 ) ) ;
#13530=ORIENTED_EDGE ( 'NONE', *, *, #6699, .F. ) ;
#13531=AXIS2_PLACEMENT_3D ( 'NONE', #4052, #1670, #6362 ) ;
#13536=CARTESIAN_POINT ( 'NONE',  ( 3.599064736766494743, 1.969292692958134472, -0.6979109735870647757 ) ) ;
#13538=FACE_OUTER_BOUND ( 'NONE', #7290, .T. ) ;
#13539=CARTESIAN_POINT ( 'NONE',  ( 3.426491571325181340, 1.575000000000016609, 1.575000000000000178 ) ) ;
#13541=EDGE_CURVE ( 'NONE', #11167, #3810, #4689, .T. ) ;
#13542=ORIENTED_EDGE ( 'NONE', *, *, #1029, .T. ) ;
#13546=AXIS2_PLACEMENT_3D ( 'NONE', #12938, #4612, #13923 ) ;
#13548=FACE_OUTER_BOUND ( 'NONE', #12966, .T. ) ;
#13551=LINE ( 'NONE', #13853, #6760 ) ;
#13552=EDGE_LOOP ( 'NONE', ( #279, #4709, #4085, #4171 ) ) ;
#13553=DIRECTION ( 'NONE',  ( 0.000000000000000000, -9.641816448226552334E-15, -1.000000000000000000 ) ) ;
#13557=CONICAL_SURFACE ( 'NONE', #2338, 0.4070000000000022489, 0.7853981633974547183 ) ;
#13559=CARTESIAN_POINT ( 'NONE',  ( 4.548733854531023191, 1.796245319939208107, -0.3336101870576589357 ) ) ;
#13560=ORIENTED_EDGE ( 'NONE', *, *, #1412, .F. ) ;
#13563=EDGE_LOOP ( 'NONE', ( #2154, #8792 ) ) ;
#13565=ORIENTED_EDGE ( 'NONE', *, *, #3436, .F. ) ;
#13569=DIRECTION ( 'NONE',  ( 1.000000000000000000, -0.000000000000000000, -0.000000000000000000 ) ) ;
#13577=FACE_OUTER_BOUND ( 'NONE', #3467, .T. ) ;
#13579=DIRECTION ( 'NONE',  ( 0.000000000000000000, 0.000000000000000000, 1.000000000000000000 ) ) ;
#13580=DIRECTION ( 'NONE',  ( 0.3420201433256623846, 0.000000000000000000, -0.9396926207859106484 ) ) ;
#13582=CARTESIAN_POINT ( 'NONE',  ( 4.454384321854326423, 1.730788856496732420, 0.4784941975638398737 ) ) ;
#13583=CARTESIAN_POINT ( 'NONE',  ( 3.621412531120375089, 1.971946916245812975, -0.4310735882759350046 ) ) ;
#13585=AXIS2_PLACEMENT_3D ( 'NONE', #6334, #9838, #14491 ) ;
#13589=ORIENTED_EDGE ( 'NONE', *, *, #6344, .T. ) ;
#13593=AXIS2_PLACEMENT_3D ( 'NONE', #10225, #9007, #9079 ) ;
#13604=CARTESIAN_POINT ( 'NONE',  ( 3.569652111961249652, 0.9182054424553791616, -0.3962596773958052543 ) ) ;
#13609=CARTESIAN_POINT ( 'NONE',  ( 4.280825855804681446, 0.9563621563813751170, -0.2925165865892054851 ) ) ;
#13616=VECTOR ( 'NONE', #1164, 39.37007874015748143 ) ;
#13618=CARTESIAN_POINT ( 'NONE',  ( 3.835129291132573837, 1.869265298754045679, -0.7500000000000001110 ) ) ;
#13620=CARTESIAN_POINT ( 'NONE',  ( 6.096491571325181269, 0.000000000000000000, 0.000000000000000000 ) ) ;
#13623=VERTEX_POINT ( 'NONE', #12308 ) ;
#13626=CARTESIAN_POINT ( 'NONE',  ( 3.874999999999999556, 2.750000000000000000, 1.097999999999997867 ) ) ;
#13628=DIRECTION ( 'NONE',  ( 0.7071067811865512365, 0.000000000000000000, -0.7071067811865436870 ) ) ;
#13632=ORIENTED_EDGE ( 'NONE', *, *, #11510, .F. ) ;
#13633=CARTESIAN_POINT ( 'NONE',  ( 3.426491571325181340, 2.359999999999994547, -1.575000000000016831 ) ) ;
#13643=CARTESIAN_POINT ( 'NONE',  ( 3.923683937046483550, 1.841036866441990050, -0.7489011557682658804 ) ) ;
#13644=ORIENTED_EDGE ( 'NONE', *, *, #499, .T. ) ;
#13646=VECTOR ( 'NONE', #5561, 39.37007874015748143 ) ;
#13651=ORIENTED_EDGE ( 'NONE', *, *, #2064, .F. ) ;
#13653=LINE ( 'NONE', #3028, #2378 ) ;
#13658=DIRECTION ( 'NONE',  ( -1.000000000000000000, -0.000000000000000000, -0.000000000000000000 ) ) ;
#13664=CARTESIAN_POINT ( 'NONE',  ( 4.454242182452238907, 1.708366068422199957, 0.5527474542283296044 ) ) ;
#13665=CARTESIAN_POINT ( 'NONE',  ( 6.826491571325181695, 0.000000000000000000, 0.000000000000000000 ) ) ;
#13669=DIRECTION ( 'NONE',  ( 1.000000000000000000, 0.000000000000000000, 0.000000000000000000 ) ) ;
#13672=CIRCLE ( 'NONE', #14414, 0.2624999999999997335 ) ;
#13678=FACE_OUTER_BOUND ( 'NONE', #10167, .T. ) ;
#13681=ORIENTED_EDGE ( 'NONE', *, *, #6771, .T. ) ;
#13687=VERTEX_POINT ( 'NONE', #5512 ) ;
#13690=ORIENTED_EDGE ( 'NONE', *, *, #12016, .F. ) ;
#13692=ADVANCED_FACE ( 'NONE', ( #11475 ), #11165, .F. ) ;
#13695=DIRECTION ( 'NONE',  ( -0.000000000000000000, -1.000000000000000000, -0.000000000000000000 ) ) ;
#13703=ORIENTED_EDGE ( 'NONE', *, *, #13245, .F. ) ;
#13709=EDGE_CURVE ( 'NONE', #8247, #628, #12086, .T. ) ;
#13714=ORIENTED_EDGE ( 'NONE', *, *, #700, .F. ) ;
#13715=ADVANCED_FACE ( 'NONE', ( #13490 ), #11871, .F. ) ;
#13716=CARTESIAN_POINT ( 'NONE',  ( 3.669841109856190275, 1.848025286936557654, -0.7790857044152560418 ) ) ;
#13721=FACE_OUTER_BOUND ( 'NONE', #1291, .T. ) ;
#13725=ORIENTED_EDGE ( 'NONE', *, *, #1820, .T. ) ;
#13727=CONICAL_SURFACE ( 'NONE', #6173, 0.2945000000000009277, 0.7853981633974503884 ) ;
#13732=CARTESIAN_POINT ( 'NONE',  ( 4.266066090114608578, 1.710594575876754231, 0.6935905660327770228 ) ) ;
#13733=CARTESIAN_POINT ( 'NONE',  ( 3.662127683554703417, 1.955924818698876244, -0.4525689758964896448 ) ) ;
#13734=ORIENTED_EDGE ( 'NONE', *, *, #13418, .T. ) ;
#13735=ADVANCED_FACE ( 'NONE', ( #13266 ), #1716, .F. ) ;
#13739=VERTEX_POINT ( 'NONE', #484 ) ;
#13744=DIRECTION ( 'NONE',  ( -1.000000000000000000, -0.000000000000000000, -0.000000000000000000 ) ) ;
#13749=ORIENTED_EDGE ( 'NONE', *, *, #3931, .T. ) ;
#13754=EDGE_CURVE ( 'NONE', #12377, #3810, #645, .T. ) ;
#13755=DIRECTION ( 'NONE',  ( 0.000000000000000000, 0.000000000000000000, -1.000000000000000000 ) ) ;
#13756=CARTESIAN_POINT ( 'NONE',  ( 6.176491571325181340, 1.679378605318059492, 1.272378605318039257 ) ) ;
#13762=DIRECTION ( 'NONE',  ( 0.000000000000000000, 0.000000000000000000, -1.000000000000000000 ) ) ;
#13766=DIRECTION ( 'NONE',  ( -1.000000000000000000, -0.000000000000000000, -0.000000000000000000 ) ) ;
#13773=CARTESIAN_POINT ( 'NONE',  ( 4.769268701363833074, 3.137999999999999901, -0.3249191361593796734 ) ) ;
#13787=EDGE_CURVE ( 'NONE', #10523, #10316, #1753, .T. ) ;
#13789=CARTESIAN_POINT ( 'NONE',  ( 3.880536119609262258, 1.799609107823162413, -0.7503340787926818800 ) ) ;
#13794=ORIENTED_EDGE ( 'NONE', *, *, #11377, .F. ) ;
#13796=AXIS2_PLACEMENT_3D ( 'NONE', #4212, #13516, #11082 ) ;
#13797=VECTOR ( 'NONE', #4153, 39.37007874015748854 ) ;
#13803=CARTESIAN_POINT ( 'NONE',  ( 3.126948208750839342, 2.499883650940541102, -0.02820439714893648725 ) ) ;
#13805=CONICAL_SURFACE ( 'NONE', #11876, 0.3750000000000007772, 0.7853981633974557175 ) ;
#13806=CARTESIAN_POINT ( 'NONE',  ( 3.875000000000000000, 0.7099999999999984102, 0.000000000000000000 ) ) ;
#13808=CONICAL_SURFACE ( 'NONE', #11641, 3.000000000000000444, 0.7853981633974415066 ) ;
#13810=CARTESIAN_POINT ( 'NONE',  ( 4.525792272712025444, 1.792887553598168759, -0.3759268146155863577 ) ) ;
#13812=ORIENTED_EDGE ( 'NONE', *, *, #8764, .F. ) ;
#13818=VECTOR ( 'NONE', #5953, 39.37007874015748854 ) ;
#13826=EDGE_CURVE ( 'NONE', #13163, #4070, #1984, .T. ) ;
#13832=DIRECTION ( 'NONE',  ( 0.000000000000000000, 0.000000000000000000, 1.000000000000000000 ) ) ;
#13834=CARTESIAN_POINT ( 'NONE',  ( 3.874999999999999556, 3.105999999999998984, -1.130000000000000560 ) ) ;
#13838=ORIENTED_EDGE ( 'NONE', *, *, #235, .T. ) ;
#13839=AXIS2_PLACEMENT_3D ( 'NONE', #9006, #6784, #14887 ) ;
#13841=EDGE_CURVE ( 'NONE', #6416, #3063, #7708, .T. ) ;
#13848=DIRECTION ( 'NONE',  ( 0.000000000000000000, 0.000000000000000000, 1.000000000000000000 ) ) ;
#13851=ORIENTED_EDGE ( 'NONE', *, *, #11510, .T. ) ;
#13852=CIRCLE ( 'NONE', #11432, 2.000179419058113695 ) ;
#13853=CARTESIAN_POINT ( 'NONE',  ( 4.315797241329101475, 3.137999999999999901, -1.570821732971949825 ) ) ;
#13854=VERTEX_POINT ( 'NONE', #2054 ) ;
#13855=CARTESIAN_POINT ( 'NONE',  ( 6.096491571325181269, 1.934941942652818220E-16, 1.580000000000000071 ) ) ;
#13857=DIRECTION ( 'NONE',  ( -1.000000000000000000, -0.000000000000000000, -0.000000000000000000 ) ) ;
#13863=CARTESIAN_POINT ( 'NONE',  ( 3.781227704530009337, 1.808100070518111835, -0.7963533161500825353 ) ) ;
#13867=CARTESIAN_POINT ( 'NONE',  ( 3.426491571325181340, 1.958274996229347087, 0.6732298969886908457 ) ) ;
#13871=CARTESIAN_POINT ( 'NONE',  ( 2.774999999999999911, -1.679378605318041950, 1.973878605318057700 ) ) ;
#13872=CONICAL_SURFACE ( 'NONE', #5108, 0.2219999999999999751, 0.7853981633974349563 ) ;
#13875=ORIENTED_EDGE ( 'NONE', *, *, #9302, .T. ) ;
#13876=DIRECTION ( 'NONE',  ( 1.000000000000000000, 0.000000000000000000, 0.000000000000000000 ) ) ;
#13877=EDGE_CURVE ( 'NONE', #10976, #9323, #14532, .T. ) ;
#13879=EDGE_CURVE ( 'NONE', #3188, #5697, #1100, .T. ) ;
#13880=DIRECTION ( 'NONE',  ( 0.000000000000000000, 0.000000000000000000, 1.000000000000000000 ) ) ;
#13881=AXIS2_PLACEMENT_3D ( 'NONE', #10874, #2541, #7295 ) ;
#13882=CIRCLE ( 'NONE', #7541, 0.4070000000000022489 ) ;
#13887=ORIENTED_EDGE ( 'NONE', *, *, #15086, .T. ) ;
#13889=EDGE_LOOP ( 'NONE', ( #6497, #1402, #10434, #228 ) ) ;
#13891=DIRECTION ( 'NONE',  ( -0.000000000000000000, -1.000000000000000000, 0.000000000000000000 ) ) ;
#13894=B_SPLINE_CURVE_WITH_KNOTS ( 'NONE', 3,
 ( #12066, #1574, #2960, #12284, #12213, #1796, #5564, #15042, #10378, #11367, #2024, #4569, #4646, #6708, #3337, #14892, #13803, #2189, #3195, #4341, #9236, #9084, #11601, #9317, #7856, #6790, #1105, #870, #3420, #5791, #8010, #7932 ),
 .UNSPECIFIED., .F., .F.,
 ( 4, 2, 2, 2, 2, 2, 2, 2, 2, 2, 2, 2, 2, 2, 2, 4 ),
 ( 0.000000000000000000, 0.004420635650383453706, 0.006630953475575180993, 0.008841271300766907412, 0.01105158912595863470, 0.01215674803855450008, 0.01326190695115036199, 0.01768254260153383217, 0.01878770151412969755, 0.01989286042672556640, 0.02210317825191729715, 0.02431349607710902791, 0.02652381390230075867, 0.03094444955268424099, 0.03315476737787598216, 0.03536508520306772679 ),
 .UNSPECIFIED. ) ;
#13899=CARTESIAN_POINT ( 'NONE',  ( 3.944129661530210385, 0.000000000000000000, 0.000000000000000000 ) ) ;
#13901=EDGE_CURVE ( 'NONE', #6443, #11969, #1341, .T. ) ;
#13902=CIRCLE ( 'NONE', #4631, 0.9499999999999992895 ) ;
#13903=CARTESIAN_POINT ( 'NONE',  ( 3.674479682832311855, 1.933833928510312328, -0.7233581415293754979 ) ) ;
#13904=ADVANCED_FACE ( 'NONE', ( #12766 ), #12614, .F. ) ;
#13912=EDGE_CURVE ( 'NONE', #8675, #10024, #1834, .T. ) ;
#13914=DIRECTION ( 'NONE',  ( -1.000000000000000000, -0.000000000000000000, -0.000000000000000000 ) ) ;
#13916=ORIENTED_EDGE ( 'NONE', *, *, #13841, .T. ) ;
#13918=EDGE_CURVE ( 'NONE', #4018, #11132, #5511, .T. ) ;
#13919=CARTESIAN_POINT ( 'NONE',  ( 3.944129661530210385, 1.867491090171841117, 0.4951980309903491473 ) ) ;
#13923=DIRECTION ( 'NONE',  ( 0.000000000000000000, 0.000000000000000000, 1.000000000000000000 ) ) ;
#13925=ADVANCED_FACE ( 'NONE', ( #10493 ), #7965, .F. ) ;
#13929=LINE ( 'NONE', #9365, #11204 ) ;
#13933=ORIENTED_EDGE ( 'NONE', *, *, #8540, .T. ) ;
#13934=ADVANCED_FACE ( 'NONE', ( #6830 ), #13078, .T. ) ;
#13937=ORIENTED_EDGE ( 'NONE', *, *, #11759, .F. ) ;
#13938=DIRECTION ( 'NONE',  ( 0.000000000000000000, 0.000000000000000000, -1.000000000000000000 ) ) ;
#13939=DIRECTION ( 'NONE',  ( -1.000000000000000000, -0.000000000000000000, -0.000000000000000000 ) ) ;
#13941=AXIS2_PLACEMENT_3D ( 'NONE', #14165, #7151, #2544 ) ;
#13944=CARTESIAN_POINT ( 'NONE',  ( 3.809126238595077485, 1.878820374380962832, -0.7477401187409083994 ) ) ;
#13949=ORIENTED_EDGE ( 'NONE', *, *, #5733, .F. ) ;
#13950=CIRCLE ( 'NONE', #2730, 0.5000000000000002220 ) ;
#13952=CARTESIAN_POINT ( 'NONE',  ( 3.875000000000000000, 3.137999999999999901, 0.5000000000000002220 ) ) ;
#13961=CARTESIAN_POINT ( 'NONE',  ( 4.626489205401124849, 1.810545309228444255, 0.03721021400973596044 ) ) ;
#13965=ORIENTED_EDGE ( 'NONE', *, *, #14266, .F. ) ;
#13968=ORIENTED_EDGE ( 'NONE', *, *, #2947, .T. ) ;
#13970=DIRECTION ( 'NONE',  ( -1.000000000000000000, -0.000000000000000000, -0.000000000000000000 ) ) ;
#13975=DIRECTION ( 'NONE',  ( 8.659560562354890950E-17, 0.7071067811865509034, -0.7071067811865441310 ) ) ;
#13980=CIRCLE ( 'NONE', #11808, 0.2944999999999856066 ) ;
#13982=CARTESIAN_POINT ( 'NONE',  ( 3.874999999999999556, 3.137999999999999901, -1.320000000000000062 ) ) ;
#13984=ADVANCED_FACE ( 'NONE', ( #3606 ), #5035, .F. ) ;
#13985=CARTESIAN_POINT ( 'NONE',  ( 4.679414359322546346, 1.732195860677045118, -0.09958524941061751290 ) ) ;
#13986=EDGE_CURVE ( 'NONE', #2564, #10875, #111, .T. ) ;
#13989=AXIS2_PLACEMENT_3D ( 'NONE', #3271, #10240, #798 ) ;
#13993=ORIENTED_EDGE ( 'NONE', *, *, #13245, .T. ) ;
#13995=EDGE_LOOP ( 'NONE', ( #5359, #9610 ) ) ;
#13996=CARTESIAN_POINT ( 'NONE',  ( 3.876560711617219379, 3.137999999999999901, 0.000000000000000000 ) ) ;
#13997=EDGE_CURVE ( 'NONE', #6090, #6131, #10563, .T. ) ;
#13998=ADVANCED_FACE ( 'NONE', ( #4520 ), #9909, .T. ) ;
#13999=DIRECTION ( 'NONE',  ( 0.000000000000000000, 2.708891287835076134E-14, 1.000000000000000000 ) ) ;
#14004=CARTESIAN_POINT ( 'NONE',  ( 3.521940692902104431, 2.009083282330886622, -0.6610767032427503631 ) ) ;
#14009=ORIENTED_EDGE ( 'NONE', *, *, #12511, .F. ) ;
#14015=CARTESIAN_POINT ( 'NONE',  ( 2.807000000000000828, 1.679378605318042395, -1.941878605318058337 ) ) ;
#14021=CARTESIAN_POINT ( 'NONE',  ( 6.826491571325181695, -1.679378605318047946, -1.679378605318053497 ) ) ;
#14025=CARTESIAN_POINT ( 'NONE',  ( 3.426491571325181340, 2.038142229251666215, 0.6032823416034359676 ) ) ;
#14028=PLANE ( 'NONE',  #5419 ) ;
#14032=ORIENTED_EDGE ( 'NONE', *, *, #6771, .F. ) ;
#14034=CIRCLE ( 'NONE', #9419, 0.9999999999999998890 ) ;
#14035=AXIS2_PLACEMENT_3D ( 'NONE', #8137, #2539, #11646 ) ;
#14041=CARTESIAN_POINT ( 'NONE',  ( 4.670780491554178404, 1.730766616691212123, 0.1519652760568382388 ) ) ;
#14043=CYLINDRICAL_SURFACE ( 'NONE', #9124, 1.000000000000000888 ) ;
#14045=ORIENTED_EDGE ( 'NONE', *, *, #5028, .T. ) ;
#14048=DIRECTION ( 'NONE',  ( -1.000000000000000000, -0.000000000000000000, -0.000000000000000000 ) ) ;
#14050=FACE_BOUND ( 'NONE', #10447, .T. ) ;
#14054=AXIS2_PLACEMENT_3D ( 'NONE', #4930, #1156, #11806 ) ;
#14059=EDGE_CURVE ( 'NONE', #2897, #3063, #11124, .T. ) ;
#14062=CARTESIAN_POINT ( 'NONE',  ( 3.743770895704081614, 0.8757747662568124980, 0.4827512383967037524 ) ) ;
#14063=CYLINDRICAL_SURFACE ( 'NONE', #8182, 1.000000000000000000 ) ;
#14064=CIRCLE ( 'NONE', #5272, 0.2219999999999999751 ) ;
#14068=ORIENTED_EDGE ( 'NONE', *, *, #8245, .T. ) ;
#14072=DIRECTION ( 'NONE',  ( 1.000000000000000000, 0.000000000000000000, 0.000000000000000000 ) ) ;
#14087=FACE_OUTER_BOUND ( 'NONE', #14509, .T. ) ;
#14089=ORIENTED_EDGE ( 'NONE', *, *, #13879, .F. ) ;
#14090=EDGE_CURVE ( 'NONE', #2897, #7967, #7282, .T. ) ;
#14093=AXIS2_PLACEMENT_3D ( 'NONE', #11989, #1497, #332 ) ;
#14094=DIRECTION ( 'NONE',  ( 1.000000000000000000, 0.000000000000000000, 0.000000000000000000 ) ) ;
#14097=DIRECTION ( 'NONE',  ( -1.000000000000000000, -0.000000000000000000, -0.000000000000000000 ) ) ;
#14106=EDGE_CURVE ( 'NONE', #2690, #7890, #3087, .T. ) ;
#14107=UNCERTAINTY_MEASURE_WITH_UNIT (LENGTH_MEASURE( 1.000000000000000082E-05 ), #1449, 'distance_accuracy_value', 'NONE');
#14110=FACE_OUTER_BOUND ( 'NONE', #7987, .T. ) ;
#14111=EDGE_CURVE ( 'NONE', #8303, #7967, #2339, .T. ) ;
#14115=AXIS2_PLACEMENT_3D ( 'NONE', #9603, #10814, #7311 ) ;
#14117=CARTESIAN_POINT ( 'NONE',  ( 6.176491571325181340, -1.679378605318047946, -1.272378605318051248 ) ) ;
#14120=CIRCLE ( 'NONE', #2889, 2.070731779878276502 ) ;
#14122=CIRCLE ( 'NONE', #10956, 2.500000000000000444 ) ;
#14123=CARTESIAN_POINT ( 'NONE',  ( 4.613342449693359271, 1.747135830664880540, 0.1413303526058345416 ) ) ;
#14124=ORIENTED_EDGE ( 'NONE', *, *, #14539, .F. ) ;
#14130=EDGE_LOOP ( 'NONE', ( #12113, #14068, #8752, #11616 ) ) ;
#14133=EDGE_CURVE ( 'NONE', #6033, #1534, #12076, .T. ) ;
#14136=ORIENTED_EDGE ( 'NONE', *, *, #2931, .F. ) ;
#14137=CARTESIAN_POINT ( 'NONE',  ( 3.426491571325181340, -2.400000000000011902, -0.6999999999999596545 ) ) ;
#14138=CARTESIAN_POINT ( 'NONE',  ( 3.426491571325181340, -1.575000000000027489, -1.574999999999989297 ) ) ;
#14139=VECTOR ( 'NONE', #13278, 39.37007874015748143 ) ;
#14140=CARTESIAN_POINT ( 'NONE',  ( 3.713865648090597826, 1.916531464605631507, 0.7332543789835506143 ) ) ;
#14147=CARTESIAN_POINT ( 'NONE',  ( 3.875000000000000000, 0.8660254037844384856, 0.5000000000000002220 ) ) ;
#14148=FACE_BOUND ( 'NONE', #4546, .T. ) ;
#14152=CARTESIAN_POINT ( 'NONE',  ( 6.794491571325179891, -1.679378605318047946, -1.679378605318053497 ) ) ;
#14153=VERTEX_POINT ( 'NONE', #1587 ) ;
#14157=CARTESIAN_POINT ( 'NONE',  ( 3.920919094826833984, 1.873066083652677793, 0.4984382268710150776 ) ) ;
#14158=CARTESIAN_POINT ( 'NONE',  ( 6.794491571325179891, 1.679378605318035733, -1.679378605318065487 ) ) ;
#14164=ORIENTED_EDGE ( 'NONE', *, *, #5314, .F. ) ;
#14165=CARTESIAN_POINT ( 'NONE',  ( 3.874999999999999556, 2.750000000000000000, -1.320000000000000062 ) ) ;
#14166=CARTESIAN_POINT ( 'NONE',  ( 3.528591654644219311, 1.932956604557751534, -0.6650985988073745414 ) ) ;
#14169=EDGE_LOOP ( 'NONE', ( #300, #110, #6279, #1184 ) ) ;
#14173=CARTESIAN_POINT ( 'NONE',  ( 3.426491571325181340, 1.679378605318042395, -1.679378605318058604 ) ) ;
#14175=CARTESIAN_POINT ( 'NONE',  ( 3.898074040635628457, 1.878528703211115092, -0.5000000000000002220 ) ) ;
#14185=EDGE_CURVE ( 'NONE', #12765, #5558, #124, .T. ) ;
#14191=DIRECTION ( 'NONE',  ( 1.000000000000000000, 0.000000000000000000, 0.000000000000000000 ) ) ;
#14192=ADVANCED_FACE ( 'NONE', ( #946 ), #1111, .T. ) ;
#14197=CARTESIAN_POINT ( 'NONE',  ( 4.394406145971391453, 1.728430255068499788, -0.5437684957058670498 ) ) ;
#14198=ORIENTED_EDGE ( 'NONE', *, *, #8012, .F. ) ;
#14200=VERTEX_POINT ( 'NONE', #11006 ) ;
#14204=DIRECTION ( 'NONE',  ( -1.000000000000000000, -0.000000000000000000, -0.000000000000000000 ) ) ;
#14210=DIRECTION ( 'NONE',  ( -1.000000000000000000, -0.000000000000000000, -0.000000000000000000 ) ) ;
#14211=VECTOR ( 'NONE', #14481, 39.37007874015748143 ) ;
#14213=PRODUCT_DEFINITION_SHAPE ( 'NONE', 'NONE',  #14914 ) ;
#14217=CARTESIAN_POINT ( 'NONE',  ( 3.462756589970257703, 1.936639940275549199, 0.7054686714132032410 ) ) ;
#14218=CARTESIAN_POINT ( 'NONE',  ( 4.675740426773506542, 1.731584457788192921, -0.1243058436455859866 ) ) ;
#14220=ORIENTED_EDGE ( 'NONE', *, *, #14106, .F. ) ;
#14222=CARTESIAN_POINT ( 'NONE',  ( 6.826491571325181695, 1.679378605318059492, 1.679378605318041506 ) ) ;
#14223=ORIENTED_EDGE ( 'NONE', *, *, #12791, .F. ) ;
#14232=ORIENTED_EDGE ( 'NONE', *, *, #12596, .T. ) ;
#14236=DIRECTION ( 'NONE',  ( 1.000000000000000000, 0.000000000000000000, -1.224646799147353207E-16 ) ) ;
#14248=DIRECTION ( 'NONE',  ( 0.000000000000000000, 1.000000000000000000, 0.000000000000000000 ) ) ;
#14249=EDGE_CURVE ( 'NONE', #6864, #3105, #2181, .T. ) ;
#14254=CIRCLE ( 'NONE', #10357, 3.000000000000000444 ) ;
#14255=FACE_OUTER_BOUND ( 'NONE', #12274, .T. ) ;
#14259=CARTESIAN_POINT ( 'NONE',  ( 3.760674742763851164, 1.911053679983126141, -0.4872933924078399759 ) ) ;
#14261=VECTOR ( 'NONE', #11627, 39.37007874015748143 ) ;
#14266=EDGE_CURVE ( 'NONE', #10754, #6601, #812, .T. ) ;
#14275=ORIENTED_EDGE ( 'NONE', *, *, #3266, .T. ) ;
#14276=DIRECTION ( 'NONE',  ( 1.000000000000000000, 0.000000000000000000, 0.000000000000000000 ) ) ;
#14279=DIRECTION ( 'NONE',  ( -1.000000000000000000, -0.000000000000000000, -0.000000000000000000 ) ) ;
#14283=CARTESIAN_POINT ( 'NONE',  ( 3.944129661530210385, 0.000000000000000000, 0.000000000000000000 ) ) ;
#14286=DIRECTION ( 'NONE',  ( -0.000000000000000000, -1.000000000000000000, -0.000000000000000000 ) ) ;
#14290=CARTESIAN_POINT ( 'NONE',  ( 3.590089328403619273, 1.905315664284169541, 0.6937522868107603990 ) ) ;
#14291=DIRECTION ( 'NONE',  ( -1.000000000000000000, -0.000000000000000000, -0.000000000000000000 ) ) ;
#14292=ORIENTED_EDGE ( 'NONE', *, *, #14819, .T. ) ;
#14294=FACE_OUTER_BOUND ( 'NONE', #5748, .T. ) ;
#14295=EDGE_LOOP ( 'NONE', ( #10498, #12568, #10722, #1712 ) ) ;
#14299=AXIS2_PLACEMENT_3D ( 'NONE', #13303, #3990, #6219 ) ;
#14304=CIRCLE ( 'NONE', #9908, 0.3750000000000007772 ) ;
#14305=VECTOR ( 'NONE', #3832, 39.37007874015748143 ) ;
#14308=CARTESIAN_POINT ( 'NONE',  ( 3.426491571325181340, 2.400000000000011458, 0.6999999999999614309 ) ) ;
#14310=TOROIDAL_SURFACE ( 'NONE', #6512, 1.580000000000000071, 0.08000000000000000167 ) ;
#14311=CARTESIAN_POINT ( 'NONE',  ( 6.176491571325181340, -1.679378605318047946, -2.086378605318055968 ) ) ;
#14317=DIRECTION ( 'NONE',  ( 0.000000000000000000, 0.000000000000000000, -1.000000000000000000 ) ) ;
#14322=EDGE_CURVE ( 'NONE', #6459, #4442, #8226, .T. ) ;
#14324=AXIS2_PLACEMENT_3D ( 'NONE', #5057, #9720, #4046 ) ;
#14332=VERTEX_POINT ( 'NONE', #9309 ) ;
#14337=DIRECTION ( 'NONE',  ( -1.000000000000000000, -0.000000000000000000, -0.000000000000000000 ) ) ;
#14342=VECTOR ( 'NONE', #9337, 39.37007874015748143 ) ;
#14345=ORIENTED_EDGE ( 'NONE', *, *, #1168, .T. ) ;
#14347=ADVANCED_FACE ( 'NONE', ( #14255 ), #13808, .T. ) ;
#14348=LINE ( 'NONE', #335, #3107 ) ;
#14350=CONICAL_SURFACE ( 'NONE', #14115, 3.000000000000000444, 0.7853981633974415066 ) ;
#14358=CARTESIAN_POINT ( 'NONE',  ( 3.426491571325181340, 0.9799999999999438050, -2.360000000000016307 ) ) ;
#14361=DIRECTION ( 'NONE',  ( -0.000000000000000000, -1.000000000000000000, -0.000000000000000000 ) ) ;
#14364=CARTESIAN_POINT ( 'NONE',  ( 3.705204738311406842, 1.834542981759929470, 0.7866137051850492501 ) ) ;
#14365=DIRECTION ( 'NONE',  ( 0.000000000000000000, 0.000000000000000000, -1.000000000000000000 ) ) ;
#14367=DIRECTION ( 'NONE',  ( 0.000000000000000000, 0.000000000000000000, -1.000000000000000000 ) ) ;
#14368=CARTESIAN_POINT ( 'NONE',  ( 3.875000000000000000, 3.085321731235734610, 0.000000000000000000 ) ) ;
#14376=ORIENTED_EDGE ( 'NONE', *, *, #6154, .F. ) ;
#14386=FACE_OUTER_BOUND ( 'NONE', #5853, .T. ) ;
#14393=ORIENTED_EDGE ( 'NONE', *, *, #6538, .T. ) ;
#14399=VERTEX_POINT ( 'NONE', #8753 ) ;
#14402=CARTESIAN_POINT ( 'NONE',  ( 3.426491571325181340, 1.679378605318059048, 1.941878605318041462 ) ) ;
#14404=AXIS2_PLACEMENT_3D ( 'NONE', #10138, #934, #4404 ) ;
#14406=CARTESIAN_POINT ( 'NONE',  ( 6.208491571325183145, 1.679378605318059492, 1.679378605318041506 ) ) ;
#14409=EDGE_CURVE ( 'NONE', #9027, #8887, #5775, .T. ) ;
#14412=ORIENTED_EDGE ( 'NONE', *, *, #78, .F. ) ;
#14414=AXIS2_PLACEMENT_3D ( 'NONE', #269, #13055, #5965 ) ;
#14417=DIRECTION ( 'NONE',  ( 0.000000000000000000, 0.000000000000000000, -1.000000000000000000 ) ) ;
#14419=CARTESIAN_POINT ( 'NONE',  ( 3.426491571325181340, 1.964030041192035947, -0.6624825471404702792 ) ) ;
#14420=DIRECTION ( 'NONE',  ( 0.000000000000000000, -1.000000000000000000, 4.591341165822195764E-16 ) ) ;
#14422=ORIENTED_EDGE ( 'NONE', *, *, #7389, .F. ) ;
#14423=ORIENTED_EDGE ( 'NONE', *, *, #10014, .F. ) ;
#14424=ORIENTED_EDGE ( 'NONE', *, *, #6818, .T. ) ;
#14425=VECTOR ( 'NONE', #10013, 39.37007874015748143 ) ;
#14426=DIRECTION ( 'NONE',  ( 0.000000000000000000, 0.000000000000000000, 1.000000000000000000 ) ) ;
#14430=CARTESIAN_POINT ( 'NONE',  ( 6.826491571325181695, 1.679378605318035733, -2.086378605318067958 ) ) ;
#14431=EDGE_LOOP ( 'NONE', ( #6552, #5575, #9504, #7187, #1804 ) ) ;
#14439=CARTESIAN_POINT ( 'NONE',  ( 3.816981501931459242, 1.796899953488545698, 0.7979432928147958126 ) ) ;
#14440=CARTESIAN_POINT ( 'NONE',  ( 3.426491571325181340, 2.400000000000011458, 0.6999999999999614309 ) ) ;
#14441=VERTEX_POINT ( 'NONE', #13107 ) ;
#14442=CARTESIAN_POINT ( 'NONE',  ( 3.394491571325182644, 1.679378605318042395, -1.416878605318058870 ) ) ;
#14444=ORIENTED_EDGE ( 'NONE', *, *, #13709, .T. ) ;
#14448=ORIENTED_EDGE ( 'NONE', *, *, #7106, .T. ) ;
#14449=AXIS2_PLACEMENT_3D ( 'NONE', #2421, #12885, #8332 ) ;
#14467=AXIS2_PLACEMENT_3D ( 'NONE', #7075, #3700, #11736 ) ;
#14468=DIRECTION ( 'NONE',  ( 1.000000000000000000, 0.000000000000000000, 0.000000000000000000 ) ) ;
#14470=DIRECTION ( 'NONE',  ( -0.7071067811865421326, 0.000000000000000000, 0.7071067811865527908 ) ) ;
#14473=AXIS2_PLACEMENT_3D ( 'NONE', #8019, #4423, #3495 ) ;
#14481=DIRECTION ( 'NONE',  ( -0.000000000000000000, -1.000000000000000000, -0.000000000000000000 ) ) ;
#14482=CARTESIAN_POINT ( 'NONE',  ( 2.774999999999999911, 1.575000000000016609, 1.575000000000000178 ) ) ;
#14484=ADVANCED_FACE ( 'NONE', ( #7833 ), #6017, .T. ) ;
#14485=CARTESIAN_POINT ( 'NONE',  ( 4.525161324076911740, 1.792777560986625662, 0.3773916261770783320 ) ) ;
#14491=DIRECTION ( 'NONE',  ( 0.000000000000000000, 0.000000000000000000, -1.000000000000000000 ) ) ;
#14493=CARTESIAN_POINT ( 'NONE',  ( 4.298771110290672048, 0.9641137807165872653, 0.2658577392121701521 ) ) ;
#14494=DIRECTION ( 'NONE',  ( 0.000000000000000000, 1.000000000000000000, -4.591341165822195764E-16 ) ) ;
#14496=CIRCLE ( 'NONE', #4745, 0.2944999999999856066 ) ;
#14498=CARTESIAN_POINT ( 'NONE',  ( 2.527624975756972425, 3.137999999999999901, -0.9199802545633498640 ) ) ;
#14502=DIRECTION ( 'NONE',  ( 0.000000000000000000, 0.000000000000000000, -1.000000000000000000 ) ) ;
#14503=CARTESIAN_POINT ( 'NONE',  ( 3.426491571325181340, 0.9799999999999436939, -3.360000000000016751 ) ) ;
#14505=CIRCLE ( 'NONE', #8669, 0.2944999999999979301 ) ;
#14509=EDGE_LOOP ( 'NONE', ( #3831, #1609, #3209, #11589 ) ) ;
#14511=DIRECTION ( 'NONE',  ( -1.000000000000000000, -0.000000000000000000, -0.000000000000000000 ) ) ;
#14516=( NAMED_UNIT ( * ) SI_UNIT ( $, .STERADIAN. ) SOLID_ANGLE_UNIT ( ) );
#14518=ORIENTED_EDGE ( 'NONE', *, *, #1824, .F. ) ;
#14523=AXIS2_PLACEMENT_3D ( 'NONE', #8461, #7316, #13100 ) ;
#14527=VERTEX_POINT ( 'NONE', #11273 ) ;
#14532=LINE ( 'NONE', #2221, #10406 ) ;
#14533=CARTESIAN_POINT ( 'NONE',  ( 3.426491571325181340, 1.574999999999994849, -1.575000000000022160 ) ) ;
#14539=EDGE_CURVE ( 'NONE', #9198, #4559, #6618, .T. ) ;
#14543=DIRECTION ( 'NONE',  ( -1.000000000000000000, -0.000000000000000000, -0.000000000000000000 ) ) ;
#14547=DIRECTION ( 'NONE',  ( 0.000000000000000000, 0.000000000000000000, -1.000000000000000000 ) ) ;
#14550=EDGE_CURVE ( 'NONE', #4931, #8434, #1605, .T. ) ;
#14551=B_SPLINE_CURVE_WITH_KNOTS ( 'NONE', 3,
 ( #11322, #980, #9111, #8050, #3152, #12535, #5671, #4445, #5599, #4296, #11251, #10039 ),
 .UNSPECIFIED., .F., .F.,
 ( 4, 2, 2, 2, 2, 4 ),
 ( 0.000000000000000000, 0.003650815867420974421, 0.007301631734841948843, 0.009127039668552414803, 0.01095244760226288423, 0.01460326346968381268 ),
 .UNSPECIFIED. ) ;
#14554=CARTESIAN_POINT ( 'NONE',  ( 3.874999999999999556, 2.750000000000000000, -1.098000000000000087 ) ) ;
#14555=ORIENTED_EDGE ( 'NONE', *, *, #1108, .T. ) ;
#14561=DIRECTION ( 'NONE',  ( 0.000000000000000000, 0.000000000000000000, -1.000000000000000000 ) ) ;
#14563=DIRECTION ( 'NONE',  ( 1.000000000000000000, 0.000000000000000000, 0.000000000000000000 ) ) ;
#14564=CARTESIAN_POINT ( 'NONE',  ( 4.368012994362165280, 1.779897144447762702, 0.5670951116580714713 ) ) ;
#14569=CARTESIAN_POINT ( 'NONE',  ( 4.042576247476339368, 1.760009672272428993, -0.7323577104505313295 ) ) ;
#14572=EDGE_CURVE ( 'NONE', #4719, #14941, #698, .T. ) ;
#14576=CARTESIAN_POINT ( 'NONE',  ( 4.348909005209756984, 0.9871496092524738586, -0.1627569400240113373 ) ) ;
#14583=CARTESIAN_POINT ( 'NONE',  ( 3.426491571325181340, -2.360000000000016751, -0.9799999999999431388 ) ) ;
#14585=CARTESIAN_POINT ( 'NONE',  ( 6.826491571325181695, 0.000000000000000000, 0.000000000000000000 ) ) ;
#14586=FACE_OUTER_BOUND ( 'NONE', #14863, .T. ) ;
#14588=CARTESIAN_POINT ( 'NONE',  ( 4.487514378271046489, 1.732936262643785419, 0.4354029880432472299 ) ) ;
#14589=CARTESIAN_POINT ( 'NONE',  ( 3.426491571325181340, 2.359999999999994547, -1.575000000000016831 ) ) ;
#14591=EDGE_CURVE ( 'NONE', #7643, #2188, #3579, .T. ) ;
#14595=DIRECTION ( 'NONE',  ( 0.000000000000000000, 0.000000000000000000, 1.000000000000000000 ) ) ;
#14596=VERTEX_POINT ( 'NONE', #11425 ) ;
#14598=CIRCLE ( 'NONE', #4099, 0.3750000000000004996 ) ;
#14599=CARTESIAN_POINT ( 'NONE',  ( 3.944129661530210385, 1.761538328845252188, -0.7935532608319411096 ) ) ;
#14606=AXIS2_PLACEMENT_3D ( 'NONE', #13022, #4705, #11816 ) ;
#14611=AXIS2_PLACEMENT_3D ( 'NONE', #10050, #9125, #11107 ) ;
#14612=DIRECTION ( 'NONE',  ( -0.3420201433256623846, 0.000000000000000000, 0.9396926207859106484 ) ) ;
#14613=AXIS2_PLACEMENT_3D ( 'NONE', #14406, #9890, #14547 ) ;
#14618=CIRCLE ( 'NONE', #663, 0.1899999999999996136 ) ;
#14619=CARTESIAN_POINT ( 'NONE',  ( 6.215861650065340527, 0.000000000000000000, -3.000000000000000444 ) ) ;
#14621=ORIENTED_EDGE ( 'NONE', *, *, #8963, .F. ) ;
#14623=CYLINDRICAL_SURFACE ( 'NONE', #2282, 1.500000000000000222 ) ;
#14627=CARTESIAN_POINT ( 'NONE',  ( 4.344846310392954436, 3.137999999999999901, -1.491010071662831171 ) ) ;
#14632=VECTOR ( 'NONE', #3035, 39.37007874015748143 ) ;
#14643=CARTESIAN_POINT ( 'NONE',  ( 3.875000000000000000, 3.085321731235734610, -0.4849999999999995981 ) ) ;
#14644=VERTEX_POINT ( 'NONE', #14643 ) ;
#14645=DIRECTION ( 'NONE',  ( 0.000000000000000000, 0.000000000000000000, -1.000000000000000000 ) ) ;
#14648=DIRECTION ( 'NONE',  ( -1.000000000000000000, -0.000000000000000000, -0.000000000000000000 ) ) ;
#14652=AXIS2_PLACEMENT_3D ( 'NONE', #2324, #13939, #12793 ) ;
#14653=EDGE_CURVE ( 'NONE', #7301, #7227, #13551, .T. ) ;
#14659=DIRECTION ( 'NONE',  ( 0.000000000000000000, 0.000000000000000000, -1.000000000000000000 ) ) ;
#14661=EDGE_CURVE ( 'NONE', #8303, #7551, #11822, .T. ) ;
#14664=CARTESIAN_POINT ( 'NONE',  ( 3.875000000000000000, 0.8660254037844385966, -0.5000000000000002220 ) ) ;
#14668=B_SPLINE_CURVE_WITH_KNOTS ( 'NONE', 3,
 ( #5899, #893, #14911, #4438 ),
 .UNSPECIFIED., .F., .F.,
 ( 4, 4 ),
 ( 2.046485264934011349E-07, 0.001800564375689165265 ),
 .UNSPECIFIED. ) ;
#14671=DIRECTION ( 'NONE',  ( 0.000000000000000000, 0.000000000000000000, 1.000000000000000000 ) ) ;
#14672=CONICAL_SURFACE ( 'NONE', #5159, 0.2944999999999856066, 0.7853981633974514986 ) ;
#14673=CARTESIAN_POINT ( 'NONE',  ( 3.910795929945357408, 1.844675076806764569, 0.7500224038636267299 ) ) ;
#14675=ORIENTED_EDGE ( 'NONE', *, *, #8764, .T. ) ;
#14677=CARTESIAN_POINT ( 'NONE',  ( 6.176491571325181340, 1.679378605318035733, -1.679378605318065487 ) ) ;
#14682=DIRECTION ( 'NONE',  ( 0.000000000000000000, -1.000000000000000000, 0.000000000000000000 ) ) ;
#14684=EDGE_LOOP ( 'NONE', ( #2587, #13450, #3236, #3882 ) ) ;
#14688=CONICAL_SURFACE ( 'NONE', #11999, 0.2945000000000006501, 0.7853981633974503884 ) ;
#14692=ORIENTED_EDGE ( 'NONE', *, *, #10286, .T. ) ;
#14694=CARTESIAN_POINT ( 'NONE',  ( 3.388167464794443084, 0.9934776249054605435, -0.1151865398313142164 ) ) ;
#14704=CARTESIAN_POINT ( 'NONE',  ( 3.562574517356508430, 1.987638485117721343, -0.6822768319053587049 ) ) ;
#14711=CARTESIAN_POINT ( 'NONE',  ( 3.920936730114974456, 1.767235543727864400, 0.7960367706888703543 ) ) ;
#14713=ORIENTED_EDGE ( 'NONE', *, *, #10199, .T. ) ;
#14715=VECTOR ( 'NONE', #10508, 39.37007874015748143 ) ;
#14717=ORIENTED_EDGE ( 'NONE', *, *, #6862, .T. ) ;
#14723=AXIS2_PLACEMENT_3D ( 'NONE', #10054, #2073, #5388 ) ;
#14724=VERTEX_POINT ( 'NONE', #5855 ) ;
#14736=ADVANCED_FACE ( 'NONE', ( #11579 ), #11657, .F. ) ;
#14739=EDGE_CURVE ( 'NONE', #6953, #6615, #2542, .T. ) ;
#14745=CARTESIAN_POINT ( 'NONE',  ( 3.896946115134541255, 1.794690806442625020, 0.7506982253096490254 ) ) ;
#14748=EDGE_LOOP ( 'NONE', ( #11039, #1302, #5117, #14393, #2733, #8715 ) ) ;
#14762=CARTESIAN_POINT ( 'NONE',  ( 3.582695665244850058, 0.9139351410924635433, -0.4059821268960285834 ) ) ;
#14763=CARTESIAN_POINT ( 'NONE',  ( 4.531732933946797992, 1.713275703896695701, -0.4642236893194010006 ) ) ;
#14765=ORIENTED_EDGE ( 'NONE', *, *, #9399, .T. ) ;
#14768=ORIENTED_EDGE ( 'NONE', *, *, #5600, .T. ) ;
#14770=AXIS2_PLACEMENT_3D ( 'NONE', #14158, #1006, #13151 ) ;
#14775=DIRECTION ( 'NONE',  ( -1.000000000000000000, -0.000000000000000000, -0.000000000000000000 ) ) ;
#14777=VERTEX_POINT ( 'NONE', #2399 ) ;
#14779=CARTESIAN_POINT ( 'NONE',  ( 6.176491571325181340, 1.679378605318035733, -1.679378605318065487 ) ) ;
#14780=CARTESIAN_POINT ( 'NONE',  ( 3.629736278057476007, 1.863380661955394091, 0.7703184054743784648 ) ) ;
#14782=AXIS2_PLACEMENT_3D ( 'NONE', #2993, #5446, #3221 ) ;
#14788=EDGE_CURVE ( 'NONE', #5479, #6020, #9624, .T. ) ;
#14789=CARTESIAN_POINT ( 'NONE',  ( 3.426491571325181340, 0.000000000000000000, 0.000000000000000000 ) ) ;
#14791=LINE ( 'NONE', #1855, #11598 ) ;
#14793=CIRCLE ( 'NONE', #3070, 0.3750000000000004996 ) ;
#14795=AXIS2_PLACEMENT_3D ( 'NONE', #5050, #14361, #8356 ) ;
#14800=AXIS2_PLACEMENT_3D ( 'NONE', #8794, #13285, #12077 ) ;
#14801=CARTESIAN_POINT ( 'NONE',  ( 4.214877066107062475, 1.735343601526363022, -0.6696222561766873582 ) ) ;
#14803=VECTOR ( 'NONE', #1320, 39.37007874015748143 ) ;
#14806=ORIENTED_EDGE ( 'NONE', *, *, #12485, .T. ) ;
#14817=DIRECTION ( 'NONE',  ( 1.000000000000000000, 0.000000000000000000, 0.000000000000000000 ) ) ;
#14818=CARTESIAN_POINT ( 'NONE',  ( 4.292613398383279488, 1.780257219922917411, 0.6242760036277545943 ) ) ;
#14819=EDGE_CURVE ( 'NONE', #3024, #10523, #12053, .T. ) ;
#14820=CARTESIAN_POINT ( 'NONE',  ( 2.980731298636167370, 3.137999999999999901, -0.3249191361593797844 ) ) ;
#14821=EDGE_LOOP ( 'NONE', ( #15010, #14422, #11359, #10772 ) ) ;
#14829=ORIENTED_EDGE ( 'NONE', *, *, #10338, .T. ) ;
#14831=DIRECTION ( 'NONE',  ( -1.000000000000000000, -0.000000000000000000, -0.000000000000000000 ) ) ;
#14832=CARTESIAN_POINT ( 'NONE',  ( 2.774999999999999911, 1.679378605318059048, 1.679378605318041506 ) ) ;
#14839=CARTESIAN_POINT ( 'NONE',  ( 3.808373759217316579, 0.8679908749363488552, -0.4966365464873185309 ) ) ;
#14841=VECTOR ( 'NONE', #12142, 39.37007874015748143 ) ;
#14844=CARTESIAN_POINT ( 'NONE',  ( 4.239713504559157187, 0.9396297378138827039, -0.3424101421577204207 ) ) ;
#14849=VECTOR ( 'NONE', #15098, 39.37007874015748143 ) ;
#14850=EDGE_CURVE ( 'NONE', #4070, #11468, #14254, .T. ) ;
#14851=AXIS2_PLACEMENT_3D ( 'NONE', #10643, #14072, #1368 ) ;
#14861=CARTESIAN_POINT ( 'NONE',  ( 6.176491571325181340, -1.679378605318048390, 1.679378605318054163 ) ) ;
#14863=EDGE_LOOP ( 'NONE', ( #5707, #13089, #10095, #7220 ) ) ;
#14865=DIRECTION ( 'NONE',  ( 0.000000000000000000, 0.000000000000000000, 1.000000000000000000 ) ) ;
#14866=EDGE_LOOP ( 'NONE', ( #11366, #10843, #8590, #12863 ) ) ;
#14867=DIRECTION ( 'NONE',  ( -1.000000000000000000, -0.000000000000000000, -0.000000000000000000 ) ) ;
#14873=CARTESIAN_POINT ( 'NONE',  ( 2.807000000000000384, 1.679378605318059048, 1.416878605318041551 ) ) ;
#14881=CARTESIAN_POINT ( 'NONE',  ( 3.827026189994130245, 1.815548848758673506, -0.7493866505369201070 ) ) ;
#14882=ORIENTED_EDGE ( 'NONE', *, *, #147, .F. ) ;
#14887=DIRECTION ( 'NONE',  ( 0.000000000000000000, 0.000000000000000000, 1.000000000000000000 ) ) ;
#14890=DIRECTION ( 'NONE',  ( 0.000000000000000000, 0.000000000000000000, -1.000000000000000000 ) ) ;
#14891=ORIENTED_EDGE ( 'NONE', *, *, #14661, .F. ) ;
#14892=CARTESIAN_POINT ( 'NONE',  ( 3.126543437434640804, 2.500005182251167746, -0.01362379177072846510 ) ) ;
#14894=FACE_OUTER_BOUND ( 'NONE', #10989, .T. ) ;
#14896=ADVANCED_FACE ( 'NONE', ( #908 ), #827, .F. ) ;
#14898=CARTESIAN_POINT ( 'NONE',  ( 4.231255996368110672, 1.713208384118555250, 0.7116634002984181251 ) ) ;
#14901=ORIENTED_EDGE ( 'NONE', *, *, #4389, .T. ) ;
#14911=CARTESIAN_POINT ( 'NONE',  ( 3.897996994672882742, 1.878547046383948205, 0.4999999999999717448 ) ) ;
#14914=PRODUCT_DEFINITION ( 'UNKNOWN', '', #12555, #8163 ) ;
#14916=VERTEX_POINT ( 'NONE', #12541 ) ;
#14917=DIRECTION ( 'NONE',  ( 0.000000000000000000, 0.000000000000000000, -1.000000000000000000 ) ) ;
#14921=CARTESIAN_POINT ( 'NONE',  ( 2.774999999999999911, 1.574999999999994849, -1.575000000000022160 ) ) ;
#14925=VERTEX_POINT ( 'NONE', #6519 ) ;
#14926=MECHANICAL_DESIGN_GEOMETRIC_PRESENTATION_REPRESENTATION('',(#4671),#11017);
#14928=CARTESIAN_POINT ( 'NONE',  ( 3.426491571325181340, -2.360000000000000320, 0.9799999999999999822 ) ) ;
#14931=DIRECTION ( 'NONE',  ( 0.000000000000000000, -1.000000000000000000, 1.423315761404775650E-14 ) ) ;
#14935=VERTEX_POINT ( 'NONE', #5607 ) ;
#14938=DIRECTION ( 'NONE',  ( 0.000000000000000000, 0.000000000000000000, -1.000000000000000000 ) ) ;
#14941=VERTEX_POINT ( 'NONE', #1756 ) ;
#14943=CARTESIAN_POINT ( 'NONE',  ( 6.208491571325183145, -1.679378605318048390, 1.679378605318054163 ) ) ;
#14945=ORIENTED_EDGE ( 'NONE', *, *, #11494, .F. ) ;
#14948=CARTESIAN_POINT ( 'NONE',  ( 3.874999999999999556, 3.137999999999999901, 1.320000000000000062 ) ) ;
#14949=CARTESIAN_POINT ( 'NONE',  ( 3.759712767994416893, 1.920664053109024660, 0.4870725753588067697 ) ) ;
#14953=CARTESIAN_POINT ( 'NONE',  ( 3.563625566911128750, 1.891043865854203920, -0.7492590735562228987 ) ) ;
#14958=ORIENTED_EDGE ( 'NONE', *, *, #2538, .T. ) ;
#14962=EDGE_CURVE ( 'NONE', #14153, #11308, #548, .T. ) ;
#14968=DIRECTION ( 'NONE',  ( 1.000000000000000000, 0.000000000000000000, 0.000000000000000000 ) ) ;
#14970=CARTESIAN_POINT ( 'NONE',  ( 4.623575768221273030, 1.748705500634446297, -0.06916614078429211832 ) ) ;
#14974=DIRECTION ( 'NONE',  ( 0.000000000000000000, 1.000000000000000000, 0.000000000000000000 ) ) ;
#14976=VERTEX_POINT ( 'NONE', #3225 ) ;
#14978=LINE ( 'NONE', #9029, #7053 ) ;
#14982=ORIENTED_EDGE ( 'NONE', *, *, #10119, .F. ) ;
#14984=CARTESIAN_POINT ( 'NONE',  ( 6.794491571325179891, -1.679378605318047946, -1.304378605318053053 ) ) ;
#14985=DIRECTION ( 'NONE',  ( 0.000000000000000000, 0.000000000000000000, -1.000000000000000000 ) ) ;
#14992=CARTESIAN_POINT ( 'NONE',  ( 4.180771277348069859, 1.718521109949383785, -0.7338151851141401227 ) ) ;
#14994=DIRECTION ( 'NONE',  ( 0.000000000000000000, 0.000000000000000000, 1.000000000000000000 ) ) ;
#14995=CARTESIAN_POINT ( 'NONE',  ( 3.874999999999999556, 3.137999999999999901, -1.509999999999999787 ) ) ;
#14999=ORIENTED_EDGE ( 'NONE', *, *, #7036, .F. ) ;
#15001=DIRECTION ( 'NONE',  ( 0.000000000000000000, -1.000000000000000000, 0.000000000000000000 ) ) ;
#15003=AXIS2_PLACEMENT_3D ( 'NONE', #7806, #12459, #12124 ) ;
#15010=ORIENTED_EDGE ( 'NONE', *, *, #3641, .F. ) ;
#15013=ORIENTED_EDGE ( 'NONE', *, *, #8540, .F. ) ;
#15015=ADVANCED_FACE ( 'NONE', ( #4303 ), #14623, .T. ) ;
#15024=CARTESIAN_POINT ( 'NONE',  ( 4.170088648937899656, 1.789706488608662216, -0.6902842372149408101 ) ) ;
#15025=VECTOR ( 'NONE', #5303, 39.37007874015748143 ) ;
#15026=AXIS2_PLACEMENT_3D ( 'NONE', #7217, #11944, #13999 ) ;
#15027=DIRECTION ( 'NONE',  ( -1.000000000000000000, -0.000000000000000000, -0.000000000000000000 ) ) ;
#15028=ORIENTED_EDGE ( 'NONE', *, *, #10795, .T. ) ;
#15029=EDGE_CURVE ( 'NONE', #8673, #6601, #4685, .T. ) ;
#15032=CARTESIAN_POINT ( 'NONE',  ( 3.426491571325181340, 0.000000000000000000, 0.000000000000000000 ) ) ;
#15033=EDGE_LOOP ( 'NONE', ( #5129, #444, #4060, #3582 ) ) ;
#15038=DIRECTION ( 'NONE',  ( -0.9396926207859107594, 0.000000000000000000, -0.3420201433256624401 ) ) ;
#15042=CARTESIAN_POINT ( 'NONE',  ( 3.193454851037015985, 2.480721379492803358, 0.3109605352214736551 ) ) ;
#15046=VECTOR ( 'NONE', #2055, 39.37007874015748854 ) ;
#15047=AXIS2_PLACEMENT_3D ( 'NONE', #8246, #172, #5783 ) ;
#15050=CARTESIAN_POINT ( 'NONE',  ( 4.616151631548642165, 1.808401919742543607, 0.1257952528007890425 ) ) ;
#15053=EDGE_LOOP ( 'NONE', ( #13472, #15134, #6458, #11280 ) ) ;
#15057=CARTESIAN_POINT ( 'NONE',  ( 3.394491571325183088, 1.679378605318059048, 1.416878605318041551 ) ) ;
#15071=LINE ( 'NONE', #4596, #1905 ) ;
#15072=CARTESIAN_POINT ( 'NONE',  ( 3.569546097624230807, 0.9179547258387925623, 0.3971843845618320268 ) ) ;
#15073=CARTESIAN_POINT ( 'NONE',  ( 4.135359820172126000, 1.724334728327786559, 0.7510612840505229704 ) ) ;
#15075=AXIS2_PLACEMENT_3D ( 'NONE', #115, #2590, #9408 ) ;
#15077=ORIENTED_EDGE ( 'NONE', *, *, #4474, .F. ) ;
#15079=EDGE_LOOP ( 'NONE', ( #11396, #11388, #426, #783 ) ) ;
#15086=EDGE_CURVE ( 'NONE', #7643, #11264, #5972, .T. ) ;
#15094=CARTESIAN_POINT ( 'NONE',  ( 2.774999999999999911, -1.679378605318059048, -1.679378605318041950 ) ) ;
#15095=EDGE_LOOP ( 'NONE', ( #3619, #3686, #5724, #4699 ) ) ;
#15098=DIRECTION ( 'NONE',  ( -0.7071067811865460184, 8.659560562354951347E-17, -0.7071067811865490160 ) ) ;
#15099=B_SPLINE_CURVE_WITH_KNOTS ( 'NONE', 3,
 ( #9090, #7863, #11299, #11379, #12513, #648, #3043, #13583, #7712, #5572, #13733, #6646, #11231, #3127, #12370, #10091, #1884, #6574 ),
 .UNSPECIFIED., .F., .F.,
 ( 4, 2, 2, 2, 2, 2, 2, 2, 4 ),
 ( 4.557956953634194787E-07, 0.003683485157311049835, 0.005524999838118879909, 0.007366514518926710851, 0.008287271859330638465, 0.009208029199734566947, 0.01104954388054238575, 0.01289105856135020454, 0.01473257324215802161 ),
 .UNSPECIFIED. ) ;
#15102=CIRCLE ( 'NONE', #3385, 1.000000000000000000 ) ;
#15105=VERTEX_POINT ( 'NONE', #12934 ) ;
#15106=AXIS2_PLACEMENT_3D ( 'NONE', #3366, #10327, #4595 ) ;
#15112=CIRCLE ( 'NONE', #2171, 0.2625000000000000111 ) ;
#15120=EDGE_CURVE ( 'NONE', #626, #4833, #5646, .T. ) ;
#15126=CARTESIAN_POINT ( 'NONE',  ( 4.663405195611884047, 1.729552445905039981, -0.1874371909834770533 ) ) ;
#15128=DIRECTION ( 'NONE',  ( 0.000000000000000000, 0.000000000000000000, 1.000000000000000000 ) ) ;
#15131=ORIENTED_EDGE ( 'NONE', *, *, #9058, .T. ) ;
#15134=ORIENTED_EDGE ( 'NONE', *, *, #14739, .F. ) ;
#15135=DIRECTION ( 'NONE',  ( -0.000000000000000000, -1.000000000000000000, -0.000000000000000000 ) ) ;
#15137=FACE_BOUND ( 'NONE', #9249, .T. ) ;
#15143=CARTESIAN_POINT ( 'NONE',  ( 0.000000000000000000, 0.000000000000000000, 0.000000000000000000 ) ) ;
#15148=CARTESIAN_POINT ( 'NONE',  ( 3.426491571325181340, 1.679378605318059048, 1.416878605318041551 ) ) ;
#15165=COLOUR_RGB('Dark Blue',0.08,0.2,0.34);
#15166=FILL_AREA_STYLE_COLOUR('',#15165);
#15167=FILL_AREA_STYLE('',(#15166));
#15168=SURFACE_STYLE_FILL_AREA(#15167);
#15169=SURFACE_SIDE_STYLE('',(#15168));
#15170=SURFACE_STYLE_USAGE(.BOTH.,#15169);
#15171=PRESENTATION_STYLE_ASSIGNMENT((#15170));
ENDSEC;
END-ISO-10303-21;
